ISO-10303-21;
HEADER;
/* Generated by software containing ST-Developer
 * from STEP Tools, Inc. (www.steptools.com) 
 */

FILE_DESCRIPTION(
/* description */ (''),
/* implementation_level */ '2;1');

FILE_NAME(
/* name */ 'Screw.step',
/* time_stamp */ '2026-10-06T13:15:55-07:00',
/* author */ (''),
/* organization */ (''),
/* preprocessor_version */ 'ST-DEVELOPER v20.2',
/* originating_system */ 'Autodesk Translation Framework v15.15.0.0',
/* authorisation */ '');

FILE_SCHEMA (('AUTOMOTIVE_DESIGN { 1 0 10303 214 3 1 1 }'));
ENDSEC;

DATA;
#10=MECHANICAL_DESIGN_GEOMETRIC_PRESENTATION_REPRESENTATION('',(#113),#27707);
#93=SHAPE_REPRESENTATION_RELATIONSHIP('SRR','None',#27750,#103);
#103=ADVANCED_BREP_SHAPE_REPRESENTATION('',(#123),#27702);
#113=STYLED_ITEM('',(#27804),#123);
#123=MANIFOLD_SOLID_BREP('Body1',#3839);
#139=FACE_BOUND('',#789,.T.);
#140=FACE_BOUND('',#791,.T.);
#141=FACE_BOUND('',#793,.T.);
#190=PLANE('',#4080);
#191=PLANE('',#4089);
#192=PLANE('',#4090);
#193=PLANE('',#4091);
#248=CIRCLE('',#4066,3.72275);
#249=CIRCLE('',#4073,3.72275);
#250=CIRCLE('',#4075,4.433);
#251=CIRCLE('',#4076,4.433);
#252=CIRCLE('',#4078,1.77625);
#253=CIRCLE('',#4079,1.77625);
#254=CIRCLE('',#4081,2.204);
#255=CIRCLE('',#4082,2.204);
#256=CIRCLE('',#4084,2.204);
#257=CIRCLE('',#4085,2.204);
#258=CIRCLE('',#4087,5.42440960677665);
#259=CIRCLE('',#4088,5.42440960677665);
#382=CYLINDRICAL_SURFACE('',#4065,3.72275);
#383=CYLINDRICAL_SURFACE('',#4067,3.72275);
#384=CYLINDRICAL_SURFACE('',#4068,3.72275);
#385=CYLINDRICAL_SURFACE('',#4069,3.72275);
#386=CYLINDRICAL_SURFACE('',#4070,3.72275);
#387=CYLINDRICAL_SURFACE('',#4071,3.72275);
#388=CYLINDRICAL_SURFACE('',#4072,3.72275);
#389=CYLINDRICAL_SURFACE('',#4074,4.433);
#390=CYLINDRICAL_SURFACE('',#4077,1.77625);
#391=CYLINDRICAL_SURFACE('',#4083,2.204);
#392=CYLINDRICAL_SURFACE('',#4086,5.42440960677665);
#540=FACE_OUTER_BOUND('',#772,.T.);
#541=FACE_OUTER_BOUND('',#773,.T.);
#542=FACE_OUTER_BOUND('',#774,.T.);
#543=FACE_OUTER_BOUND('',#775,.T.);
#544=FACE_OUTER_BOUND('',#776,.T.);
#545=FACE_OUTER_BOUND('',#777,.T.);
#546=FACE_OUTER_BOUND('',#778,.T.);
#547=FACE_OUTER_BOUND('',#779,.T.);
#548=FACE_OUTER_BOUND('',#780,.T.);
#549=FACE_OUTER_BOUND('',#781,.T.);
#550=FACE_OUTER_BOUND('',#782,.T.);
#551=FACE_OUTER_BOUND('',#783,.T.);
#552=FACE_OUTER_BOUND('',#784,.T.);
#553=FACE_OUTER_BOUND('',#785,.T.);
#554=FACE_OUTER_BOUND('',#786,.T.);
#555=FACE_OUTER_BOUND('',#787,.T.);
#556=FACE_OUTER_BOUND('',#788,.T.);
#557=FACE_OUTER_BOUND('',#790,.T.);
#558=FACE_OUTER_BOUND('',#792,.T.);
#772=EDGE_LOOP('',(#2987,#2988,#2989,#2990));
#773=EDGE_LOOP('',(#2991,#2992,#2993,#2994));
#774=EDGE_LOOP('',(#2995,#2996,#2997,#2998));
#775=EDGE_LOOP('',(#2999,#3000,#3001,#3002));
#776=EDGE_LOOP('',(#3003,#3004,#3005,#3006));
#777=EDGE_LOOP('',(#3007,#3008,#3009,#3010));
#778=EDGE_LOOP('',(#3011,#3012,#3013,#3014,#3015,#3016));
#779=EDGE_LOOP('',(#3017,#3018,#3019,#3020,#3021,#3022,#3023,#3024,#3025,
#3026,#3027,#3028,#3029,#3030,#3031,#3032,#3033,#3034));
#780=EDGE_LOOP('',(#3035,#3036,#3037,#3038,#3039));
#781=EDGE_LOOP('',(#3040,#3041,#3042,#3043));
#782=EDGE_LOOP('',(#3044,#3045,#3046,#3047,#3048));
#783=EDGE_LOOP('',(#3049,#3050,#3051,#3052,#3053,#3054));
#784=EDGE_LOOP('',(#3055,#3056,#3057,#3058,#3059,#3060,#3061,#3062));
#785=EDGE_LOOP('',(#3063,#3064,#3065,#3066,#3067,#3068,#3069,#3070,#3071,
#3072,#3073,#3074,#3075,#3076,#3077,#3078,#3079,#3080,#3081));
#786=EDGE_LOOP('',(#3082,#3083,#3084,#3085,#3086,#3087,#3088,#3089,#3090,
#3091,#3092,#3093,#3094,#3095,#3096,#3097,#3098,#3099,#3100));
#787=EDGE_LOOP('',(#3101,#3102,#3103,#3104));
#788=EDGE_LOOP('',(#3105));
#789=EDGE_LOOP('',(#3106,#3107,#3108,#3109,#3110));
#790=EDGE_LOOP('',(#3111,#3112,#3113,#3114,#3115));
#791=EDGE_LOOP('',(#3116,#3117,#3118,#3119,#3120));
#792=EDGE_LOOP('',(#3121));
#793=EDGE_LOOP('',(#3122));
#1024=LINE('',#7645,#1200);
#1025=LINE('',#7975,#1201);
#1026=LINE('',#8319,#1202);
#1027=LINE('',#8653,#1203);
#1028=LINE('',#8983,#1204);
#1029=LINE('',#9319,#1205);
#1030=LINE('',#14727,#1206);
#1031=LINE('',#15524,#1207);
#1200=VECTOR('',#4619,3.72275);
#1201=VECTOR('',#4624,3.72275);
#1202=VECTOR('',#4627,3.72275);
#1203=VECTOR('',#4630,3.72275);
#1204=VECTOR('',#4633,3.72275);
#1205=VECTOR('',#4636,3.72275);
#1206=VECTOR('',#4663,2.204);
#1207=VECTOR('',#4670,5.42440960677665);
#1390=B_SPLINE_CURVE_WITH_KNOTS('',3,(#7647,#7648,#7649,#7650,#7651,#7652,
#7653,#7654,#7655,#7656,#7657,#7658,#7659,#7660,#7661,#7662,#7663,#7664,
#7665,#7666,#7667,#7668,#7669,#7670,#7671,#7672,#7673,#7674,#7675,#7676,
#7677,#7678,#7679,#7680,#7681,#7682,#7683,#7684,#7685,#7686,#7687,#7688,
#7689,#7690,#7691,#7692,#7693,#7694,#7695,#7696,#7697,#7698,#7699,#7700,
#7701,#7702,#7703,#7704,#7705,#7706,#7707,#7708,#7709,#7710,#7711,#7712,
#7713,#7714,#7715,#7716,#7717,#7718,#7719,#7720,#7721,#7722,#7723,#7724,
#7725,#7726,#7727,#7728,#7729,#7730,#7731,#7732,#7733,#7734,#7735,#7736,
#7737,#7738,#7739,#7740,#7741,#7742,#7743,#7744,#7745,#7746,#7747,#7748,
#7749,#7750,#7751,#7752,#7753,#7754,#7755,#7756,#7757,#7758,#7759,#7760,
#7761,#7762,#7763,#7764,#7765,#7766,#7767,#7768,#7769,#7770,#7771,#7772,
#7773,#7774,#7775,#7776,#7777,#7778,#7779,#7780,#7781,#7782,#7783,#7784,
#7785,#7786,#7787,#7788,#7789,#7790,#7791,#7792,#7793,#7794,#7795,#7796,
#7797,#7798,#7799,#7800,#7801,#7802,#7803,#7804,#7805,#7806,#7807,#7808,
#7809,#7810,#7811,#7812,#7813,#7814,#7815,#7816,#7817,#7818,#7819,#7820,
#7821,#7822,#7823,#7824,#7825,#7826,#7827,#7828,#7829,#7830,#7831,#7832,
#7833),.UNSPECIFIED.,.F.,.F.,(4,3,3,3,3,3,3,3,3,3,3,3,3,3,3,3,3,3,3,3,3,
3,3,3,3,3,3,3,3,3,3,3,3,3,3,3,3,3,3,3,3,3,3,3,3,3,3,3,3,3,3,3,3,3,3,3,3,
3,3,3,3,3,4),(10.3850888958016,10.4641373814769,10.5520588327897,10.6410762182378,
10.7288594652779,10.8166179102709,10.9043752172213,10.9943308920096,11.0822044534747,
11.1676514039115,11.1732011849246,11.2524595516301,11.2641583632187,11.2641979163745,
11.3459974247077,11.3543883418031,11.4444664958327,11.5344565843787,11.6243852832326,
11.7142815564214,11.804167167181,11.8940638650899,11.9840486455302,12.074077267802,
12.1642488110667,12.2472698528716,12.247304603897,12.3294279854305,12.337349377077,
12.4272819895897,12.517126854226,12.6069114553117,12.6966643802678,12.786407578033,
12.8761629846047,12.9660091578037,13.0559004439681,13.1459382866182,13.2303745458392,
13.2304112914194,13.3122318951338,13.3202803122904,13.4100337681398,13.4996963272619,
13.5892945887802,13.6788587810357,13.7684110716423,13.8579736136466,13.947625011734,
14.0373201915803,14.1271617222868,14.2075665015184,14.2134811498394,14.2135179789419,
14.2954243505238,14.3034962162208,14.3933692649306,14.4831592957879,14.5728884092593,
14.6625930287075,14.7522802792272,14.8420075718479,14.9177889943201),
 .UNSPECIFIED.);
#1391=B_SPLINE_CURVE_WITH_KNOTS('',3,(#7836,#7837,#7838,#7839,#7840,#7841,
#7842,#7843,#7844,#7845,#7846,#7847,#7848,#7849,#7850,#7851,#7852,#7853,
#7854,#7855,#7856,#7857,#7858,#7859,#7860,#7861,#7862,#7863,#7864,#7865,
#7866,#7867,#7868,#7869,#7870,#7871,#7872,#7873,#7874,#7875,#7876,#7877,
#7878,#7879,#7880,#7881,#7882,#7883,#7884,#7885,#7886,#7887,#7888,#7889,
#7890,#7891,#7892,#7893,#7894,#7895,#7896,#7897,#7898,#7899,#7900,#7901,
#7902,#7903,#7904,#7905,#7906,#7907,#7908,#7909,#7910,#7911,#7912,#7913,
#7914,#7915,#7916,#7917,#7918,#7919,#7920,#7921,#7922,#7923,#7924,#7925,
#7926,#7927,#7928,#7929,#7930,#7931,#7932,#7933,#7934,#7935,#7936,#7937,
#7938,#7939,#7940,#7941,#7942,#7943,#7944,#7945,#7946,#7947,#7948,#7949,
#7950,#7951,#7952,#7953,#7954,#7955,#7956,#7957,#7958,#7959,#7960,#7961,
#7962,#7963,#7964,#7965,#7966,#7967,#7968,#7969,#7970,#7971),
 .UNSPECIFIED.,.F.,.F.,(4,3,3,3,3,3,3,3,3,3,3,3,3,3,3,3,3,3,3,3,3,3,3,3,
3,3,3,3,3,3,3,3,3,3,3,3,3,3,3,3,3,3,3,3,3,4),(11.6150691238056,11.716887748291,
11.818807396451,11.9206982029579,12.0224123053014,12.106615918772,12.1066224675668,
12.1974625342849,12.2882944241597,12.379171523673,12.4700739203339,12.561061507472,
12.598175811328,12.5981975387223,12.6813394695241,12.6891753523971,12.7800935403341,
12.8709528368157,12.9617902529354,13.0526187338464,13.1434585576012,13.2343300061399,
13.3253148905754,13.4163587789532,13.5075598865992,13.5812824988505,13.5813185969407,
13.66123779196,13.6704071444793,13.7594059294644,13.8483044456942,13.9378150382791,
14.0265967435875,14.1153607025908,14.2041298440541,14.2941946796338,14.3830904507549,
14.4737398185639,14.5549025675923,14.5643891863729,14.5644292218501,14.6449085802043,
14.6545593024114,14.7446311850219,14.8346130791444,14.9185733201878),
 .UNSPECIFIED.);
#1392=B_SPLINE_CURVE_WITH_KNOTS('',3,(#7976,#7977,#7978,#7979,#7980,#7981,
#7982,#7983,#7984,#7985,#7986,#7987,#7988,#7989,#7990,#7991,#7992,#7993,
#7994,#7995,#7996,#7997,#7998,#7999,#8000,#8001,#8002,#8003,#8004,#8005,
#8006,#8007,#8008,#8009,#8010,#8011,#8012,#8013,#8014,#8015,#8016,#8017,
#8018,#8019,#8020,#8021,#8022,#8023,#8024,#8025,#8026,#8027,#8028,#8029,
#8030,#8031,#8032,#8033,#8034,#8035,#8036,#8037,#8038,#8039,#8040,#8041,
#8042,#8043,#8044,#8045,#8046,#8047,#8048,#8049,#8050,#8051,#8052,#8053,
#8054,#8055,#8056,#8057,#8058,#8059,#8060,#8061,#8062,#8063,#8064,#8065,
#8066,#8067,#8068,#8069,#8070,#8071,#8072,#8073,#8074,#8075,#8076,#8077,
#8078,#8079,#8080,#8081,#8082,#8083,#8084,#8085,#8086,#8087,#8088,#8089,
#8090,#8091,#8092,#8093,#8094,#8095,#8096,#8097,#8098,#8099,#8100,#8101,
#8102,#8103,#8104,#8105,#8106,#8107,#8108,#8109,#8110,#8111,#8112,#8113,
#8114,#8115,#8116,#8117,#8118,#8119,#8120,#8121,#8122,#8123,#8124,#8125,
#8126,#8127,#8128,#8129,#8130,#8131,#8132,#8133,#8134,#8135,#8136,#8137,
#8138,#8139,#8140,#8141,#8142,#8143,#8144,#8145,#8146,#8147),
 .UNSPECIFIED.,.F.,.F.,(4,2,2,2,2,2,2,2,2,2,2,2,2,2,2,2,2,2,2,2,2,2,2,2,
2,2,2,2,2,2,2,2,2,2,2,2,2,2,2,2,2,2,2,2,2,2,2,2,2,2,2,2,2,2,2,2,2,2,2,2,
2,2,2,2,2,2,2,2,2,2,2,2,2,2,2,2,2,2,2,2,2,2,2,2,2,4),(-2.34349935747219,
-2.32479321244631,-2.3115095086961,-2.30353059275682,-2.29532108129983,
-2.28088936810031,-2.26189886696644,-2.20929781208258,-2.15450652873946,
-2.13394329508488,-2.12155686493844,-2.10788626489361,-2.08783834376536,
-2.03424657964964,-1.95860390922288,-1.94507668101036,-1.93704913924088,
-1.92889606131535,-1.91474449864053,-1.89626288592835,-1.84654371676776,
-1.78804151246791,-1.76738860818391,-1.75361468301218,-1.73969844149924,
-1.71824200221813,-1.69214031600218,-1.62636836462047,-1.58789145006146,
-1.57643226148622,-1.56877805451772,-1.55996076245785,-1.54234252694852,
-1.51710804433584,-1.47285455929373,-1.42093470919277,-1.40050503777244,
-1.38814022198954,-1.37444924313941,-1.35427615186781,-1.30006083507845,
-1.22569587408321,-1.21196384643384,-1.2038950116354,-1.19578131764764,
-1.18183742260512,-1.13378381169967,-1.05260288386253,-1.03294463075192,
-1.01947068923136,-1.00535317643753,-0.982805291875028,-0.921353089151828,
-0.858204884788433,-0.844923691725052,-0.836944277344367,-0.828737610032856,
-0.81430811178137,-0.795319608194366,-0.742722325438803,-0.687907248193089,
-0.667347214427635,-0.654966036493293,-0.641304419454002,-0.621277994696126,
-0.567810711042773,-0.491908125022253,-0.47842388550636,-0.470408074913927,
-0.462255044052201,-0.448086925837385,-0.429574435509035,-0.379697817459574,
-0.321252544528174,-0.300590533312429,-0.286816292445277,-0.27290500586233,
-0.251468064151761,-0.225396140987684,-0.159778836579698,-0.121158200649779,
-0.109685408742185,-0.102018673693576,-0.0931614321386275,-0.0754292161435672,
-0.000158205331122453),.UNSPECIFIED.);
#1393=B_SPLINE_CURVE_WITH_KNOTS('',3,(#8148,#8149,#8150,#8151,#8152,#8153,
#8154,#8155,#8156,#8157,#8158,#8159,#8160,#8161,#8162,#8163,#8164,#8165,
#8166,#8167,#8168,#8169,#8170,#8171,#8172,#8173,#8174,#8175,#8176,#8177,
#8178,#8179,#8180,#8181,#8182,#8183,#8184,#8185,#8186,#8187,#8188,#8189,
#8190,#8191,#8192,#8193,#8194,#8195,#8196,#8197,#8198,#8199,#8200,#8201,
#8202,#8203,#8204,#8205,#8206,#8207,#8208,#8209,#8210,#8211,#8212,#8213,
#8214,#8215,#8216,#8217,#8218,#8219,#8220,#8221,#8222,#8223,#8224,#8225,
#8226,#8227,#8228,#8229,#8230,#8231,#8232,#8233,#8234,#8235,#8236,#8237,
#8238,#8239,#8240,#8241,#8242,#8243,#8244,#8245,#8246,#8247,#8248,#8249,
#8250,#8251,#8252,#8253,#8254,#8255,#8256,#8257,#8258,#8259,#8260,#8261,
#8262,#8263,#8264,#8265,#8266,#8267,#8268,#8269,#8270,#8271,#8272,#8273,
#8274,#8275,#8276,#8277,#8278,#8279,#8280,#8281,#8282,#8283,#8284,#8285,
#8286,#8287,#8288,#8289,#8290,#8291,#8292,#8293,#8294,#8295,#8296,#8297,
#8298,#8299,#8300,#8301,#8302,#8303,#8304,#8305,#8306,#8307,#8308,#8309,
#8310,#8311,#8312,#8313,#8314,#8315),.UNSPECIFIED.,.F.,.F.,(4,2,2,2,2,2,
2,2,2,2,2,2,2,2,2,2,2,2,2,2,2,2,2,2,2,2,2,2,2,2,2,2,2,2,2,2,2,2,2,2,2,2,
2,2,2,2,2,2,2,2,2,2,2,2,2,2,2,2,2,2,2,2,2,2,2,2,2,2,2,2,2,2,2,2,2,2,2,2,
2,2,2,2,2,4),(-12.0121045471319,-11.9908765110274,-11.9746552288482,-11.9620401761327,
-11.9485323873418,-11.9311366610153,-11.8881357893894,-11.8073824176125,
-11.7892270360545,-11.7801851308519,-11.772439210027,-11.7608113343547,
-11.7188325800486,-11.6562211330763,-11.6307170509891,-11.6096421761874,
-11.5958396202625,-11.5820863501214,-11.5612988389604,-11.4917675903954,
-11.4492693879947,-11.4322152629272,-11.4188825625983,-11.4109381992301,
-11.4028732288876,-11.3889027591304,-11.3361610911638,-11.2654114051204,
-11.2430699259675,-11.2290912255745,-11.215769797557,-11.1963964587597,
-11.1134640302362,-11.0662228114669,-11.0524250800485,-11.0443936055418,
-11.0363673713181,-11.0227534785367,-10.9629834042421,-10.9148133988729,
-10.8922381306211,-10.8729136314128,-10.8593852164036,-10.8451946670713,
-10.8221064791139,-10.7287784010119,-10.7051397925194,-10.6883037169419,
-10.679635851479,-10.6720470804712,-10.66039924893,-10.6164842479188,-10.5373715822647,
-10.512352604061,-10.4978361838047,-10.4845081137113,-10.4663250505177,
-10.4114707069489,-10.3547296673,-10.3350754146237,-10.3202982198305,-10.3120482621597,
-10.3041857562166,-10.2913544933126,-10.2231672905296,-10.1654515082249,
-10.1432424285699,-10.1292419722719,-10.1158244545399,-10.0961572061151,
-10.015350938565,-9.97964995117286,-9.96415391429196,-9.95172596416459,
-9.94393776729407,-9.93556012340714,-9.9201582013566,-9.85052325946428,
-9.79061306498618,-9.77224860026096,-9.75888936619271,-9.74443089117664,
-9.71976128169862,-9.66952787558574),.UNSPECIFIED.);
#1394=B_SPLINE_CURVE_WITH_KNOTS('',3,(#8320,#8321,#8322,#8323,#8324,#8325,
#8326,#8327,#8328,#8329,#8330,#8331,#8332,#8333,#8334,#8335,#8336,#8337,
#8338,#8339,#8340,#8341,#8342,#8343,#8344,#8345,#8346,#8347,#8348,#8349,
#8350,#8351,#8352,#8353,#8354,#8355,#8356,#8357,#8358,#8359,#8360,#8361,
#8362,#8363,#8364,#8365,#8366,#8367,#8368,#8369,#8370,#8371,#8372,#8373,
#8374,#8375,#8376,#8377,#8378,#8379,#8380,#8381,#8382,#8383,#8384,#8385,
#8386,#8387,#8388,#8389,#8390,#8391,#8392,#8393,#8394,#8395,#8396,#8397,
#8398,#8399,#8400,#8401,#8402,#8403,#8404,#8405,#8406,#8407,#8408,#8409,
#8410,#8411,#8412,#8413,#8414,#8415,#8416,#8417,#8418,#8419,#8420,#8421,
#8422,#8423,#8424,#8425,#8426,#8427,#8428,#8429,#8430,#8431,#8432,#8433,
#8434,#8435,#8436,#8437,#8438,#8439,#8440,#8441,#8442,#8443,#8444,#8445,
#8446,#8447,#8448,#8449,#8450,#8451,#8452,#8453,#8454,#8455,#8456,#8457,
#8458,#8459,#8460,#8461,#8462,#8463,#8464,#8465,#8466,#8467,#8468,#8469,
#8470,#8471,#8472,#8473,#8474,#8475,#8476,#8477,#8478,#8479,#8480,#8481,
#8482,#8483,#8484,#8485),.UNSPECIFIED.,.F.,.F.,(4,2,2,2,2,2,2,2,2,2,2,2,
2,2,2,2,2,2,2,2,2,2,2,2,2,2,2,2,2,2,2,2,2,2,2,2,2,2,2,2,2,2,2,2,2,2,2,2,
2,2,2,2,2,2,2,2,2,2,2,2,2,2,2,2,2,2,2,2,2,2,2,2,2,2,2,2,2,2,2,2,2,2,4),
(-4.6872551568627,-4.68453856924504,-4.66991807190972,-4.64460086592956,
-4.56421223924462,-4.52178108697756,-4.51014758765552,-4.50254083643499,
-4.49383144259538,-4.47681210054929,-4.45282204631766,-4.40676877106719,
-4.35448822173273,-4.33403881478831,-4.321668850125,-4.30797717731899,-4.28781372718408,
-4.26388279683943,-4.20976031928825,-4.15941791454452,-4.14557393886306,
-4.13748201867114,-4.1293941168964,-4.11557044478061,-4.0685869812435,-3.98550638224759,
-3.96609140230899,-3.95265842757976,-3.93848031642065,-3.91558953360281,
-3.86196741561931,-3.79000665350435,-3.77756736530792,-3.77051785566562,
-3.76235952107894,-3.74818642975285,-3.72966710361026,-3.67974873853684,
-3.62148726597934,-3.6008363620686,-3.58706086041255,-3.5731407583426,-3.55167337024444,
-3.52555474014413,-3.45969282291043,-3.42130908118452,-3.40985398308619,
-3.40219898424307,-3.39337584403388,-3.37573324200417,-3.35044936600466,
-3.25350740040407,-3.23342896032252,-3.21988899860481,-3.20587950474091,
-3.18391045542044,-3.15692710154751,-3.08537325705784,-3.05349803705644,
-3.04252959462255,-3.03494038312588,-3.02586770177019,-3.0068014010698,
-2.97841342525751,-2.88489320431958,-2.86566867336246,-2.85226716735696,
-2.83803779896376,-2.814857777735,-2.76064875846864,-2.69018708794146,-2.67757867507596,
-2.67050158217975,-2.66239083688479,-2.64844934808739,-2.6003981139853,
-2.51916721540283,-2.49951326823847,-2.48604394833592,-2.47193328112946,
-2.44940233342474,-2.38777167582929,-2.34349935747219),.UNSPECIFIED.);
#1395=B_SPLINE_CURVE_WITH_KNOTS('',3,(#8486,#8487,#8488,#8489,#8490,#8491,
#8492,#8493,#8494,#8495,#8496,#8497,#8498,#8499,#8500,#8501,#8502,#8503,
#8504,#8505,#8506,#8507,#8508,#8509,#8510,#8511,#8512,#8513,#8514,#8515,
#8516,#8517,#8518,#8519,#8520,#8521,#8522,#8523,#8524,#8525,#8526,#8527,
#8528,#8529,#8530,#8531,#8532,#8533,#8534,#8535,#8536,#8537,#8538,#8539,
#8540,#8541,#8542,#8543,#8544,#8545,#8546,#8547,#8548,#8549,#8550,#8551,
#8552,#8553,#8554,#8555,#8556,#8557,#8558,#8559,#8560,#8561,#8562,#8563,
#8564,#8565,#8566,#8567,#8568,#8569,#8570,#8571,#8572,#8573,#8574,#8575,
#8576,#8577,#8578,#8579,#8580,#8581,#8582,#8583,#8584,#8585,#8586,#8587,
#8588,#8589,#8590,#8591,#8592,#8593,#8594,#8595,#8596,#8597,#8598,#8599,
#8600,#8601,#8602,#8603,#8604,#8605,#8606,#8607,#8608,#8609,#8610,#8611,
#8612,#8613,#8614,#8615,#8616,#8617,#8618,#8619,#8620,#8621,#8622,#8623,
#8624,#8625,#8626,#8627,#8628,#8629,#8630,#8631,#8632,#8633,#8634,#8635,
#8636,#8637,#8638,#8639,#8640,#8641,#8642,#8643,#8644,#8645,#8646,#8647,
#8648,#8649),.UNSPECIFIED.,.F.,.F.,(4,2,2,2,2,2,2,2,2,2,2,2,2,2,2,2,2,2,
2,2,2,2,2,2,2,2,2,2,2,2,2,2,2,2,2,2,2,2,2,2,2,2,2,2,2,2,2,2,2,2,2,2,2,2,
2,2,2,2,2,2,2,2,2,2,2,2,2,2,2,2,2,2,2,2,2,2,2,2,2,2,2,4),(-9.66952787558574,
-9.62868542371412,-9.60520062981699,-9.58844533869582,-9.57980828371517,
-9.57222901153777,-9.56059480413288,-9.5170778567058,-9.43763536439442,
-9.41252443129322,-9.39798885206807,-9.38466240087352,-9.36651121024875,
-9.31294936426819,-9.2386478440979,-9.22184860523329,-9.21320585112177,
-9.20563196293017,-9.19402541406683,-9.15136526291876,-9.07126042488672,
-9.04599378470264,-9.03142938571179,-9.01811100797761,-9.00002543686721,
-8.94863083498729,-8.87500555804877,-8.85628683614255,-8.84729887989887,
-8.83973898748868,-8.82876790080423,-8.79659998462749,-8.72534295999101,
-8.69843461298902,-8.67652777274758,-8.66257503441782,-8.64910702303971,
-8.62917941511827,-8.53970141911645,-8.4958980082845,-8.48434227946981,
-8.4766999086319,-8.46799791967759,-8.45088493681171,-8.3830111739851,-8.32401611422044,
-8.30569223340769,-8.29234017454075,-8.27786956648423,-8.2531273293098,
-8.16209894991134,-8.13861306244888,-8.1218569329555,-8.11322081777102,
-8.10564173854272,-8.0940105026094,-8.05065722445383,-7.97106403955552,
-7.94591453942605,-7.9313693142187,-7.91804111436483,-7.89989863184858,
-7.8467945305261,-7.77463105200812,-7.75614643313473,-7.74719805924447,
-7.73962754296779,-7.72857957716986,-7.69604972364799,-7.62518263866841,
-7.59832788401122,-7.57645115790679,-7.56250267368732,-7.54902878339568,
-7.52907323922341,-7.45052320627916,-7.40075949487996,-7.38665625180731,
-7.37853516625404,-7.37055265491604,-7.35713706650612,-7.32614666109582),
 .UNSPECIFIED.);
#1396=B_SPLINE_CURVE_WITH_KNOTS('',3,(#8654,#8655,#8656,#8657,#8658,#8659,
#8660,#8661,#8662,#8663,#8664,#8665,#8666,#8667,#8668,#8669,#8670,#8671,
#8672,#8673,#8674,#8675,#8676,#8677,#8678,#8679,#8680,#8681,#8682,#8683,
#8684,#8685,#8686,#8687,#8688,#8689,#8690,#8691,#8692,#8693,#8694,#8695,
#8696,#8697,#8698,#8699,#8700,#8701,#8702,#8703,#8704,#8705,#8706,#8707,
#8708,#8709,#8710,#8711,#8712,#8713,#8714,#8715,#8716,#8717,#8718,#8719,
#8720,#8721,#8722,#8723,#8724,#8725,#8726,#8727,#8728,#8729,#8730,#8731,
#8732,#8733,#8734,#8735,#8736,#8737,#8738,#8739,#8740,#8741,#8742,#8743,
#8744,#8745,#8746,#8747,#8748,#8749,#8750,#8751,#8752,#8753,#8754,#8755,
#8756,#8757,#8758,#8759,#8760,#8761,#8762,#8763,#8764,#8765,#8766,#8767,
#8768,#8769,#8770,#8771,#8772,#8773,#8774,#8775,#8776,#8777,#8778,#8779,
#8780,#8781,#8782,#8783,#8784,#8785,#8786,#8787,#8788,#8789,#8790,#8791,
#8792,#8793,#8794,#8795,#8796,#8797,#8798,#8799,#8800,#8801,#8802,#8803,
#8804,#8805,#8806,#8807,#8808,#8809,#8810,#8811,#8812,#8813,#8814,#8815,
#8816,#8817,#8818,#8819),.UNSPECIFIED.,.F.,.F.,(4,2,2,2,2,2,2,2,2,2,2,2,
2,2,2,2,2,2,2,2,2,2,2,2,2,2,2,2,2,2,2,2,2,2,2,2,2,2,2,2,2,2,2,2,2,2,2,2,
2,2,2,2,2,2,2,2,2,2,2,2,2,2,2,2,2,2,2,2,2,2,2,2,2,2,2,2,2,2,2,2,2,2,4),
(-7.03092428991815,-6.97855283092003,-6.9263091663785,-6.90343298259714,
-6.88925830885356,-6.87582481163164,-6.85640239143679,-6.77333102668129,
-6.72630900129152,-6.71248092785882,-6.70439254001495,-6.69630206458313,
-6.68246413762466,-6.63222946623531,-6.57807897662565,-6.554145369954,-6.53397925550643,
-6.52028767087055,-6.50791875477817,-6.48747398280066,-6.43534194700939,
-6.38047727199338,-6.36110356835586,-6.34646347389874,-6.33821192318486,
-6.33026471659157,-6.31714721189776,-6.25137040240187,-6.19216694575456,
-6.16968526743576,-6.1555819194505,-6.14210405022866,-6.12240866899558,
-6.04140145475523,-6.0057936227912,-5.98440903922514,-5.97471869973732,
-5.9672018270527,-5.95727813229174,-5.93262002789266,-5.88946728917574,
-5.82201903183326,-5.80124641436259,-5.78744961801039,-5.7735531340635,
-5.75221782649401,-5.72632447723042,-5.66182519233804,-5.62189284919537,
-5.61029382386929,-5.60269250544359,-5.59396870881027,-5.57687042216555,
-5.55271825777665,-5.50690128728101,-5.45467183960923,-5.43422541324809,
-5.42185618649729,-5.40816452564173,-5.3879993507525,-5.31231040573843,
-5.2598117547567,-5.24583363617778,-5.23771458731285,-5.22965305611284,
-5.21596019245505,-5.17012076798599,-5.08502266380873,-5.06588440242545,
-5.05249442002963,-5.0382359272281,-5.01490587903616,-4.97003309320845,
-4.89123397820596,-4.8782316604893,-4.87030666715579,-4.86202490906503,
-4.8472341505162,-4.82758384494265,-4.77097978873096,-4.71615769979187,
-4.69792986251239,-4.6872551568627),.UNSPECIFIED.);
#1397=B_SPLINE_CURVE_WITH_KNOTS('',3,(#8820,#8821,#8822,#8823,#8824,#8825,
#8826,#8827,#8828,#8829,#8830,#8831,#8832,#8833,#8834,#8835,#8836,#8837,
#8838,#8839,#8840,#8841,#8842,#8843,#8844,#8845,#8846,#8847,#8848,#8849,
#8850,#8851,#8852,#8853,#8854,#8855,#8856,#8857,#8858,#8859,#8860,#8861,
#8862,#8863,#8864,#8865,#8866,#8867,#8868,#8869,#8870,#8871,#8872,#8873,
#8874,#8875,#8876,#8877,#8878,#8879,#8880,#8881,#8882,#8883,#8884,#8885,
#8886,#8887,#8888,#8889,#8890,#8891,#8892,#8893,#8894,#8895,#8896,#8897,
#8898,#8899,#8900,#8901,#8902,#8903,#8904,#8905,#8906,#8907,#8908,#8909,
#8910,#8911,#8912,#8913,#8914,#8915,#8916,#8917,#8918,#8919,#8920,#8921,
#8922,#8923,#8924,#8925,#8926,#8927,#8928,#8929,#8930,#8931,#8932,#8933,
#8934,#8935,#8936,#8937,#8938,#8939,#8940,#8941,#8942,#8943,#8944,#8945,
#8946,#8947,#8948,#8949,#8950,#8951,#8952,#8953,#8954,#8955,#8956,#8957,
#8958,#8959,#8960,#8961,#8962,#8963,#8964,#8965,#8966,#8967,#8968,#8969,
#8970,#8971,#8972,#8973,#8974,#8975,#8976,#8977,#8978,#8979),
 .UNSPECIFIED.,.F.,.F.,(4,2,2,2,2,2,2,2,2,2,2,2,2,2,2,2,2,2,2,2,2,2,2,2,
2,2,2,2,2,2,2,2,2,2,2,2,2,2,2,2,2,2,2,2,2,2,2,2,2,2,2,2,2,2,2,2,2,2,2,2,
2,2,2,2,2,2,2,2,2,2,2,2,2,2,2,2,2,2,2,4),(-7.32614666109582,-7.28096698223301,
-7.23562803637869,-7.21162934426962,-7.19729251320309,-7.18388375068752,
-7.16518217490911,-7.07722444883571,-7.03289792320862,-7.01940820560591,
-7.01141074740473,-7.00330563531193,-6.98928302806448,-6.93614518328078,
-6.8652480833897,-6.84317515560592,-6.82919042136076,-6.81574073928767,
-6.79593493623575,-6.71611341835179,-6.67992048340898,-6.6643005392503,
-6.65179695153731,-6.64399069092723,-6.63563088050373,-6.62032620712114,
-6.55055504570233,-6.49490052330849,-6.47460941120627,-6.46094246774894,
-6.44866670606722,-6.42855563745406,-6.33050714358575,-6.3058821414785,
-6.28856916654671,-6.27982905235152,-6.27219739126771,-6.26072068633731,
-6.22143949391177,-6.15631346069807,-6.13034405198082,-6.10898157803086,
-6.0951242581727,-6.08141294441578,-6.06087434513043,-6.00605848692176,
-5.93686821031972,-5.92097174994566,-5.91249654995843,-5.90475289072757,
-5.8926001789557,-5.83630947403731,-5.76145077257432,-5.74111113201973,
-5.72879829778636,-5.71516775213148,-5.69510030327021,-5.64110693300335,
-5.56611671133825,-5.55249555007277,-5.54447069556817,-5.53639182697379,
-5.52250401970487,-5.4747323679861,-5.39293308176922,-5.37338080834743,
-5.3599708437162,-5.3459196567532,-5.32349191688792,-5.26930329735693,-5.19693781019109,
-5.1845653948362,-5.17754835921317,-5.16942952970917,-5.15534350812577,
-5.10575287413854,-5.02695703768258,-5.00703131203136,-4.99356017536515,
-4.98211504750834),.UNSPECIFIED.);
#1398=B_SPLINE_CURVE_WITH_KNOTS('',3,(#8984,#8985,#8986,#8987,#8988,#8989,
#8990,#8991,#8992,#8993,#8994,#8995,#8996,#8997,#8998,#8999,#9000,#9001,
#9002,#9003,#9004,#9005,#9006,#9007,#9008,#9009,#9010,#9011,#9012,#9013,
#9014,#9015,#9016,#9017,#9018,#9019,#9020,#9021,#9022,#9023,#9024,#9025,
#9026,#9027,#9028,#9029,#9030,#9031,#9032,#9033,#9034,#9035,#9036,#9037,
#9038,#9039,#9040,#9041,#9042,#9043,#9044,#9045,#9046,#9047,#9048,#9049,
#9050,#9051,#9052,#9053,#9054,#9055,#9056,#9057,#9058,#9059,#9060,#9061,
#9062,#9063,#9064,#9065,#9066,#9067,#9068,#9069,#9070,#9071,#9072,#9073,
#9074,#9075,#9076,#9077,#9078,#9079,#9080,#9081,#9082,#9083,#9084,#9085,
#9086,#9087,#9088,#9089,#9090,#9091,#9092,#9093,#9094,#9095,#9096,#9097,
#9098,#9099,#9100,#9101,#9102,#9103,#9104,#9105,#9106,#9107,#9108,#9109,
#9110,#9111,#9112,#9113,#9114,#9115,#9116,#9117,#9118,#9119,#9120,#9121,
#9122,#9123,#9124,#9125,#9126,#9127,#9128,#9129,#9130,#9131,#9132,#9133,
#9134,#9135,#9136,#9137,#9138,#9139,#9140,#9141,#9142,#9143,#9144,#9145,
#9146,#9147),.UNSPECIFIED.,.F.,.F.,(4,2,2,2,2,2,2,2,2,2,2,2,2,2,2,2,2,2,
2,2,2,2,2,2,2,2,2,2,2,2,2,2,2,2,2,2,2,2,2,2,2,2,2,2,2,2,2,2,2,2,2,2,2,2,
2,2,2,2,2,2,2,2,2,2,2,2,2,2,2,2,2,2,2,2,2,2,2,2,2,2,2,4),(-9.37444697003052,
-9.36860397369544,-9.32240173150912,-9.29849118483135,-9.28151276112979,
-9.27281267140479,-9.26520583183669,-9.25356126267184,-9.2107091024805,
-9.13071309151711,-9.10548397620025,-9.09088184965157,-9.07748882582584,
-9.05922923026725,-9.00257070167362,-8.9259559883791,-8.9123957957723,-8.90436198580832,
-8.89621588766257,-8.88210060219873,-8.81098892561669,-8.7547756043323,
-8.73437099593029,-8.72063943506135,-8.70830829152862,-8.68810220976385,
-8.61149871851205,-8.5561222885708,-8.54418314931867,-8.53645223412902,
-8.52783466528434,-8.51130300976799,-8.44279842169963,-8.38776072769088,
-8.36751487256203,-8.35381126284092,-8.34145724310435,-8.32109916431765,
-8.24603712495091,-8.18947470268103,-8.17752065648051,-8.16978766483035,
-8.16117659025836,-8.14467861603178,-8.06941895795403,-8.02739637637241,
-8.00397748130146,-7.98970468931823,-7.97632563747552,-7.95724656237035,
-7.87170706103843,-7.82609223850768,-7.8124264037268,-7.80437132627203,
-7.79624833559249,-7.78224667498632,-7.72949532573729,-7.65826525661566,
-7.6361217363585,-7.62208137192172,-7.60856501126946,-7.58862503459442,
-7.50964021201676,-7.46018559008857,-7.44609043288053,-7.43794855465407,
-7.42991066299454,-7.41633158194777,-7.34105716007606,-7.30218464586766,
-7.27405119537271,-7.25893610676225,-7.24566259847408,-7.22872678051576,
-7.18881191312969,-7.11805910413513,-7.09647688090981,-7.08066848294191,
-7.07218839087097,-7.06448383369831,-7.05225199715093,-7.03092428991815),
 .UNSPECIFIED.);
#1399=B_SPLINE_CURVE_WITH_KNOTS('',3,(#9148,#9149,#9150,#9151,#9152,#9153,
#9154,#9155,#9156,#9157,#9158,#9159,#9160,#9161,#9162,#9163,#9164,#9165,
#9166,#9167,#9168,#9169,#9170,#9171,#9172,#9173,#9174,#9175,#9176,#9177,
#9178,#9179,#9180,#9181,#9182,#9183,#9184,#9185,#9186,#9187,#9188,#9189,
#9190,#9191,#9192,#9193,#9194,#9195,#9196,#9197,#9198,#9199,#9200,#9201,
#9202,#9203,#9204,#9205,#9206,#9207,#9208,#9209,#9210,#9211,#9212,#9213,
#9214,#9215,#9216,#9217,#9218,#9219,#9220,#9221,#9222,#9223,#9224,#9225,
#9226,#9227,#9228,#9229,#9230,#9231,#9232,#9233,#9234,#9235,#9236,#9237,
#9238,#9239,#9240,#9241,#9242,#9243,#9244,#9245,#9246,#9247,#9248,#9249,
#9250,#9251,#9252,#9253,#9254,#9255,#9256,#9257,#9258,#9259,#9260,#9261,
#9262,#9263,#9264,#9265,#9266,#9267,#9268,#9269,#9270,#9271,#9272,#9273,
#9274,#9275,#9276,#9277,#9278,#9279,#9280,#9281,#9282,#9283,#9284,#9285,
#9286,#9287,#9288,#9289,#9290,#9291,#9292,#9293,#9294,#9295,#9296,#9297,
#9298,#9299,#9300,#9301,#9302,#9303,#9304,#9305,#9306,#9307,#9308,#9309,
#9310,#9311,#9312,#9313,#9314,#9315),.UNSPECIFIED.,.F.,.F.,(4,2,2,2,2,2,
2,2,2,2,2,2,2,2,2,2,2,2,2,2,2,2,2,2,2,2,2,2,2,2,2,2,2,2,2,2,2,2,2,2,2,2,
2,2,2,2,2,2,2,2,2,2,2,2,2,2,2,2,2,2,2,2,2,2,2,2,2,2,2,2,2,2,2,2,2,2,2,2,
2,2,2,2,2,4),(-4.98211504750834,-4.97960063193846,-4.95767565633769,-4.93073742230588,
-4.85935336811027,-4.82722732298744,-4.81625866099638,-4.80869677205353,
-4.79970127835455,-4.78095312169327,-4.753247623603,-4.68632185495199,-4.65136073286413,
-4.63500893476475,-4.62184838259256,-4.60624279295363,-4.57488647608268,
-4.52845309893571,-4.46513173709856,-4.45187972741629,-4.44392892090097,
-4.43576821840269,-4.42147248844589,-4.40271013950669,-4.35133310384803,
-4.29487929009314,-4.27431309268189,-4.26059668695628,-4.24674418205149,
-4.22541069965359,-4.19948872683417,-4.13467796516697,-4.09494221816735,
-4.0834447470089,-4.07588466633776,-4.0671875456654,-4.05011034884746,-4.02597442541414,
-3.98013192947666,-3.92785853677376,-3.90744713109667,-3.89512343885818,
-3.88150545087404,-3.86150946815811,-3.80802560135013,-3.73209523135118,
-3.71862757412871,-3.71063378109328,-3.70252226173147,-3.68847150651585,
-3.63920649586705,-3.5598911169119,-3.54002811680221,-3.52656777128116,
-3.51259426797233,-3.49059036191807,-3.46351470430398,-3.3911513437316,
-3.36007613184864,-3.34920897924011,-3.3416594071886,-3.33260637130064,
-3.31352175143696,-3.28506136826114,-3.19168175786884,-3.17245815755866,
-3.15910160745751,-3.14496299393442,-3.12205151671813,-3.07705551532191,
-2.99731067183335,-2.98448858784473,-2.9766218488312,-2.96835271732448,
-2.95351112578539,-2.93374400027773,-2.87627457967711,-2.82246247762319,
-2.80430138815174,-2.79096846613929,-2.77642633681938,-2.75130610660706,
-2.6718338395991,-2.63816549894618),.UNSPECIFIED.);
#1400=B_SPLINE_CURVE_WITH_KNOTS('',3,(#9320,#9321,#9322,#9323,#9324,#9325,
#9326,#9327,#9328,#9329,#9330,#9331,#9332,#9333,#9334,#9335,#9336,#9337,
#9338,#9339,#9340,#9341,#9342,#9343,#9344,#9345,#9346,#9347,#9348,#9349,
#9350,#9351,#9352,#9353,#9354,#9355,#9356,#9357,#9358,#9359,#9360,#9361,
#9362,#9363,#9364,#9365,#9366,#9367,#9368,#9369,#9370,#9371,#9372,#9373,
#9374,#9375,#9376,#9377,#9378,#9379,#9380,#9381,#9382,#9383,#9384,#9385,
#9386,#9387,#9388,#9389,#9390,#9391,#9392,#9393,#9394,#9395,#9396,#9397,
#9398,#9399,#9400,#9401,#9402,#9403,#9404,#9405,#9406,#9407,#9408,#9409,
#9410,#9411,#9412,#9413,#9414,#9415,#9416,#9417,#9418,#9419,#9420,#9421,
#9422,#9423,#9424,#9425,#9426,#9427,#9428,#9429,#9430,#9431,#9432,#9433,
#9434,#9435,#9436,#9437,#9438,#9439,#9440,#9441,#9442,#9443,#9444,#9445,
#9446,#9447,#9448,#9449,#9450,#9451,#9452,#9453,#9454,#9455,#9456,#9457,
#9458,#9459,#9460,#9461,#9462,#9463,#9464,#9465,#9466,#9467,#9468,#9469,
#9470,#9471,#9472,#9473,#9474,#9475,#9476,#9477,#9478,#9479,#9480,#9481,
#9482,#9483),.UNSPECIFIED.,.F.,.F.,(4,2,2,2,2,2,2,2,2,2,2,2,2,2,2,2,2,2,
2,2,2,2,2,2,2,2,2,2,2,2,2,2,2,2,2,2,2,2,2,2,2,2,2,2,2,2,2,2,2,2,2,2,2,2,
2,2,2,2,2,2,2,2,2,2,2,2,2,2,2,2,2,2,2,2,2,2,2,2,2,2,2,4),(-11.7176550926435,
-11.6925733333226,-11.670571262262,-11.6565557431794,-11.6430192663134,
-11.6229712773436,-11.543612482416,-11.4936466144152,-11.4795004301893,
-11.4713674999825,-11.4634062931843,-11.4500711400182,-11.3734355996136,
-11.320362171509,-11.3004333139884,-11.2868375303002,-11.2745205372655,
-11.2540919076865,-11.2014722057254,-11.146861212341,-11.1275458236573,
-11.112950609905,-11.1047354431383,-11.0967929517176,-11.0837127825482,
-11.0054137050487,-10.9602462437258,-10.9369010099404,-10.9226173072797,
-10.9091894597464,-10.8899633117181,-10.7920467278553,-10.7664454448966,
-10.7486491603722,-10.7397812883413,-10.7321194339839,-10.7206742944183,
-10.6824566401323,-10.6165618956935,-10.5904516488257,-10.5689918274307,
-10.5550779902243,-10.5413098404039,-10.5206744784597,-10.4633509001598,
-10.4125741270717,-10.3938986263645,-10.3796419541323,-10.3714719607649,
-10.364441687959,-10.3520919246372,-10.2794662596866,-10.2263183271194,
-10.2034913183482,-10.1893322088993,-10.175904787544,-10.1564765109787,
-10.0735119782026,-10.026436619268,-10.0126063537849,-10.0045206903181,
-9.99742920909095,-9.98473853621118,-9.91504126037811,-9.85921237518751,
-9.836600994619,-9.82247262646748,-9.8090067897254,-9.78939512477712,-9.70780528753865,
-9.65995952470061,-9.64603852627451,-9.63792983587098,-9.62985702579027,
-9.61610426939685,-9.54192921750345,-9.48758843057746,-9.46743861757221,
-9.45375197493255,-9.44138383733526,-9.42093171973615,-9.37444697003052),
 .UNSPECIFIED.);
#1401=B_SPLINE_CURVE_WITH_KNOTS('',3,(#9484,#9485,#9486,#9487,#9488,#9489,
#9490,#9491,#9492,#9493,#9494,#9495,#9496,#9497,#9498,#9499,#9500,#9501,
#9502,#9503,#9504,#9505,#9506,#9507,#9508,#9509,#9510,#9511,#9512,#9513,
#9514,#9515,#9516,#9517,#9518,#9519,#9520,#9521,#9522,#9523,#9524,#9525,
#9526,#9527,#9528,#9529,#9530,#9531,#9532,#9533,#9534,#9535,#9536,#9537,
#9538,#9539,#9540,#9541,#9542,#9543,#9544,#9545,#9546,#9547,#9548,#9549,
#9550,#9551,#9552,#9553,#9554,#9555,#9556,#9557,#9558,#9559,#9560,#9561,
#9562,#9563,#9564,#9565,#9566,#9567,#9568,#9569,#9570,#9571,#9572,#9573,
#9574,#9575,#9576,#9577,#9578,#9579,#9580,#9581,#9582,#9583,#9584,#9585,
#9586,#9587,#9588,#9589,#9590,#9591,#9592,#9593,#9594,#9595,#9596,#9597,
#9598,#9599,#9600,#9601,#9602,#9603,#9604,#9605,#9606,#9607,#9608,#9609,
#9610,#9611,#9612,#9613,#9614,#9615,#9616,#9617,#9618,#9619,#9620,#9621,
#9622,#9623,#9624,#9625,#9626,#9627,#9628,#9629,#9630,#9631,#9632,#9633,
#9634,#9635,#9636,#9637,#9638,#9639,#9640,#9641,#9642,#9643,#9644,#9645,
#9646,#9647,#9648,#9649,#9650,#9651,#9652,#9653,#9654,#9655),
 .UNSPECIFIED.,.F.,.F.,(4,2,2,2,2,2,2,2,2,2,2,2,2,2,2,2,2,2,2,2,2,2,2,2,
2,2,2,2,2,2,2,2,2,2,2,2,2,2,2,2,2,2,2,2,2,2,2,2,2,2,2,2,2,2,2,2,2,2,2,2,
2,2,2,2,2,2,2,2,2,2,2,2,2,2,2,2,2,2,2,2,2,2,2,2,2,4),(-2.63816549894618,
-2.62822464334572,-2.61658219791459,-2.60900017022781,-2.60036573047471,
-2.58362511651739,-2.56017465258522,-2.46956214919072,-2.44456443123561,
-2.43004529991365,-2.41670594128353,-2.39849216605184,-2.3418328786306,
-2.26461197727369,-2.25136149568447,-2.24341146337504,-2.23525097355374,
-2.22095508195867,-2.20219194203138,-2.15080563245531,-2.09437897628173,
-2.07381523531863,-2.06009979804973,-2.04624769011226,-2.02491345165107,
-1.99898954580249,-1.93416028527984,-1.89446338860352,-1.88296602777026,
-1.87540645377818,-1.86671073380068,-1.84963730658322,-1.82550784494192,
-1.77966425287867,-1.72739480904774,-1.70698577409659,-1.69466374500704,
-1.68104782246321,-1.66105548792797,-1.60758673920447,-1.53164143219895,
-1.51817873402861,-1.5101867868185,-1.50207668553401,-1.48802753064419,
-1.43876669091307,-1.35943609955817,-1.33957528102245,-1.3261168029736,
-1.31214570165233,-1.29014682869026,-1.26307812357526,-1.19074732853763,
-1.15965160743421,-1.14878298140033,-1.14123255301325,-1.13217663974462,
-1.11308486336267,-1.08460847547084,-0.991339465378589,-0.972104214822802,
-0.958743359160055,-0.944602771071675,-0.921693086199137,-0.864661332780008,
-0.797171307040493,-0.784244819127981,-0.776357916275508,-0.768121397819388,
-0.753429496506319,-0.733937027354846,-0.678193138830802,-0.622238280397907,
-0.604040641736677,-0.590709636511149,-0.576197034069192,-0.551206792878598,
-0.518680002167478,-0.470510111833088,-0.42789133709684,-0.416286394664346,
-0.408715000213329,-0.4000793088898,-0.383307782692103,-0.35979250168467,
-0.294449080646368),.UNSPECIFIED.);
#1402=B_SPLINE_CURVE_WITH_KNOTS('',3,(#9658,#9659,#9660,#9661,#9662,#9663,
#9664,#9665,#9666,#9667,#9668,#9669,#9670,#9671,#9672,#9673,#9674,#9675,
#9676,#9677,#9678,#9679,#9680,#9681,#9682,#9683),.UNSPECIFIED.,.F.,.F.,
(4,2,2,2,2,2,2,2,2,2,2,2,4),(-0.294449080646368,-0.268387930386075,-0.243820374475458,
-0.22938269985925,-0.216021618487623,-0.19762188835446,-0.136808234456886,
-0.063856534004244,-0.0508349045132531,-0.0429260567403737,-0.0359882159395519,
-0.0276063209548247,-0.000158070576422473),.UNSPECIFIED.);
#1403=B_SPLINE_CURVE_WITH_KNOTS('',3,(#9685,#9686,#9687,#9688,#9689,#9690,
#9691,#9692,#9693,#9694,#9695,#9696,#9697,#9698,#9699,#9700,#9701,#9702,
#9703,#9704,#9705,#9706,#9707,#9708,#9709,#9710,#9711,#9712,#9713,#9714,
#9715,#9716,#9717,#9718,#9719,#9720,#9721,#9722,#9723,#9724,#9725,#9726,
#9727,#9728,#9729,#9730,#9731,#9732,#9733,#9734,#9735,#9736,#9737,#9738,
#9739,#9740,#9741,#9742,#9743,#9744,#9745,#9746,#9747,#9748,#9749,#9750,
#9751,#9752,#9753,#9754,#9755,#9756,#9757,#9758,#9759,#9760,#9761,#9762,
#9763,#9764,#9765,#9766,#9767,#9768,#9769,#9770,#9771,#9772,#9773,#9774,
#9775,#9776,#9777,#9778,#9779,#9780,#9781,#9782,#9783,#9784,#9785,#9786,
#9787,#9788,#9789,#9790,#9791,#9792,#9793,#9794,#9795,#9796,#9797,#9798,
#9799,#9800,#9801,#9802,#9803,#9804,#9805,#9806,#9807,#9808,#9809,#9810,
#9811,#9812,#9813,#9814,#9815,#9816,#9817,#9818,#9819,#9820,#9821,#9822,
#9823,#9824,#9825,#9826,#9827,#9828,#9829,#9830,#9831,#9832,#9833,#9834,
#9835,#9836,#9837,#9838,#9839,#9840,#9841,#9842,#9843,#9844,#9845,#9846,
#9847,#9848,#9849,#9850,#9851,#9852,#9853,#9854,#9855,#9856,#9857,#9858,
#9859,#9860,#9861,#9862,#9863,#9864,#9865,#9866,#9867,#9868,#9869,#9870,
#9871),.UNSPECIFIED.,.F.,.F.,(4,3,3,3,3,3,3,3,3,3,3,3,3,3,3,3,3,3,3,3,3,
3,3,3,3,3,3,3,3,3,3,3,3,3,3,3,3,3,3,3,3,3,3,3,3,3,3,3,3,3,3,3,3,3,3,3,3,
3,3,3,3,3,4),(47.12389017617,47.212634310815,47.3012804954036,47.3898536706167,
47.4783881657889,47.5669071783758,47.6554338879542,47.7440444285322,47.8326984185048,
47.9214901286793,47.9900165621361,47.9900533884742,48.0705655363816,48.079878475582,
48.1696262134622,48.2592844383872,48.3488804771275,48.4384437308739,48.5279963661167,
48.6175605357571,48.707215576596,48.7969155021056,48.8867636103351,48.9684752652717,
48.9731232496585,48.9731599923317,49.0537238943936,49.0631813344679,49.1531246430108,
49.2429775986181,49.3327663197129,49.4225209467818,49.5122634308969,49.6020157083635,
49.6918549669428,49.7817372622351,49.8717626820065,49.956229937181,49.9562646843143,
50.0372658835791,50.0464205997571,50.1364989391249,50.2264891614412,50.3164179156243,
50.4063141963529,50.4961997669363,50.5860963769902,50.6760809951302,50.766109414171,
50.8562806870504,50.9393366247034,50.9393761753254,51.0185464949487,51.0273822113533,
51.1153142003882,51.2043285952813,51.2921153635596,51.379874703757,51.4676302816496,
51.5575800511205,51.6454454055357,51.7364373825343,51.8184455727287),
 .UNSPECIFIED.);
#1404=B_SPLINE_CURVE_WITH_KNOTS('',3,(#9875,#9876,#9877,#9878,#9879,#9880,
#9881,#9882,#9883,#9884,#9885,#9886,#9887,#9888,#9889,#9890,#9891,#9892,
#9893,#9894,#9895,#9896,#9897,#9898,#9899,#9900,#9901,#9902,#9903,#9904,
#9905,#9906,#9907,#9908,#9909,#9910,#9911,#9912,#9913,#9914,#9915,#9916,
#9917,#9918,#9919,#9920,#9921,#9922,#9923,#9924,#9925,#9926,#9927,#9928,
#9929,#9930,#9931,#9932,#9933,#9934,#9935,#9936,#9937,#9938,#9939,#9940,
#9941,#9942,#9943,#9944,#9945,#9946,#9947,#9948,#9949,#9950,#9951,#9952,
#9953,#9954,#9955,#9956,#9957,#9958,#9959,#9960,#9961,#9962,#9963,#9964,
#9965,#9966,#9967,#9968,#9969,#9970,#9971,#9972,#9973,#9974,#9975,#9976,
#9977,#9978,#9979,#9980,#9981,#9982,#9983,#9984,#9985,#9986,#9987,#9988,
#9989,#9990,#9991,#9992,#9993,#9994,#9995,#9996,#9997,#9998,#9999,#10000,
#10001,#10002,#10003,#10004,#10005,#10006,#10007,#10008,#10009,#10010,#10011,
#10012,#10013,#10014,#10015,#10016),.UNSPECIFIED.,.F.,.F.,(4,3,3,3,3,3,
3,3,3,3,3,3,3,3,3,3,3,3,3,3,3,3,3,3,3,3,3,3,3,3,3,3,3,3,3,3,3,3,3,3,3,3,
3,3,3,3,3,4),(47.1238898038469,47.2174754673338,47.3111680100548,47.4050579725487,
47.4990543518043,47.5843560963284,47.5932435711771,47.6391053165797,47.639145354705,
47.7202593538192,47.7282111079036,47.8171624892304,47.9060250358962,47.9955534116876,
48.0843273344302,48.1730941115943,48.2618766705276,48.3519705134526,48.4409057141138,
48.5315788781706,48.6115449556694,48.6222159452476,48.6222520422274,48.704134821478,
48.7134731108222,48.8045685913688,48.8955611216527,48.9864649966019,49.0773190413066,
49.1681435703031,49.2589588697564,49.3498243415436,49.4407136971665,49.5317037438762,
49.6053370119153,49.6053587297499,49.69634898757,49.7872668551369,49.8781345589675,
49.9689726175072,50.0598150491269,50.0969120735111,50.0969186132547,50.1985524169299,
50.3004232260078,50.4023379611143,50.5041923151378,50.5884654172723),
 .UNSPECIFIED.);
#1405=B_SPLINE_CURVE_WITH_KNOTS('',3,(#10017,#10018,#10019,#10020,#10021,
#10022,#10023,#10024,#10025,#10026,#10027,#10028,#10029,#10030,#10031,#10032,
#10033,#10034,#10035,#10036,#10037,#10038,#10039,#10040),.UNSPECIFIED.,
 .F.,.F.,(4,2,2,2,2,2,2,2,2,2,2,4),(-12.0120719037212,-12.0010573616161,
-11.9867119540422,-11.904250798684,-11.8715813211036,-11.850683020791,-11.8411538380416,
-11.8334529515479,-11.822560800604,-11.7920652487739,-11.7196340744173,
-11.7176550926435),.UNSPECIFIED.);
#1406=B_SPLINE_CURVE_WITH_KNOTS('',3,(#10044,#10045,#10046,#10047,#10048,
#10049,#10050,#10051,#10052,#10053,#10054,#10055,#10056,#10057,#10058,#10059,
#10060,#10061,#10062,#10063,#10064,#10065,#10066,#10067,#10068,#10069,#10070,
#10071,#10072,#10073,#10074,#10075,#10076,#10077,#10078,#10079,#10080,#10081,
#10082,#10083,#10084,#10085,#10086,#10087,#10088,#10089,#10090,#10091,#10092,
#10093,#10094,#10095,#10096,#10097,#10098,#10099,#10100,#10101,#10102,#10103,
#10104,#10105,#10106,#10107,#10108,#10109,#10110,#10111,#10112,#10113,#10114,
#10115,#10116,#10117,#10118,#10119,#10120,#10121,#10122,#10123,#10124,#10125,
#10126,#10127,#10128,#10129,#10130,#10131,#10132,#10133,#10134,#10135,#10136,
#10137,#10138,#10139,#10140,#10141,#10142,#10143,#10144,#10145,#10146,#10147,
#10148,#10149,#10150,#10151,#10152,#10153,#10154,#10155,#10156,#10157,#10158,
#10159,#10160,#10161),.UNSPECIFIED.,.F.,.F.,(4,3,3,3,3,3,3,3,3,3,3,3,3,
3,3,3,3,3,3,3,3,3,3,3,3,3,3,3,3,3,3,3,3,3,3,3,3,3,3,4),(-4.09289414414334,
-4.00843569444614,-3.95955978524779,-3.9324557935787,-3.93242675008978,
-3.85384525365456,-3.84608852572687,-3.75985370563718,-3.67370105299863,
-3.60241376041841,-3.58315342919472,-3.51290061676997,-3.49709435009809,
-3.41104793156076,-3.33194995829287,-3.32499509288074,-3.25893240679908,
-3.2389167535879,-3.15274805448362,-3.06652690774132,-2.98763571046433,
-2.98018641192965,-2.94935374406167,-2.94932006256734,-2.87252712645479,
-2.86503523867605,-2.7808550431761,-2.69675631414078,-2.63498082505163,
-2.61271378948831,-2.54090460291134,-2.52869995275755,-2.41037007810133,
-2.36067529736391,-2.29985971128565,-2.27657679923735,-2.20652088686618,
-2.1924341240595,-2.10817127163918,-2.0620931210805),.UNSPECIFIED.);
#1407=B_SPLINE_CURVE_WITH_KNOTS('',3,(#10165,#10166,#10167,#10168,#10169,
#10170,#10171,#10172,#10173,#10174,#10175,#10176,#10177,#10178,#10179,#10180,
#10181,#10182,#10183,#10184,#10185,#10186,#10187,#10188,#10189,#10190),
 .UNSPECIFIED.,.F.,.F.,(4,2,2,2,2,2,2,2,2,2,2,2,4),(0.,0.0194959022105328,
0.0584392371124239,0.114822265828151,0.164960797084267,0.246283622826695,
0.323295648367368,0.397518421465989,0.41363588735925,0.425864804055925,
0.436832758233511,0.455647012980926,0.492598869825882),.UNSPECIFIED.);
#1408=B_SPLINE_CURVE_WITH_KNOTS('',3,(#10192,#10193,#10194,#10195,#10196,
#10197,#10198,#10199,#10200,#10201,#10202,#10203,#10204,#10205,#10206,#10207,
#10208,#10209,#10210,#10211,#10212,#10213,#10214,#10215,#10216,#10217,#10218,
#10219,#10220,#10221,#10222,#10223,#10224,#10225,#10226,#10227,#10228,#10229,
#10230,#10231,#10232,#10233,#10234,#10235,#10236,#10237,#10238,#10239,#10240,
#10241,#10242,#10243,#10244,#10245,#10246,#10247,#10248,#10249,#10250,#10251,
#10252,#10253,#10254,#10255,#10256,#10257,#10258,#10259,#10260,#10261,#10262,
#10263,#10264,#10265,#10266,#10267,#10268,#10269,#10270,#10271,#10272,#10273,
#10274,#10275,#10276,#10277,#10278,#10279,#10280,#10281,#10282,#10283,#10284,
#10285,#10286,#10287,#10288,#10289,#10290,#10291,#10292,#10293,#10294,#10295,
#10296,#10297,#10298,#10299,#10300,#10301,#10302,#10303,#10304,#10305,#10306,
#10307,#10308,#10309,#10310,#10311,#10312,#10313,#10314,#10315,#10316,#10317,
#10318,#10319,#10320,#10321,#10322,#10323,#10324,#10325,#10326,#10327,#10328,
#10329,#10330,#10331,#10332,#10333,#10334,#10335,#10336,#10337,#10338,#10339,
#10340,#10341,#10342,#10343,#10344,#10345,#10346,#10347,#10348,#10349,#10350,
#10351,#10352,#10353,#10354,#10355,#10356,#10357,#10358,#10359,#10360,#10361,
#10362,#10363,#10364,#10365,#10366,#10367,#10368,#10369,#10370,#10371,#10372,
#10373,#10374,#10375,#10376,#10377,#10378,#10379,#10380,#10381,#10382,#10383,
#10384,#10385,#10386,#10387,#10388,#10389,#10390,#10391,#10392,#10393,#10394,
#10395,#10396,#10397,#10398,#10399,#10400,#10401,#10402,#10403,#10404,#10405,
#10406,#10407,#10408,#10409,#10410,#10411,#10412,#10413,#10414,#10415,#10416,
#10417,#10418,#10419,#10420,#10421,#10422,#10423,#10424,#10425,#10426,#10427,
#10428,#10429,#10430,#10431,#10432,#10433,#10434,#10435,#10436,#10437,#10438,
#10439,#10440,#10441,#10442,#10443,#10444,#10445,#10446,#10447,#10448,#10449,
#10450,#10451,#10452,#10453,#10454,#10455,#10456,#10457,#10458,#10459,#10460,
#10461,#10462,#10463,#10464,#10465,#10466,#10467,#10468,#10469,#10470,#10471,
#10472,#10473,#10474,#10475,#10476,#10477,#10478,#10479,#10480,#10481,#10482,
#10483,#10484,#10485,#10486,#10487,#10488,#10489,#10490,#10491,#10492,#10493,
#10494,#10495,#10496,#10497,#10498,#10499,#10500,#10501,#10502,#10503,#10504,
#10505,#10506,#10507,#10508,#10509,#10510,#10511,#10512,#10513,#10514,#10515,
#10516,#10517,#10518,#10519),.UNSPECIFIED.,.F.,.F.,(4,3,3,3,3,3,3,3,3,3,
3,3,3,3,3,3,3,3,3,3,3,3,3,3,3,3,3,3,3,3,3,3,3,3,3,3,3,3,3,3,3,3,3,3,3,3,
3,3,3,3,3,3,3,3,3,3,3,3,3,3,3,3,3,3,3,3,3,3,3,3,3,3,3,3,3,3,3,3,3,3,3,3,
3,3,3,3,3,3,3,3,3,3,3,3,3,3,3,3,3,3,3,3,3,3,3,3,3,3,3,4),(1.10990013830804,
1.1961286058751,1.25196222134668,1.28229535123711,1.39349992939904,1.51275424662582,
1.54068094018495,1.62683182926768,1.68212521043177,1.71308212960078,1.79938293490773,
1.88094723079734,1.88582928212476,1.96618291867898,1.96621337504489,2.04375333511063,
2.05153108173538,2.13673294970428,2.22184143229054,2.28102853375086,2.30687888662215,
2.3918736400768,2.50546630057955,2.56182185653531,2.61816392998536,2.64681554817045,
2.73189761684025,2.81702879702236,2.89630232944247,2.90228614623796,2.94928686442096,
2.94932006256734,3.0274018791421,3.03565805991247,3.12189270046458,3.2080452208331,
3.29077173342695,3.29859291199018,3.36018397709367,3.38465197828492,3.47069842778444,
3.55675134115351,3.61893904656727,3.64282979885581,3.72899868109771,3.81522004855201,
3.89464542126761,3.90156081956687,3.93239753466603,3.93242675008978,4.01081868217623,
4.01862531663163,4.10472062379942,4.19073408969261,4.25235268719438,4.27668705919604,
4.36260993804403,4.4766480016078,4.53443659800429,4.60851037805321,4.62037886781216,
4.70641359734286,4.79250118256877,4.87185479163746,4.87871238538384,4.91550255891886,
4.91553343761223,4.99363650524933,5.00156375899611,5.08748769640701,5.17332689219006,
5.23826602356694,5.25910291179368,5.33123427756829,5.3448454961129,5.45886531939574,
5.51630566495775,5.59065164197529,5.60206211830088,5.68790953458488,5.77380869437548,
5.85324777795459,5.85983139642645,5.8986091808827,5.89864012513467,5.97682534817979,
5.98479447136155,6.07084407042382,6.15681040430506,6.22339442557936,6.24271488026911,
6.31278432489712,6.32858741328564,6.442683640289,6.50031001604005,6.58619867867155,
6.67217852283113,6.75821041676436,6.83768892414904,6.84436517205843,6.88171630337422,
6.88174681265712,6.96162680560509,6.97139414465698,7.06090018627908,7.15023013756892,
7.21226088232711,7.23945576258717,7.32855559990409,7.39308541414175),
 .UNSPECIFIED.);
#1409=B_SPLINE_CURVE_WITH_KNOTS('',3,(#10521,#10522,#10523,#10524,#10525,
#10526,#10527,#10528,#10529,#10530,#10531,#10532,#10533,#10534,#10535,#10536,
#10537,#10538,#10539,#10540,#10541,#10542,#10543,#10544,#10545,#10546,#10547,
#10548,#10549,#10550,#10551,#10552,#10553,#10554,#10555,#10556,#10557,#10558,
#10559,#10560,#10561,#10562,#10563,#10564,#10565,#10566,#10567,#10568,#10569,
#10570,#10571,#10572,#10573,#10574,#10575,#10576,#10577,#10578,#10579,#10580,
#10581,#10582,#10583,#10584,#10585,#10586,#10587,#10588,#10589,#10590,#10591,
#10592,#10593,#10594,#10595,#10596,#10597,#10598,#10599,#10600,#10601,#10602,
#10603,#10604,#10605,#10606,#10607,#10608,#10609,#10610,#10611,#10612,#10613,
#10614,#10615,#10616,#10617,#10618,#10619,#10620,#10621,#10622,#10623,#10624,
#10625,#10626,#10627,#10628,#10629,#10630,#10631,#10632,#10633,#10634,#10635,
#10636,#10637,#10638,#10639,#10640,#10641,#10642,#10643,#10644,#10645,#10646,
#10647,#10648,#10649,#10650,#10651,#10652,#10653,#10654,#10655,#10656,#10657,
#10658,#10659,#10660,#10661,#10662,#10663,#10664,#10665,#10666,#10667,#10668,
#10669,#10670,#10671,#10672,#10673,#10674,#10675,#10676,#10677,#10678,#10679,
#10680,#10681,#10682,#10683,#10684,#10685,#10686,#10687,#10688,#10689,#10690,
#10691,#10692,#10693,#10694,#10695,#10696,#10697,#10698,#10699,#10700,#10701,
#10702,#10703,#10704,#10705,#10706,#10707,#10708,#10709,#10710,#10711,#10712,
#10713,#10714,#10715,#10716,#10717,#10718,#10719,#10720,#10721,#10722,#10723,
#10724,#10725,#10726,#10727,#10728,#10729,#10730,#10731,#10732,#10733,#10734,
#10735,#10736,#10737,#10738,#10739,#10740,#10741,#10742,#10743,#10744,#10745,
#10746,#10747,#10748,#10749,#10750,#10751,#10752,#10753,#10754,#10755,#10756,
#10757,#10758,#10759,#10760,#10761,#10762,#10763,#10764,#10765,#10766,#10767,
#10768,#10769,#10770,#10771,#10772,#10773,#10774,#10775,#10776,#10777,#10778,
#10779,#10780,#10781,#10782,#10783,#10784,#10785,#10786,#10787,#10788,#10789,
#10790,#10791,#10792,#10793,#10794,#10795,#10796,#10797,#10798,#10799,#10800,
#10801,#10802,#10803,#10804,#10805,#10806,#10807,#10808,#10809,#10810,#10811,
#10812,#10813,#10814,#10815,#10816,#10817,#10818,#10819,#10820,#10821,#10822,
#10823,#10824,#10825,#10826,#10827,#10828,#10829,#10830,#10831,#10832,#10833,
#10834,#10835,#10836,#10837,#10838,#10839,#10840,#10841,#10842,#10843,#10844,
#10845,#10846,#10847,#10848,#10849,#10850,#10851,#10852,#10853,#10854,#10855,
#10856,#10857,#10858,#10859,#10860),.UNSPECIFIED.,.F.,.F.,(4,3,3,3,3,3,
3,3,3,3,3,3,3,3,3,3,3,3,3,3,3,3,3,3,3,3,3,3,3,3,3,3,3,3,3,3,3,3,3,3,3,3,
3,3,3,3,3,3,3,3,3,3,3,3,3,3,3,3,3,3,3,3,3,3,3,3,3,3,3,3,3,3,3,3,3,3,3,3,
3,3,3,3,3,3,3,3,3,3,3,3,3,3,3,3,3,3,3,3,3,3,3,3,3,3,3,3,3,3,3,3,3,3,3,4),
(7.3930854143344,7.46038550079444,7.48366125998094,7.5789593200306,7.66991850903281,
7.75593207956134,7.7610068757006,7.84118324163327,7.85228887176144,7.86482277028161,
7.86485350017956,7.94303010247594,7.95096567356472,8.0369726336412,8.12289591723387,
8.18821517045417,8.20875698581783,8.28063321315669,8.29458574146171,8.40864764903128,
8.4662201866803,8.54699140015504,8.55206456429625,8.63800018005379,8.7239878182005,
8.80343769099625,8.81009865991351,8.84792947320008,8.84796018770201,8.92614885835429,
8.93408705165396,9.02010890939336,9.10604727849447,9.17147498951346,9.19192360144347,
9.26368552584356,9.27776780665372,9.39183773100395,9.44943348524598,9.53529361359441,
9.62124502178279,9.70724849768268,9.78670119867335,9.79337510940081,9.83103620527342,
9.83106687522445,9.90925690090911,9.91718938261793,10.0032068469648,10.0891407914262,
10.1543660154415,10.1750126640201,10.2471131548751,10.2608523972262,10.3749177581416,
10.4325091004347,10.5137737355322,10.5183647351718,10.604311670713,10.6903106799034,
10.7697586512753,10.7764328728798,10.8141428649052,10.8141735627469,10.892359956357,
10.9002949112415,10.9863111869436,11.0722439146069,11.1375528108811,11.1581145438086,
11.2300578046464,11.2439529984951,11.3580189170255,11.4156070814413,11.4970857186119,
11.5014613770805,11.5874069521317,11.6734045867373,11.752854448271,11.7595253953439,
11.7972495568869,11.7972802502693,11.8754682914925,11.8834032732732,11.9694212484686,
12.0553556984052,12.120667522524,12.1412280704876,12.2131749688845,12.2270682923214,
12.3411350037324,12.3987259514211,12.4845820522888,12.5705294391601,12.6565288918185,
12.7359788613518,12.7426515122888,12.7803562486784,12.7803869377918,12.8579454211869,
12.8655355434748,12.9505796553732,13.0355418164815,13.1021756909872,13.1204452668709,
13.1890182990663,13.20531838703,13.3238563297698,13.3750546099121,13.4395618577246,
13.4600018316116,13.5449901073353,13.6300921524228,13.6762707211195),
 .UNSPECIFIED.);
#1410=B_SPLINE_CURVE_WITH_KNOTS('',3,(#10862,#10863,#10864,#10865,#10866,
#10867,#10868,#10869,#10870,#10871,#10872,#10873,#10874,#10875,#10876,#10877,
#10878,#10879,#10880,#10881,#10882,#10883,#10884,#10885,#10886,#10887,#10888,
#10889,#10890,#10891,#10892,#10893,#10894,#10895,#10896,#10897,#10898,#10899,
#10900,#10901,#10902,#10903,#10904,#10905,#10906,#10907,#10908,#10909,#10910,
#10911,#10912,#10913,#10914,#10915,#10916,#10917,#10918,#10919,#10920,#10921,
#10922,#10923,#10924,#10925,#10926,#10927,#10928,#10929,#10930,#10931,#10932,
#10933,#10934,#10935,#10936,#10937,#10938,#10939,#10940,#10941,#10942,#10943,
#10944,#10945,#10946,#10947,#10948,#10949,#10950,#10951,#10952,#10953,#10954,
#10955,#10956,#10957,#10958,#10959,#10960,#10961,#10962,#10963,#10964,#10965,
#10966,#10967,#10968,#10969,#10970,#10971,#10972,#10973,#10974,#10975,#10976,
#10977,#10978,#10979,#10980,#10981,#10982,#10983,#10984,#10985,#10986,#10987,
#10988,#10989,#10990,#10991,#10992,#10993,#10994,#10995,#10996,#10997,#10998,
#10999,#11000,#11001,#11002,#11003,#11004,#11005,#11006,#11007,#11008,#11009,
#11010,#11011,#11012,#11013,#11014,#11015,#11016,#11017,#11018,#11019,#11020,
#11021,#11022,#11023,#11024,#11025,#11026,#11027,#11028,#11029,#11030,#11031,
#11032,#11033,#11034,#11035,#11036,#11037,#11038,#11039,#11040,#11041,#11042,
#11043,#11044,#11045,#11046,#11047,#11048,#11049,#11050,#11051,#11052,#11053,
#11054,#11055,#11056,#11057,#11058,#11059,#11060,#11061,#11062,#11063,#11064,
#11065,#11066,#11067,#11068,#11069,#11070,#11071,#11072,#11073,#11074,#11075,
#11076,#11077,#11078,#11079,#11080,#11081,#11082,#11083,#11084,#11085,#11086,
#11087,#11088,#11089,#11090,#11091,#11092,#11093,#11094,#11095,#11096,#11097,
#11098,#11099,#11100,#11101,#11102,#11103,#11104,#11105,#11106,#11107,#11108,
#11109,#11110,#11111,#11112,#11113,#11114,#11115,#11116,#11117,#11118,#11119,
#11120,#11121,#11122,#11123,#11124,#11125,#11126,#11127,#11128,#11129,#11130,
#11131,#11132,#11133,#11134,#11135,#11136,#11137,#11138,#11139,#11140,#11141,
#11142,#11143,#11144,#11145,#11146,#11147,#11148,#11149,#11150,#11151,#11152,
#11153,#11154,#11155,#11156,#11157,#11158,#11159,#11160,#11161,#11162,#11163,
#11164,#11165,#11166,#11167,#11168,#11169,#11170,#11171,#11172,#11173,#11174,
#11175,#11176,#11177,#11178,#11179,#11180,#11181,#11182,#11183,#11184,#11185,
#11186,#11187,#11188,#11189,#11190,#11191,#11192,#11193,#11194,#11195,#11196,
#11197,#11198,#11199,#11200,#11201,#11202,#11203,#11204,#11205,#11206,#11207),
 .UNSPECIFIED.,.F.,.F.,(4,3,3,3,3,3,3,3,3,3,3,3,3,3,3,3,3,3,3,3,3,3,3,3,
3,3,3,3,3,3,3,3,3,3,3,3,3,3,3,3,3,3,3,3,3,3,3,3,3,3,3,3,3,3,3,3,3,3,3,3,
3,3,3,3,3,3,3,3,3,3,3,3,3,3,3,3,3,3,3,3,3,3,3,3,3,3,3,3,3,3,3,3,3,3,3,3,
3,3,3,3,3,3,3,3,3,3,3,3,3,3,3,3,3,3,3,4),(13.6762707213213,13.7634629327955,
13.7634936253142,13.8416812604774,13.8496159580763,13.9356332340953,14.0215669768221,
14.0868681734509,14.1074386345513,14.179400911131,14.1932781340374,14.3073443975024,
14.3649343349407,14.4464660882827,14.4507897015138,14.536736353218,14.6227350692125,
14.7021847788391,14.7088569571122,14.7465696211511,14.7466003128367,14.8247881614203,
14.8327228290312,14.9187402913841,15.0046742231037,15.069974604919,15.0905460722461,
15.1625107839159,15.1763857660457,15.2904521017495,15.3480423606136,15.4295863405157,
15.4338979261233,15.5198447777085,15.6058436943958,15.6852933898944,15.6919657824959,
15.7296763090431,15.7297070003591,15.8078948248047,15.8158294310186,15.9018468068606,
15.9877806512044,16.0530788150397,16.0736524122154,16.1456206491793,16.1594920170861,
16.2735582856674,16.3311484324836,16.4126770413684,16.4170039079444,16.5029506695495,
16.5889494961742,16.6683991387936,16.675071494867,16.7127829961687,16.7128136878816,
16.7910014741668,16.7989361209402,16.8849534990149,16.9708873454232,17.0361869085138,
17.0567591083282,17.1287248468944,17.1425987148302,17.2566650025967,17.3142551329948,
17.3957891316664,17.4001106095863,17.4860573720587,17.5720561994008,17.6515058741772,
17.6581781985741,17.6958896838184,17.695920375404,17.7741081883125,17.7820428278235,
17.8680602255835,17.953994091976,18.0192934276472,18.0398658751388,18.1118321246165,
18.1257055022317,18.2397717958319,18.2973619621599,18.3788967293656,18.3832174598805,
18.4691642436063,18.555163092302,18.6346127623353,18.6412851127977,18.6789963713672,
18.6790270629265,18.7572148705848,18.7651495041418,18.8511668905623,18.9371007454944,
19.002399871327,19.0229725170903,19.0949390859491,19.1088121325003,19.2228784179173,
19.2804685688698,19.3620017052309,19.3663240547399,19.4522708266136,19.5382696634402,
19.6177193281047,19.6243916721438,19.6621030588424,19.6621337504489,19.7455613159664,
19.7659686645438,19.8527584971793,19.8686725452676,19.9594558713002),
 .UNSPECIFIED.);
#1411=B_SPLINE_CURVE_WITH_KNOTS('',3,(#11209,#11210,#11211,#11212,#11213,
#11214,#11215,#11216,#11217,#11218,#11219,#11220,#11221,#11222,#11223,#11224,
#11225,#11226,#11227,#11228,#11229,#11230,#11231,#11232,#11233,#11234,#11235,
#11236,#11237,#11238,#11239,#11240,#11241,#11242,#11243,#11244,#11245,#11246,
#11247,#11248,#11249,#11250,#11251,#11252,#11253,#11254,#11255,#11256,#11257,
#11258,#11259,#11260,#11261,#11262,#11263,#11264,#11265,#11266,#11267,#11268,
#11269,#11270,#11271,#11272,#11273,#11274,#11275,#11276,#11277,#11278,#11279,
#11280,#11281,#11282,#11283,#11284,#11285,#11286,#11287,#11288,#11289,#11290,
#11291,#11292,#11293,#11294,#11295,#11296,#11297,#11298,#11299,#11300,#11301,
#11302,#11303,#11304,#11305,#11306,#11307,#11308,#11309,#11310,#11311,#11312,
#11313,#11314,#11315,#11316,#11317,#11318,#11319,#11320,#11321,#11322,#11323,
#11324,#11325,#11326,#11327,#11328,#11329,#11330,#11331,#11332,#11333,#11334,
#11335,#11336,#11337,#11338,#11339,#11340,#11341,#11342,#11343,#11344,#11345,
#11346,#11347,#11348,#11349,#11350,#11351,#11352,#11353,#11354,#11355,#11356,
#11357,#11358,#11359,#11360,#11361,#11362,#11363,#11364,#11365,#11366,#11367,
#11368,#11369,#11370,#11371,#11372,#11373,#11374,#11375,#11376,#11377,#11378,
#11379,#11380,#11381,#11382,#11383,#11384,#11385,#11386,#11387,#11388,#11389,
#11390,#11391,#11392,#11393,#11394,#11395,#11396,#11397,#11398,#11399,#11400,
#11401,#11402,#11403,#11404,#11405,#11406,#11407,#11408,#11409,#11410,#11411,
#11412,#11413,#11414,#11415,#11416,#11417,#11418,#11419,#11420,#11421,#11422,
#11423,#11424,#11425,#11426,#11427,#11428,#11429,#11430,#11431,#11432,#11433,
#11434,#11435,#11436,#11437),.UNSPECIFIED.,.F.,.F.,(4,3,3,3,3,3,3,3,3,3,
3,3,3,3,3,3,3,3,3,3,3,3,3,3,3,3,3,3,3,3,3,3,3,3,3,3,3,3,3,3,3,3,3,3,3,3,
3,3,3,3,3,3,3,3,3,3,3,3,3,3,3,3,3,3,3,3,3,3,3,3,3,3,3,3,3,3,4),(19.9594560285009,
20.0451790796847,20.1305458428908,20.2159059621089,20.3012792146047,20.3872695204463,
20.4727722942822,20.5590063661267,20.6452404379713,20.7313628836198,20.8173802745045,
20.903314133926,20.9891859100309,21.0750255299629,21.1608511074417,21.246681975391,
21.3325374657882,21.4184842421596,21.5044830834734,21.5906050966088,21.6283471254938,
21.7144695676753,21.8004869550807,21.8864208110143,21.9722925836273,22.0581322000745,
22.1439577740739,22.2297886385524,22.3156441254915,22.4015908984418,22.4875897363515,
22.5737117461376,22.6114538130162,22.6975762542529,22.783593640691,22.8695274956365,
22.9553992672416,23.0412388826549,23.1270644556048,23.2128953190199,23.2987508048819,
23.3846975767421,23.4706964135524,23.5568184222344,23.5945605005387,23.6806829535161,
23.7667003517293,23.8526342184696,23.9385060018757,24.0243456290561,24.110171213748,
24.196002088868,24.2818575863844,24.3678043697609,24.453803218024,24.5399252379628,
24.5776671880611,24.6637896198065,24.7498069968154,24.8357408424047,24.9216126047368,
25.007452211033,25.0932777749654,25.1791086294714,25.2649641065426,25.350910869837,
25.436909698198,25.5230316986823,25.5607738755836,25.6464658524267,25.7320583612643,
25.8175712968715,25.9030244902211,25.9884489916975,26.0738534974488,26.1592909000781,
26.2426413356805),.UNSPECIFIED.);
#1412=B_SPLINE_CURVE_WITH_KNOTS('',3,(#11439,#11440,#11441,#11442,#11443,
#11444,#11445,#11446,#11447,#11448,#11449,#11450,#11451,#11452,#11453,#11454,
#11455,#11456,#11457,#11458,#11459,#11460,#11461,#11462,#11463,#11464,#11465,
#11466,#11467,#11468,#11469,#11470,#11471,#11472,#11473,#11474,#11475,#11476,
#11477,#11478,#11479,#11480,#11481,#11482,#11483,#11484,#11485,#11486,#11487,
#11488,#11489,#11490,#11491,#11492,#11493,#11494,#11495,#11496,#11497,#11498,
#11499,#11500,#11501,#11502,#11503,#11504,#11505,#11506,#11507,#11508,#11509,
#11510,#11511,#11512,#11513,#11514,#11515,#11516,#11517,#11518,#11519,#11520,
#11521,#11522,#11523,#11524,#11525,#11526,#11527,#11528,#11529,#11530,#11531,
#11532,#11533,#11534,#11535,#11536,#11537,#11538,#11539,#11540,#11541,#11542,
#11543,#11544,#11545,#11546,#11547,#11548,#11549,#11550,#11551,#11552,#11553,
#11554,#11555,#11556,#11557,#11558,#11559,#11560,#11561,#11562,#11563,#11564,
#11565,#11566,#11567,#11568,#11569,#11570,#11571,#11572,#11573,#11574,#11575,
#11576,#11577,#11578,#11579,#11580,#11581,#11582,#11583,#11584,#11585,#11586,
#11587,#11588,#11589,#11590,#11591,#11592,#11593,#11594,#11595,#11596,#11597,
#11598,#11599,#11600,#11601,#11602,#11603,#11604,#11605,#11606,#11607,#11608,
#11609,#11610,#11611,#11612,#11613,#11614,#11615,#11616,#11617,#11618,#11619,
#11620,#11621,#11622,#11623,#11624,#11625,#11626,#11627,#11628,#11629,#11630,
#11631,#11632,#11633,#11634,#11635,#11636,#11637,#11638,#11639,#11640,#11641,
#11642,#11643,#11644,#11645,#11646,#11647,#11648,#11649,#11650,#11651,#11652,
#11653,#11654,#11655,#11656,#11657,#11658,#11659,#11660,#11661,#11662,#11663,
#11664,#11665,#11666,#11667,#11668,#11669,#11670,#11671,#11672,#11673,#11674,
#11675,#11676,#11677,#11678,#11679,#11680,#11681,#11682,#11683,#11684,#11685,
#11686,#11687,#11688,#11689,#11690,#11691,#11692,#11693,#11694,#11695,#11696,
#11697,#11698,#11699,#11700,#11701,#11702,#11703,#11704,#11705,#11706,#11707,
#11708,#11709,#11710,#11711,#11712,#11713,#11714,#11715,#11716,#11717,#11718,
#11719,#11720,#11721,#11722,#11723,#11724,#11725,#11726,#11727,#11728,#11729,
#11730,#11731,#11732,#11733,#11734,#11735,#11736,#11737,#11738,#11739,#11740,
#11741,#11742,#11743,#11744,#11745,#11746,#11747,#11748,#11749,#11750,#11751,
#11752,#11753,#11754,#11755,#11756,#11757,#11758,#11759,#11760,#11761,#11762,
#11763,#11764,#11765,#11766,#11767,#11768,#11769,#11770,#11771,#11772,#11773,
#11774,#11775,#11776,#11777,#11778,#11779,#11780,#11781),.UNSPECIFIED.,
 .F.,.F.,(4,3,3,3,3,3,3,3,3,3,3,3,3,3,3,3,3,3,3,3,3,3,3,3,3,3,3,3,3,3,3,
3,3,3,3,3,3,3,3,3,3,3,3,3,3,3,3,3,3,3,3,3,3,3,3,3,3,3,3,3,3,3,3,3,3,3,3,
3,3,3,3,3,3,3,3,3,3,3,3,3,3,3,3,3,3,3,3,3,3,3,3,3,3,3,3,3,3,3,3,3,3,3,3,
3,3,3,3,3,3,3,3,3,3,3,4),(26.242641499509,26.3324415864858,26.3446941768379,
26.4313149906762,26.4478838155214,26.5302507572133,26.5438498718212,26.543880563106,
26.622068448048,26.6300030833935,26.7160205490677,26.8019544833399,26.8672543793336,
26.8878263342683,26.9597921828112,26.9736660287096,27.0877323185049,27.1453226224228,
27.2268738403406,27.2311781864362,27.3171250354588,27.4031239489703,27.4825736061514,
27.4892460329838,27.5269565589012,27.5269872506285,27.6051750106045,27.6131095715702,
27.6991268379978,27.7850605733534,27.8503602927242,27.8709322259246,27.942897926408,
27.9567717235579,28.0708378791915,28.1284279269293,28.2099819216018,28.2142832978237,
28.3002299569284,28.3862286820944,28.4656782525,28.4723505817956,28.5100632455641,
28.5100939381509,28.5882815216702,28.5962163393846,28.6822336845469,28.7681674970097,
28.8334629716548,28.8540392249894,28.9260092202108,28.9398787952556,29.0539453790681,
29.111535138587,29.1929504221305,29.1973905766713,29.2833372997852,29.3693360872299,
29.4487860194801,29.4554580460383,29.4931699369254,29.4932006256733,29.5713891295633,
29.5793236759997,29.6653416733656,29.7512761403407,29.81658196337,29.8371485243456,
29.9091094146335,29.9229887504622,30.0370549240626,30.0946464038566,30.1805024947355,
30.2664498645006,30.3524492959591,30.4318987707329,30.4385718891503,30.4762766193398,
30.4763073131958,30.5544944690055,30.5624285594366,30.6484447521662,30.7343774160621,
30.7996775079718,30.8202480006432,30.8922116034977,30.9060864392999,31.0201517567277,
31.0777405435947,31.1635948766145,31.2495405156828,31.3355382296261,31.4149872318963,
31.4216591403216,31.4593833024249,31.4594140007182,31.5376003722513,31.5455366257588,
31.6315541855686,31.7174882033962,31.7827581688761,31.8033601273273,31.8753555708931,
31.8891998789751,32.0032688426819,32.0608565576179,32.1414714565194,32.1467121493448,
32.2326590112296,32.3186579291363,32.3981099080769,32.4047800046536,32.4424900212834,
32.4425206882407,32.5258266428601),.UNSPECIFIED.);
#1413=B_SPLINE_CURVE_WITH_KNOTS('',3,(#11783,#11784,#11785,#11786,#11787,
#11788,#11789,#11790,#11791,#11792,#11793,#11794,#11795,#11796,#11797,#11798,
#11799,#11800,#11801,#11802,#11803,#11804,#11805,#11806,#11807,#11808,#11809,
#11810,#11811,#11812,#11813,#11814,#11815,#11816,#11817,#11818,#11819,#11820,
#11821,#11822,#11823,#11824,#11825,#11826,#11827,#11828,#11829,#11830,#11831,
#11832,#11833,#11834,#11835,#11836,#11837,#11838,#11839,#11840,#11841,#11842,
#11843,#11844,#11845,#11846,#11847,#11848,#11849,#11850,#11851,#11852,#11853,
#11854,#11855,#11856,#11857,#11858,#11859,#11860,#11861,#11862,#11863,#11864,
#11865,#11866,#11867,#11868,#11869,#11870,#11871,#11872,#11873,#11874,#11875,
#11876,#11877,#11878,#11879,#11880,#11881,#11882,#11883,#11884,#11885,#11886,
#11887,#11888,#11889,#11890,#11891,#11892,#11893,#11894,#11895,#11896,#11897,
#11898,#11899,#11900,#11901,#11902,#11903,#11904,#11905,#11906,#11907,#11908,
#11909,#11910,#11911,#11912,#11913,#11914,#11915,#11916,#11917,#11918,#11919,
#11920,#11921,#11922,#11923,#11924,#11925,#11926,#11927,#11928,#11929,#11930,
#11931,#11932,#11933,#11934,#11935,#11936,#11937,#11938,#11939,#11940,#11941,
#11942,#11943,#11944,#11945,#11946,#11947,#11948,#11949,#11950,#11951,#11952,
#11953,#11954,#11955,#11956,#11957,#11958,#11959,#11960,#11961,#11962,#11963,
#11964,#11965,#11966,#11967,#11968,#11969,#11970,#11971,#11972,#11973,#11974,
#11975,#11976,#11977,#11978,#11979,#11980,#11981,#11982,#11983,#11984,#11985,
#11986,#11987,#11988,#11989,#11990,#11991,#11992,#11993,#11994,#11995,#11996,
#11997,#11998,#11999,#12000,#12001,#12002,#12003,#12004,#12005,#12006,#12007,
#12008,#12009,#12010,#12011,#12012,#12013,#12014,#12015,#12016,#12017,#12018,
#12019,#12020,#12021,#12022,#12023,#12024,#12025,#12026,#12027,#12028,#12029,
#12030,#12031,#12032,#12033,#12034,#12035,#12036,#12037,#12038,#12039,#12040,
#12041,#12042,#12043,#12044,#12045,#12046,#12047,#12048,#12049,#12050,#12051,
#12052,#12053,#12054,#12055,#12056,#12057,#12058,#12059,#12060,#12061,#12062,
#12063,#12064,#12065,#12066,#12067,#12068,#12069,#12070,#12071,#12072,#12073,
#12074,#12075,#12076,#12077,#12078,#12079,#12080,#12081,#12082,#12083,#12084,
#12085,#12086,#12087,#12088,#12089,#12090,#12091,#12092,#12093,#12094,#12095,
#12096,#12097,#12098,#12099,#12100,#12101,#12102,#12103,#12104,#12105,#12106,
#12107,#12108,#12109,#12110,#12111,#12112,#12113,#12114,#12115,#12116,#12117,
#12118,#12119,#12120,#12121,#12122,#12123,#12124,#12125),.UNSPECIFIED.,
 .F.,.F.,(4,3,3,3,3,3,3,3,3,3,3,3,3,3,3,3,3,3,3,3,3,3,3,3,3,3,3,3,3,3,3,
3,3,3,3,3,3,3,3,3,3,3,3,3,3,3,3,3,3,3,3,3,3,3,3,3,3,3,3,3,3,3,3,3,3,3,3,
3,3,3,3,3,3,3,3,3,3,3,3,3,3,3,3,3,3,3,3,3,3,3,3,3,3,3,3,3,3,3,3,3,3,3,3,
3,3,3,3,3,3,3,3,3,3,3,4),(32.5258266430594,32.6109724346887,32.6960210961378,
32.7626267165768,32.7809951098591,32.8492755535054,32.8659214354213,32.9837841938069,
33.0357235442058,33.0955474570151,33.1206397523944,33.2056408545587,33.2906886895505,
33.3702936267599,33.3758609577714,33.4255966563581,33.4256273757631,33.5038076716489,
33.5117386977598,33.5977449669701,33.6836677195876,33.7489468907353,33.7695284165969,
33.8414965542859,33.8553570387069,33.9694167254514,34.0269916614943,34.1083538408373,
34.1128363502318,34.1987724988946,34.2847607974944,34.3642063976649,34.3708724891257,
34.4087033319985,34.4087340632856,34.4869140335835,34.4948626039088,34.5808860086697,
34.6668257949821,34.731910342736,34.7527034050599,34.8248937007329,34.8385487008752,
34.9526382498946,35.0102161927437,35.0858142890628,35.0960770425472,35.1820289830922,
35.2680328840028,35.3475020183578,35.3541597537952,35.3918102649572,35.391840750808,
35.470077668493,35.4779957931001,35.564045956927,35.6500127247878,35.7158985485698,
35.7359175043445,35.807382148658,35.8217901462905,35.9358306049138,35.9935126031944,
36.0794010110302,36.1653804190781,36.2514117725677,36.330834342922,36.3375658326432,
36.3749164460689,36.3749474383305,36.4530570251503,36.4609709985879,36.5468894484378,
36.6327244251594,36.6976322862784,36.7184974902785,36.7906951843131,36.8042390095103,
36.9182650828356,36.9757005755,37.0503973116492,37.0614594912268,37.1473111312689,
37.2332155266954,37.3126454208301,37.3192449713843,37.3580232566258,37.3580541258529,
37.4362146806441,37.4442653932351,37.5303710041113,37.616392385932,37.6802782697322,
37.7023508908437,37.7760215559506,37.7882757520974,37.9025348642431,37.9600997363509,
38.0195474650972,38.0460373477549,38.132064110626,38.2181418243531,38.2977501570041,
38.3043403342073,38.3411317666744,38.3411608133753,38.4219344625309,38.4323669275132,
38.5186731840825,38.5265281831132,38.6173539858577,38.6828524694273,38.7080464538249,
38.7985713335135,38.8090119499132),.UNSPECIFIED.);
#1414=B_SPLINE_CURVE_WITH_KNOTS('',3,(#12127,#12128,#12129,#12130,#12131,
#12132,#12133,#12134,#12135,#12136,#12137,#12138,#12139,#12140,#12141,#12142,
#12143,#12144,#12145,#12146,#12147,#12148,#12149,#12150,#12151,#12152,#12153,
#12154,#12155,#12156,#12157,#12158,#12159,#12160,#12161,#12162,#12163,#12164,
#12165,#12166,#12167,#12168,#12169,#12170,#12171,#12172,#12173,#12174,#12175,
#12176,#12177,#12178,#12179,#12180,#12181,#12182,#12183,#12184,#12185,#12186,
#12187,#12188,#12189,#12190,#12191,#12192,#12193,#12194,#12195,#12196,#12197,
#12198,#12199,#12200,#12201,#12202,#12203,#12204,#12205),.UNSPECIFIED.,
 .F.,.F.,(4,3,3,3,3,3,3,3,3,3,3,3,3,3,3,3,3,3,3,3,3,3,3,3,3,3,4),(38.8090119500397,
38.8859986035339,38.8986001599551,38.9583027320439,38.9882861023177,39.0781574059986,
39.1681251672574,39.2510575887847,39.2582803096457,39.3242338171694,39.3242675008978,
39.4010604352791,39.4085522045926,39.4927322947236,39.5768309331739,39.6386139026977,
39.6608734290088,39.7326664346078,39.7448872573002,39.8632170642639,39.9129119571121,
39.973722445964,39.9970107280833,40.0670781135363,40.0811536853461,40.1654173637519,
40.2123859659494),.UNSPECIFIED.);
#1415=B_SPLINE_CURVE_WITH_KNOTS('',3,(#12209,#12210,#12211,#12212,#12213,
#12214,#12215,#12216,#12217,#12218,#12219,#12220),.UNSPECIFIED.,.F.,.F.,
(4,2,2,2,2,4),(0.,0.0190431087261921,0.0547437896044447,0.10678546066118,
0.157808217256731,0.213640188390348),.UNSPECIFIED.);
#1416=B_SPLINE_CURVE_WITH_KNOTS('',3,(#12222,#12223,#12224,#12225,#12226,
#12227,#12228,#12229,#12230,#12231,#12232,#12233,#12234,#12235,#12236,#12237,
#12238,#12239,#12240,#12241,#12242,#12243,#12244,#12245,#12246,#12247,#12248,
#12249,#12250,#12251,#12252,#12253,#12254,#12255,#12256,#12257,#12258,#12259,
#12260,#12261,#12262,#12263,#12264,#12265,#12266,#12267,#12268,#12269,#12270,
#12271,#12272,#12273,#12274,#12275,#12276,#12277,#12278,#12279,#12280,#12281,
#12282,#12283,#12284,#12285,#12286,#12287,#12288,#12289,#12290,#12291,#12292,
#12293,#12294,#12295,#12296,#12297,#12298,#12299,#12300,#12301,#12302,#12303,
#12304,#12305,#12306,#12307,#12308,#12309,#12310,#12311,#12312,#12313,#12314,
#12315,#12316,#12317,#12318,#12319,#12320,#12321,#12322,#12323,#12324,#12325,
#12326,#12327,#12328,#12329,#12330,#12331,#12332,#12333,#12334,#12335,#12336,
#12337,#12338,#12339,#12340,#12341,#12342,#12343,#12344,#12345,#12346,#12347,
#12348,#12349,#12350,#12351,#12352,#12353,#12354,#12355,#12356,#12357,#12358,
#12359,#12360,#12361,#12362,#12363,#12364,#12365,#12366,#12367,#12368,#12369,
#12370,#12371,#12372,#12373,#12374,#12375,#12376,#12377,#12378,#12379,#12380,
#12381,#12382,#12383,#12384,#12385,#12386,#12387,#12388,#12389,#12390,#12391,
#12392,#12393,#12394,#12395,#12396,#12397,#12398,#12399,#12400,#12401,#12402,
#12403,#12404,#12405,#12406,#12407,#12408,#12409,#12410,#12411,#12412,#12413,
#12414,#12415,#12416,#12417,#12418,#12419,#12420,#12421,#12422,#12423,#12424,
#12425,#12426,#12427,#12428,#12429,#12430,#12431,#12432,#12433,#12434,#12435,
#12436,#12437,#12438,#12439,#12440,#12441,#12442,#12443,#12444,#12445,#12446,
#12447,#12448,#12449,#12450,#12451,#12452,#12453,#12454,#12455,#12456,#12457,
#12458,#12459,#12460,#12461,#12462,#12463,#12464,#12465,#12466,#12467,#12468,
#12469,#12470,#12471,#12472,#12473,#12474,#12475,#12476,#12477,#12478,#12479,
#12480,#12481,#12482,#12483,#12484,#12485,#12486,#12487,#12488,#12489,#12490,
#12491,#12492,#12493,#12494,#12495,#12496,#12497,#12498,#12499,#12500,#12501,
#12502,#12503,#12504,#12505,#12506,#12507,#12508,#12509,#12510,#12511,#12512,
#12513,#12514,#12515,#12516,#12517,#12518,#12519,#12520,#12521,#12522,#12523,
#12524,#12525,#12526,#12527,#12528,#12529,#12530,#12531,#12532,#12533,#12534,
#12535,#12536,#12537,#12538,#12539,#12540,#12541,#12542,#12543,#12544,#12545,
#12546,#12547,#12548,#12549,#12550,#12551,#12552),.UNSPECIFIED.,.F.,.F.,
(4,3,3,3,3,3,3,3,3,3,3,3,3,3,3,3,3,3,3,3,3,3,3,3,3,3,3,3,3,3,3,3,3,3,3,
3,3,3,3,3,3,3,3,3,3,3,3,3,3,3,3,3,3,3,3,3,3,3,3,3,3,3,3,3,3,3,3,3,3,3,3,
3,3,3,3,3,3,3,3,3,3,3,3,3,3,3,3,3,3,3,3,3,3,3,3,3,3,3,3,3,3,3,3,3,3,3,3,
3,3,3,4),(-41.79200593275,-41.7820342197039,-41.7820289155157,-41.6950743300943,
-41.6081223321859,-41.5211282447415,-41.4341127720792,-41.3470146427639,
-41.2905004994869,-41.2904808759427,-41.2098667853675,-41.20336832383,-41.1163307621064,
-41.0585781090169,-41.0293484847566,-40.9391016977146,-40.82443344383,-40.7126439695405,
-40.6782149646209,-40.6237387775751,-40.5911902746634,-40.5040544223173,
-40.4168531658136,-40.3384683697826,-40.329521224308,-40.3074046461754,
-40.3073741884203,-40.2298340840655,-40.2220564467519,-40.1368545416153,
-40.0517460197423,-39.9925639013076,-39.9667085240719,-39.8817137263903,
-39.7681210243195,-39.7117654161815,-39.6554187743151,-39.6267716751265,
-39.5416895547738,-39.4565583215444,-39.3772848419879,-39.3713009176492,
-39.3243006969237,-39.3242675008978,-39.2461857144567,-39.2379295253732,
-39.1516949070862,-39.0655424093964,-38.9828521641219,-38.9749947098938,
-38.9133947084934,-38.8889356671652,-38.8028892415144,-38.7168363522496,
-38.6546592803102,-38.6307579188814,-38.5445890611926,-38.4583677184446,
-38.3789423236917,-38.3720269721772,-38.3411900255245,-38.3411608133754,
-38.2627688277661,-38.2549622066264,-38.1688668587652,-38.0828533517434,
-38.0212440044143,-37.9969003407262,-37.9109774199415,-37.7969393456923,
-37.7391506754001,-37.6651611227124,-37.6532083630363,-37.567173590932,
-37.4810859630649,-37.4017323695988,-37.3948747178714,-37.3580850021048,
-37.3580541258529,-37.279951088596,-37.2720238464053,-37.1860999512967,
-37.1002607981332,-37.0353332851499,-37.0144848214179,-36.9423340886966,
-36.9287422802383,-36.8147224638751,-36.7572821980678,-36.683026967767,
-36.6715257881743,-36.5856784152043,-36.4997792987108,-36.4203402253949,
-36.4137566395602,-36.3749783802581,-36.3749474383305,-36.2974958690074,
-36.2899292270807,-36.2050152151128,-36.1179908982539,-36.0505591832992,
-36.0332183657195,-35.9653932816982,-35.9484752386565,-35.8291557711193,
-35.7750110506216,-35.6901947599964,-35.6053351568716,-35.5203766098291,
-35.5088206802422),.UNSPECIFIED.);
#1417=B_SPLINE_CURVE_WITH_KNOTS('',3,(#12554,#12555,#12556,#12557,#12558,
#12559,#12560,#12561,#12562,#12563,#12564,#12565,#12566,#12567,#12568,#12569,
#12570,#12571,#12572,#12573,#12574,#12575,#12576,#12577,#12578,#12579,#12580,
#12581,#12582,#12583,#12584,#12585,#12586,#12587,#12588,#12589,#12590,#12591,
#12592,#12593,#12594,#12595,#12596,#12597,#12598,#12599,#12600,#12601,#12602,
#12603,#12604,#12605,#12606,#12607,#12608,#12609,#12610,#12611,#12612,#12613,
#12614,#12615,#12616,#12617,#12618,#12619,#12620,#12621,#12622,#12623,#12624,
#12625,#12626,#12627,#12628,#12629,#12630,#12631,#12632,#12633,#12634,#12635,
#12636,#12637,#12638,#12639,#12640,#12641,#12642,#12643,#12644,#12645,#12646,
#12647,#12648,#12649,#12650,#12651,#12652,#12653,#12654,#12655,#12656,#12657,
#12658,#12659,#12660,#12661,#12662,#12663,#12664,#12665,#12666,#12667,#12668,
#12669,#12670,#12671,#12672,#12673,#12674,#12675,#12676,#12677,#12678,#12679,
#12680,#12681,#12682,#12683,#12684,#12685,#12686,#12687,#12688,#12689,#12690,
#12691,#12692,#12693,#12694,#12695,#12696,#12697,#12698,#12699,#12700,#12701,
#12702,#12703,#12704,#12705,#12706,#12707,#12708,#12709,#12710,#12711,#12712,
#12713,#12714,#12715,#12716,#12717,#12718,#12719,#12720,#12721,#12722,#12723,
#12724,#12725,#12726,#12727,#12728,#12729,#12730,#12731,#12732,#12733,#12734,
#12735,#12736,#12737,#12738,#12739,#12740,#12741,#12742,#12743,#12744,#12745,
#12746,#12747,#12748,#12749,#12750,#12751,#12752,#12753,#12754,#12755,#12756,
#12757,#12758,#12759,#12760,#12761,#12762,#12763,#12764,#12765,#12766,#12767,
#12768,#12769,#12770,#12771,#12772,#12773,#12774,#12775,#12776,#12777,#12778,
#12779,#12780,#12781,#12782,#12783,#12784,#12785,#12786,#12787,#12788,#12789,
#12790,#12791,#12792,#12793,#12794,#12795,#12796,#12797,#12798,#12799,#12800,
#12801,#12802,#12803,#12804,#12805,#12806,#12807,#12808,#12809,#12810,#12811,
#12812,#12813,#12814,#12815,#12816,#12817,#12818,#12819,#12820,#12821,#12822,
#12823,#12824,#12825,#12826,#12827,#12828,#12829,#12830,#12831,#12832,#12833,
#12834,#12835,#12836,#12837,#12838,#12839,#12840,#12841,#12842,#12843,#12844,
#12845,#12846,#12847,#12848,#12849,#12850,#12851,#12852,#12853,#12854,#12855,
#12856,#12857,#12858,#12859,#12860,#12861,#12862,#12863,#12864,#12865,#12866,
#12867,#12868,#12869,#12870,#12871,#12872,#12873,#12874,#12875,#12876,#12877,
#12878,#12879,#12880,#12881,#12882,#12883,#12884,#12885,#12886,#12887,#12888,
#12889,#12890,#12891,#12892,#12893,#12894,#12895,#12896,#12897,#12898,#12899),
 .UNSPECIFIED.,.F.,.F.,(4,3,3,3,3,3,3,3,3,3,3,3,3,3,3,3,3,3,3,3,3,3,3,3,
3,3,3,3,3,3,3,3,3,3,3,3,3,3,3,3,3,3,3,3,3,3,3,3,3,3,3,3,3,3,3,3,3,3,3,3,
3,3,3,3,3,3,3,3,3,3,3,3,3,3,3,3,3,3,3,3,3,3,3,3,3,3,3,3,3,3,3,3,3,3,3,3,
3,3,3,3,3,3,3,3,3,3,3,3,3,3,3,3,3,3,3,4),(-35.5088206800413,-35.4252279654651,
-35.3918712573551,-35.391840750808,-35.3136311441657,-35.3057134673612,
-35.2196910812655,-35.1337520760534,-35.0690300403527,-35.0478750102457,
-34.974784245045,-34.9620299050909,-34.8479689727154,-34.7903621339832,
-34.7106196849279,-34.7045008142665,-34.6185480744502,-34.5325431848047,
-34.45310662989,-34.4464150450444,-34.4087647906727,-34.4087340632856,-34.330557471788,
-34.322621901095,-34.2366149523578,-34.1506916802349,-34.0853841922607,
-34.0648306232373,-33.9929355963962,-33.9790018793112,-33.8649399597694,
-33.8073674577515,-33.7267315923107,-33.7215230920524,-33.6355874882297,
-33.5495998620446,-33.4701499889646,-33.4634890322309,-33.4256580877462,
-33.4256273757631,-33.3474387042409,-33.3395005067057,-33.2534786438155,
-33.1675402695245,-33.1021242827212,-33.0816639413529,-33.0098835327419,
-32.9958197308907,-32.8817497850192,-32.8241540417499,-32.7382939081162,
-32.6523424946626,-32.5663390135018,-32.4868863076403,-32.480212396575,
-32.4425513556011,-32.4425206882407,-32.3643306588553,-32.3563981804201,
-32.2703807156258,-32.1844467706973,-32.119233340652,-32.0985748976172,
-32.02645504593,-32.0127351638982,-31.898669787616,-31.8410784596148,-31.7599527945309,
-31.7552228243167,-31.6692758881938,-31.5832768784092,-31.5038289086898,
-31.4971546848244,-31.4594446960179,-31.4594140007183,-31.3812276090757,
-31.3732926541172,-31.2872763803364,-31.20134365462,-31.136046512765,-31.1154730273881,
-31.0435108360474,-31.0296345746987,-30.9155686400612,-30.8579804957934,
-30.7766425020302,-30.7721262021939,-30.6861806291898,-30.6001829966384,
-30.5207331340705,-30.514062190079,-30.4763380040283,-30.4763073131958,
-30.3981192712659,-30.3901842891515,-30.3041663129045,-30.2182318619066,
-30.1529317867028,-30.1323594887544,-30.0603936548166,-30.046519265842,
-29.9324525368224,-29.8748616045711,-29.7933742647299,-29.7890055026128,
-29.7030581146527,-29.6170586609049,-29.5376086899911,-29.5309360393539,
-29.4932313122272,-29.4932006256734,-29.4094094906891,-29.3853784705262,
-29.2988803407037,-29.2791332454367,-29.2256353730422),.UNSPECIFIED.);
#1418=B_SPLINE_CURVE_WITH_KNOTS('',3,(#12901,#12902,#12903,#12904,#12905,
#12906,#12907,#12908,#12909,#12910,#12911,#12912,#12913,#12914,#12915,#12916,
#12917,#12918,#12919,#12920,#12921,#12922,#12923,#12924,#12925,#12926,#12927,
#12928,#12929,#12930,#12931,#12932,#12933,#12934,#12935,#12936,#12937,#12938,
#12939,#12940,#12941,#12942,#12943,#12944,#12945,#12946,#12947,#12948,#12949,
#12950,#12951,#12952,#12953,#12954,#12955,#12956,#12957,#12958,#12959,#12960,
#12961,#12962,#12963,#12964,#12965,#12966,#12967,#12968,#12969,#12970,#12971,
#12972,#12973,#12974,#12975,#12976,#12977,#12978,#12979,#12980,#12981,#12982,
#12983,#12984,#12985,#12986,#12987,#12988,#12989,#12990,#12991,#12992,#12993,
#12994,#12995,#12996,#12997,#12998,#12999,#13000,#13001,#13002,#13003,#13004,
#13005,#13006,#13007,#13008,#13009,#13010,#13011,#13012,#13013,#13014,#13015,
#13016,#13017,#13018,#13019,#13020,#13021,#13022,#13023,#13024,#13025,#13026,
#13027,#13028,#13029,#13030,#13031,#13032,#13033,#13034,#13035,#13036,#13037,
#13038,#13039,#13040,#13041,#13042,#13043,#13044,#13045,#13046,#13047,#13048,
#13049,#13050,#13051,#13052,#13053,#13054,#13055,#13056,#13057,#13058,#13059,
#13060,#13061,#13062,#13063,#13064,#13065,#13066,#13067,#13068,#13069,#13070,
#13071,#13072,#13073,#13074,#13075,#13076,#13077,#13078,#13079,#13080,#13081,
#13082,#13083,#13084,#13085,#13086,#13087,#13088,#13089,#13090,#13091,#13092,
#13093,#13094,#13095,#13096,#13097,#13098,#13099,#13100,#13101,#13102,#13103,
#13104,#13105,#13106,#13107,#13108,#13109,#13110,#13111,#13112,#13113,#13114,
#13115,#13116,#13117,#13118,#13119,#13120,#13121,#13122,#13123,#13124,#13125,
#13126,#13127,#13128,#13129,#13130,#13131,#13132,#13133,#13134,#13135,#13136,
#13137,#13138,#13139,#13140,#13141,#13142,#13143,#13144,#13145,#13146,#13147,
#13148,#13149,#13150,#13151,#13152,#13153,#13154,#13155,#13156,#13157,#13158,
#13159,#13160,#13161,#13162,#13163,#13164,#13165,#13166,#13167,#13168,#13169,
#13170,#13171,#13172,#13173,#13174,#13175,#13176,#13177,#13178,#13179,#13180,
#13181,#13182,#13183,#13184,#13185,#13186,#13187,#13188,#13189,#13190,#13191,
#13192,#13193,#13194,#13195,#13196,#13197,#13198,#13199,#13200,#13201,#13202,
#13203,#13204,#13205,#13206,#13207,#13208,#13209,#13210,#13211,#13212,#13213,
#13214,#13215,#13216,#13217,#13218,#13219,#13220,#13221,#13222,#13223,#13224,
#13225,#13226,#13227,#13228,#13229,#13230,#13231,#13232,#13233,#13234,#13235,
#13236,#13237,#13238,#13239,#13240,#13241,#13242,#13243),.UNSPECIFIED.,
 .F.,.F.,(4,3,3,3,3,3,3,3,3,3,3,3,3,3,3,3,3,3,3,3,3,3,3,3,3,3,3,3,3,3,3,
3,3,3,3,3,3,3,3,3,3,3,3,3,3,3,3,3,3,3,3,3,3,3,3,3,3,3,3,3,3,3,3,3,3,3,3,
3,3,3,3,3,3,3,3,3,3,3,3,3,3,3,3,3,3,3,3,3,3,3,3,3,3,3,3,3,3,3,3,3,3,3,3,
3,3,3,3,3,3,3,3,3,3,3,4),(-29.2256353728617,-29.1630398051076,-29.1361926935229,
-29.0511260979808,-28.9353197102132,-28.88102302201,-28.8096224637669,-28.7959463909764,
-28.7107799985853,-28.6255612560834,-28.5471267143894,-28.5402214425233,
-28.5101246280994,-28.5100939381509,-28.4319063030582,-28.4239716056522,
-28.3379543299007,-28.2520205874456,-28.1867311485525,-28.1661489299919,
-28.0941676710746,-28.0803094307853,-27.9662431504983,-27.9086532304487,
-27.8272624804431,-27.822797864162,-27.7368512127461,-27.6508524970411,
-27.5714027865234,-27.5647306094304,-27.5270179397605,-27.5269872506285,
-27.4487994016289,-27.4408647342574,-27.3548472717257,-27.2689133398253,
-27.2036247164402,-27.1830414905009,-27.1110577884387,-27.0972017965172,
-26.9831354437756,-26.9255452015783,-26.8441422998106,-26.8396896358817,
-26.7537427841098,-26.6677438672355,-26.5882941708569,-26.5816217789496,
-26.5439112518674,-26.543880563106,-26.4656927382692,-26.4577581324764,
-26.3717407566645,-26.2858069123508,-26.2205205104771,-26.1999351513698,
-26.1279479104358,-26.1140955465289,-26.0000292610949,-25.9424391311903,
-25.8610515026847,-25.856583655759,-25.7706368941827,-25.6846380675869,
-25.6051884242157,-25.598516068922,-25.5608045647431,-25.5607738755836,
-25.4825860890327,-25.4746514425571,-25.3886340645148,-25.3027002181393,
-25.2374124146042,-25.216828455268,-25.1448437226632,-25.1309888488002,
-25.0169225441039,-24.9593324307051,-24.8779394469641,-24.8734769541487,
-24.7875301917118,-24.7015313644052,-24.6220816888261,-24.6154093652677,
-24.5776978770929,-24.5776671880611,-24.4994793748203,-24.4915447356144,
-24.4055273378264,-24.3195934714057,-24.2543058956866,-24.2337216882146,
-24.1617364426304,-24.1478820610932,-24.033815750705,-23.9762256011071,
-23.8948318526411,-23.8903701033575,-23.8044233196025,-23.7184244708774,
-23.6389748000345,-23.6323024503526,-23.594591189544,-23.5945605005387,
-23.5164327751492,-23.5084383448351,-23.4224191446739,-23.3364834599017,
-23.2711382794071,-23.2506119149563,-23.1786842672096,-23.1647805520879,
-23.0511684817596,-22.9931527448939,-22.9424500656821),.UNSPECIFIED.);
#1419=B_SPLINE_CURVE_WITH_KNOTS('',3,(#13245,#13246,#13247,#13248,#13249,
#13250,#13251,#13252,#13253,#13254,#13255,#13256,#13257,#13258,#13259,#13260,
#13261,#13262,#13263,#13264,#13265,#13266,#13267,#13268,#13269,#13270,#13271,
#13272,#13273,#13274,#13275,#13276,#13277,#13278,#13279,#13280,#13281,#13282,
#13283,#13284,#13285,#13286,#13287,#13288,#13289,#13290,#13291,#13292,#13293,
#13294,#13295,#13296,#13297,#13298,#13299,#13300,#13301,#13302,#13303,#13304,
#13305,#13306,#13307,#13308,#13309,#13310,#13311,#13312,#13313,#13314,#13315,
#13316,#13317,#13318,#13319,#13320,#13321,#13322,#13323,#13324,#13325,#13326,
#13327,#13328,#13329,#13330,#13331,#13332,#13333,#13334,#13335,#13336,#13337,
#13338,#13339,#13340,#13341,#13342,#13343,#13344,#13345,#13346,#13347,#13348,
#13349,#13350,#13351,#13352,#13353,#13354,#13355,#13356,#13357,#13358,#13359,
#13360,#13361,#13362,#13363,#13364,#13365,#13366,#13367,#13368,#13369,#13370,
#13371,#13372,#13373,#13374,#13375,#13376,#13377,#13378,#13379,#13380,#13381,
#13382,#13383,#13384,#13385,#13386,#13387,#13388,#13389,#13390,#13391,#13392,
#13393,#13394,#13395,#13396,#13397,#13398,#13399,#13400,#13401,#13402,#13403,
#13404,#13405,#13406,#13407,#13408,#13409,#13410,#13411,#13412,#13413,#13414,
#13415,#13416,#13417,#13418,#13419,#13420,#13421,#13422,#13423,#13424,#13425,
#13426,#13427,#13428,#13429,#13430,#13431,#13432,#13433,#13434,#13435,#13436,
#13437,#13438,#13439,#13440,#13441,#13442,#13443,#13444,#13445,#13446,#13447,
#13448,#13449,#13450,#13451,#13452,#13453,#13454,#13455,#13456,#13457,#13458,
#13459,#13460,#13461,#13462,#13463,#13464,#13465,#13466,#13467,#13468,#13469,
#13470,#13471,#13472,#13473,#13474,#13475,#13476,#13477,#13478,#13479,#13480,
#13481,#13482,#13483,#13484,#13485,#13486,#13487,#13488,#13489,#13490,#13491,
#13492,#13493,#13494,#13495,#13496,#13497,#13498,#13499,#13500,#13501,#13502,
#13503,#13504,#13505,#13506,#13507,#13508,#13509,#13510,#13511,#13512,#13513,
#13514,#13515,#13516,#13517,#13518,#13519,#13520,#13521,#13522,#13523,#13524,
#13525,#13526,#13527,#13528,#13529,#13530,#13531,#13532,#13533,#13534,#13535,
#13536,#13537,#13538,#13539,#13540,#13541,#13542,#13543,#13544,#13545,#13546,
#13547,#13548,#13549,#13550,#13551,#13552,#13553,#13554,#13555,#13556,#13557,
#13558,#13559,#13560,#13561,#13562,#13563,#13564,#13565,#13566,#13567,#13568,
#13569,#13570,#13571,#13572,#13573,#13574,#13575,#13576,#13577,#13578,#13579,
#13580,#13581,#13582,#13583,#13584,#13585,#13586,#13587,#13588,#13589,#13590,
#13591,#13592,#13593,#13594,#13595,#13596),.UNSPECIFIED.,.F.,.F.,(4,3,3,
3,3,3,3,3,3,3,3,3,3,3,3,3,3,3,3,3,3,3,3,3,3,3,3,3,3,3,3,3,3,3,3,3,3,3,3,
3,3,3,3,3,3,3,3,3,3,3,3,3,3,3,3,3,3,3,3,3,3,3,3,3,3,3,3,3,3,3,3,3,3,3,3,
3,3,3,3,3,3,3,3,3,3,3,3,3,3,3,3,3,3,3,3,3,3,3,3,3,3,3,3,3,3,3,3,3,3,3,3,
3,3,3,3,3,3,4),(-22.9424500654772,-22.8507510669165,-22.8432492269214,-22.7550777090342,
-22.743518032141,-22.6599168656772,-22.6431790088504,-22.6114845020791,
-22.6114538130162,-22.5332660091545,-22.525331370706,-22.4393139831972,
-22.3533801271849,-22.288092600173,-22.2675083545179,-22.1955230788735,
-22.1816687380548,-22.0676024323464,-22.0100122996148,-21.9286196934413,
-21.92415681273,-21.838210039868,-21.7522112020671,-21.6727615321577,-21.6660891924192,
-21.6283778145229,-21.6283471254938,-21.5501593170398,-21.5422246798375,
-21.4562072889451,-21.370273429516,-21.3049859330506,-21.2844016534033,
-21.2124163014448,-21.1985620334634,-21.084495727377,-21.0269055880192,
-20.9455126904598,-20.9410500976143,-20.855103321235,-20.7691044799135,
-20.6896548110226,-20.6829824667704,-20.6452711270011,-20.6452404379714,
-20.5670526310498,-20.5591179957949,-20.4731006083946,-20.3871667524656,
-20.3218792629951,-20.3012949798572,-20.2293096167709,-20.215455363415,
-20.1013890607534,-20.0437989249469,-19.9624057597513,-19.9579434380131,
-19.8719966650674,-19.7859978271626,-19.7065481606488,-19.6998758173811,
-19.6621644395034,-19.6621337504489,-19.5839459482762,-19.5760113092192,
-19.4899939227884,-19.4040600678502,-19.338772629847,-19.3181882962524,
-19.246202899276,-19.2323486808462,-19.1182823723598,-19.0606922444959,
-18.979301196102,-18.9748367586413,-18.8888899867884,-18.8028911499858,
-18.7234414782139,-18.716769141311,-18.6790577519268,-18.6790270629265,
-18.6008392476307,-18.5929046099203,-18.5068872116786,-18.4209533449092,
-18.3556657989052,-18.3350815614742,-18.2630962457753,-18.2492419342651,
-18.1351756270659,-18.0775854743959,-17.9961912899178,-17.9917299768508,
-17.905783193446,-17.8197843451551,-17.7403346763732,-17.733662325189,-17.6959510644389,
-17.695920375404,-17.6177325704747,-17.609797943694,-17.5237805667203,-17.4378467211662,
-17.3725591380261,-17.3519749588694,-17.2799897136122,-17.2661353526079,
-17.1520690646227,-17.0944789342378,-17.0130826630226,-17.0086234572,-16.9226766939388,
-16.8366778656107,-16.7572282103778,-16.7505558651585,-16.7128443770544,
-16.7128136878816,-16.6592647585025),.UNSPECIFIED.);
#1420=B_SPLINE_CURVE_WITH_KNOTS('',3,(#13598,#13599,#13600,#13601,#13602,
#13603,#13604,#13605,#13606,#13607,#13608,#13609,#13610,#13611,#13612,#13613,
#13614,#13615,#13616,#13617,#13618,#13619,#13620,#13621,#13622,#13623,#13624,
#13625,#13626,#13627,#13628,#13629,#13630,#13631,#13632,#13633,#13634,#13635,
#13636,#13637,#13638,#13639,#13640,#13641,#13642,#13643,#13644,#13645,#13646,
#13647,#13648,#13649,#13650,#13651,#13652,#13653,#13654,#13655,#13656,#13657,
#13658,#13659,#13660,#13661,#13662,#13663,#13664,#13665,#13666,#13667,#13668,
#13669,#13670,#13671,#13672,#13673,#13674,#13675,#13676,#13677,#13678,#13679,
#13680,#13681,#13682,#13683,#13684,#13685,#13686,#13687,#13688,#13689,#13690,
#13691,#13692,#13693,#13694,#13695,#13696,#13697,#13698,#13699,#13700,#13701,
#13702,#13703,#13704,#13705,#13706,#13707,#13708,#13709,#13710,#13711,#13712,
#13713,#13714,#13715,#13716,#13717,#13718,#13719,#13720,#13721,#13722,#13723,
#13724,#13725,#13726,#13727,#13728,#13729,#13730,#13731,#13732,#13733,#13734,
#13735,#13736,#13737,#13738,#13739,#13740,#13741,#13742,#13743,#13744,#13745,
#13746,#13747,#13748,#13749,#13750,#13751,#13752,#13753,#13754,#13755,#13756,
#13757,#13758,#13759,#13760,#13761,#13762,#13763,#13764,#13765,#13766,#13767,
#13768,#13769,#13770,#13771,#13772,#13773,#13774,#13775,#13776,#13777,#13778,
#13779,#13780,#13781,#13782,#13783,#13784,#13785,#13786,#13787,#13788,#13789,
#13790,#13791,#13792,#13793,#13794,#13795,#13796,#13797,#13798,#13799,#13800,
#13801,#13802,#13803,#13804,#13805,#13806,#13807,#13808,#13809,#13810,#13811,
#13812,#13813,#13814,#13815,#13816,#13817,#13818,#13819,#13820,#13821,#13822,
#13823,#13824,#13825,#13826,#13827,#13828,#13829,#13830,#13831,#13832,#13833,
#13834,#13835,#13836,#13837,#13838,#13839,#13840,#13841,#13842,#13843,#13844,
#13845,#13846,#13847,#13848,#13849,#13850,#13851,#13852,#13853,#13854,#13855,
#13856,#13857,#13858,#13859,#13860,#13861,#13862,#13863,#13864,#13865,#13866,
#13867,#13868,#13869,#13870,#13871,#13872,#13873,#13874,#13875,#13876,#13877,
#13878,#13879,#13880,#13881,#13882,#13883,#13884,#13885,#13886,#13887,#13888,
#13889,#13890,#13891,#13892,#13893,#13894,#13895,#13896,#13897,#13898,#13899,
#13900,#13901,#13902,#13903,#13904,#13905,#13906,#13907,#13908,#13909,#13910,
#13911,#13912,#13913,#13914,#13915,#13916,#13917,#13918,#13919,#13920,#13921,
#13922,#13923,#13924,#13925,#13926,#13927,#13928,#13929,#13930,#13931,#13932,
#13933,#13934,#13935,#13936,#13937),.UNSPECIFIED.,.F.,.F.,(4,3,3,3,3,3,
3,3,3,3,3,3,3,3,3,3,3,3,3,3,3,3,3,3,3,3,3,3,3,3,3,3,3,3,3,3,3,3,3,3,3,3,
3,3,3,3,3,3,3,3,3,3,3,3,3,3,3,3,3,3,3,3,3,3,3,3,3,3,3,3,3,3,3,3,3,3,3,3,
3,3,3,3,3,3,3,3,3,3,3,3,3,3,3,3,3,3,3,3,3,3,3,3,3,3,3,3,3,3,3,3,3,3,3,4),
(-16.6592647583439,-16.57834727546,-16.5738430149373,-16.4885227334712,
-16.4032816523275,-16.3459598776537,-16.3180945864984,-16.2004506632273,
-16.1477847574117,-16.0817816596509,-16.0626219831902,-15.9942979489986,
-15.9773761668429,-15.8920884458071,-15.8066680671297,-15.7297376890762,
-15.7297070003591,-15.651519114883,-15.6435844798867,-15.5575670140271,
-15.471633079569,-15.4063449429491,-15.3857612284546,-15.3137763848075,
-15.2999215338279,-15.1858552272951,-15.1282649397453,-15.0468548409394,
-15.0424093755484,-14.9564625263443,-14.8704636126523,-14.7910139547004,
-14.7843415284612,-14.7466310020105,-14.7466003128367,-14.6684125526381,
-14.6604779921827,-14.5744607260426,-14.4885269909739,-14.4232390313135,
-14.4026553386888,-14.3306706437354,-14.3168158413389,-14.2027496692409,
-14.145159638529,-14.0637467865836,-14.0593042679126,-13.9733576090808,
-13.8873588841852,-13.8079093131886,-13.8012369847486,-13.7635243153496,
-13.7634936253142,-13.685306041895,-13.6773712241262,-13.5913538790123,
-13.5054200666001,-13.4401363550069,-13.4195483386733,-13.3475593369649,
-13.3337087684636,-13.2196421674157,-13.162052425251,-13.0807773831844,
-13.0761969872289,-12.99025026418,-12.9042514768019,-12.8248015432038,-12.8181295180617,
-12.7804176239796,-12.7803869377918,-12.7021984322804,-12.6942638863894,
-12.6082458879433,-12.5223114198845,-12.457017353168,-12.4364390347946,
-12.3644591608565,-12.3505988075939,-12.2365326173997,-12.1789411520357,
-12.0930850600792,-12.0071376892478,-11.9211382567276,-11.8416887815353,
-11.8350156624911,-11.7973109415761,-11.7972802502693,-11.719093095323,
-11.7111590060667,-11.6251428153763,-11.5392101535174,-11.4739218216529,
-11.4533395709698,-11.3813569797693,-11.367501134333,-11.2534358016061,
-11.195847034049,-11.1143771280478,-11.1099927030158,-11.0240470659038,
-10.9380493539021,-10.858600351834,-10.851928445109,-10.8142042584984,-10.8141735627469,
-10.7330908037065,-10.7213212232863,-10.6350324102581,-10.6287599994176,
-10.5363786705168,-10.4732766489798,-10.4442738471014,-10.3760794514417),
 .UNSPECIFIED.);
#1421=B_SPLINE_CURVE_WITH_KNOTS('',3,(#13938,#13939,#13940,#13941,#13942,
#13943,#13944,#13945,#13946,#13947,#13948,#13949,#13950,#13951,#13952,#13953,
#13954,#13955,#13956,#13957,#13958,#13959,#13960,#13961,#13962,#13963,#13964,
#13965,#13966,#13967,#13968,#13969,#13970,#13971,#13972,#13973,#13974,#13975,
#13976,#13977,#13978,#13979,#13980,#13981,#13982,#13983,#13984,#13985,#13986,
#13987,#13988,#13989,#13990,#13991,#13992,#13993,#13994,#13995,#13996,#13997,
#13998,#13999,#14000,#14001,#14002,#14003,#14004,#14005,#14006,#14007,#14008,
#14009,#14010,#14011,#14012,#14013,#14014,#14015,#14016,#14017,#14018,#14019,
#14020,#14021,#14022,#14023,#14024,#14025,#14026,#14027,#14028,#14029,#14030,
#14031,#14032,#14033,#14034,#14035,#14036,#14037,#14038,#14039,#14040,#14041,
#14042,#14043,#14044,#14045,#14046,#14047,#14048,#14049,#14050,#14051,#14052,
#14053,#14054,#14055,#14056,#14057,#14058,#14059,#14060,#14061,#14062,#14063,
#14064,#14065,#14066,#14067,#14068,#14069,#14070,#14071,#14072,#14073,#14074,
#14075,#14076,#14077,#14078,#14079,#14080,#14081,#14082,#14083,#14084,#14085,
#14086,#14087,#14088,#14089,#14090,#14091,#14092,#14093,#14094,#14095,#14096,
#14097,#14098,#14099,#14100,#14101,#14102,#14103,#14104,#14105,#14106,#14107,
#14108,#14109,#14110,#14111,#14112,#14113,#14114,#14115,#14116,#14117,#14118,
#14119,#14120,#14121,#14122,#14123,#14124,#14125,#14126,#14127,#14128,#14129,
#14130,#14131,#14132,#14133,#14134,#14135,#14136,#14137,#14138,#14139,#14140,
#14141,#14142,#14143,#14144,#14145,#14146,#14147,#14148,#14149,#14150,#14151,
#14152,#14153,#14154,#14155,#14156,#14157,#14158,#14159,#14160,#14161,#14162,
#14163,#14164,#14165,#14166,#14167,#14168,#14169,#14170,#14171,#14172,#14173,
#14174,#14175,#14176,#14177,#14178,#14179,#14180,#14181,#14182,#14183,#14184,
#14185,#14186,#14187,#14188,#14189,#14190,#14191,#14192,#14193,#14194,#14195,
#14196,#14197,#14198,#14199,#14200,#14201,#14202,#14203,#14204,#14205,#14206,
#14207,#14208,#14209,#14210,#14211,#14212,#14213,#14214,#14215,#14216,#14217,
#14218,#14219,#14220,#14221,#14222,#14223,#14224,#14225,#14226,#14227,#14228,
#14229,#14230,#14231,#14232,#14233,#14234,#14235,#14236,#14237,#14238,#14239,
#14240,#14241,#14242,#14243,#14244,#14245,#14246,#14247,#14248,#14249,#14250,
#14251,#14252,#14253,#14254,#14255,#14256,#14257,#14258,#14259,#14260,#14261,
#14262,#14263,#14264,#14265,#14266,#14267,#14268,#14269,#14270,#14271,#14272,
#14273,#14274,#14275,#14276,#14277,#14278,#14279,#14280),.UNSPECIFIED.,
 .F.,.F.,(4,3,3,3,3,3,3,3,3,3,3,3,3,3,3,3,3,3,3,3,3,3,3,3,3,3,3,3,3,3,3,
3,3,3,3,3,3,3,3,3,3,3,3,3,3,3,3,3,3,3,3,3,3,3,3,3,3,3,3,3,3,3,3,3,3,3,3,
3,3,3,3,3,3,3,3,3,3,3,3,3,3,3,3,3,3,3,3,3,3,3,3,3,3,3,3,3,3,3,3,3,3,3,3,
3,3,3,3,3,3,3,3,3,3,3,4),(-10.3760794513229,-10.3264153263384,-10.2925120173749,
-10.2601968567228,-10.1998923966073,-10.1363908395232,-10.1076860162616,
-10.0193432467952,-9.93091491142239,-9.85194692512929,-9.84233871959151,
-9.83109753959046,-9.83106687522445,-9.75287310045053,-9.74493984606962,
-9.65891785327206,-9.57297937914544,-9.50762889976171,-9.48710298111784,
-9.41517189571804,-9.40125874556535,-9.28719446135969,-9.22959308987034,
-9.14373301477612,-9.05778170156634,-8.97177834463815,-8.89233113759898,
-8.88565188756136,-8.84799090459512,-8.84796018770201,-8.76977990021687,
-8.76184887755315,-8.67584262021201,-8.58991987947197,-8.52465246550391,
-8.50405919433414,-8.43207207388185,-8.41823058404444,-8.30417088660895,
-8.24659598478001,-8.16537366735408,-8.16075130772062,-8.07481517058394,
-7.98882688343906,-7.90938128579593,-7.90271520305529,-7.86488422895974,
-7.86485350017956,-7.78667353382456,-7.77872495169094,-7.69270153910995,
-7.60676174503123,-7.54168886120423,-7.52088412724879,-7.44867448273856,
-7.4350388238479,-7.32094923965079,-7.26337131704426,-7.18787402876446,
-7.17751045990625,-7.09155851220294,-7.00555460422482,-6.92608545369845,
-6.91942772756424,-6.88177729574692,-6.88174681265712,-6.80350986483478,
-6.79559175471683,-6.70954157508135,-6.62357479127157,-6.55770110774451,
-6.53766999564482,-6.46618696034968,-6.45179733750838,-6.33775687888313,
-6.2800748480303,-6.19418642384597,-6.10820699948371,-6.02217562967714,
-5.94275307736442,-5.936021553422,-5.89867111508928,-5.89864012513467,-5.82053057812116,
-5.8126166075868,-5.72669820066755,-5.64086326704925,-5.57596685375035,
-5.55509024515823,-5.48287344868061,-5.46934876919013,-5.35532269157411,
-5.2978872897214,-5.22328485573253,-5.21212841716633,-5.12627681995917,
-5.04037246723583,-4.96094257333632,-4.95434306467912,-4.91556430437963,
-4.91553343761223,-4.83814842128407,-4.83052634717772,-4.74562463000397,
-4.66081596132364,-4.59544057673657,-4.57605895127486,-4.50694700115561,
-4.49133320716937,-4.37135018659226,-4.32185837814588,-4.26407962449433,
-4.23707535482957,-4.15219887483577,-4.09289414427507),.UNSPECIFIED.);
#1422=B_SPLINE_CURVE_WITH_KNOTS('',3,(#14307,#14308,#14309,#14310,#14311,
#14312,#14313,#14314,#14315,#14316,#14317,#14318,#14319,#14320,#14321,#14322,
#14323,#14324,#14325,#14326,#14327,#14328,#14329,#14330,#14331,#14332,#14333,
#14334,#14335,#14336,#14337,#14338,#14339,#14340,#14341,#14342,#14343,#14344,
#14345,#14346,#14347,#14348,#14349,#14350,#14351,#14352,#14353,#14354,#14355,
#14356,#14357,#14358,#14359,#14360,#14361,#14362,#14363,#14364,#14365,#14366,
#14367,#14368,#14369,#14370,#14371,#14372,#14373,#14374,#14375,#14376,#14377,
#14378,#14379,#14380,#14381,#14382,#14383,#14384,#14385,#14386,#14387,#14388,
#14389,#14390,#14391,#14392,#14393,#14394),.UNSPECIFIED.,.F.,.F.,(4,3,3,
3,3,3,3,3,3,3,3,3,3,3,3,3,3,3,3,3,3,3,3,3,3,3,3,3,3,4),(2.05878368674717E-14,
0.0234054472019564,0.0471352136142213,0.0707669153608998,0.0840367480408261,
0.0878713467795278,0.110975706690514,0.133712282260844,0.150709160734639,
0.158060268187143,0.163470733062873,0.167953178850733,0.189907599318317,
0.201793217244577,0.224252520140966,0.234752288110081,0.240507487537732,
0.24411168274315,0.265884710195976,0.287663355668543,0.308957241466627,
0.317294467212432,0.321188873214287,0.341934990903991,0.362478952452641,
0.367608141617428,0.372096895882347,0.385217611626515,0.405963257765431,
0.415993328865176),.UNSPECIFIED.);
#1423=B_SPLINE_CURVE_WITH_KNOTS('',3,(#14396,#14397,#14398,#14399),
 .UNSPECIFIED.,.F.,.F.,(4,4),(-2.84914982550175,-2.06894047480313),
 .UNSPECIFIED.);
#1424=B_SPLINE_CURVE_WITH_KNOTS('',3,(#14401,#14402,#14403,#14404,#14405,
#14406,#14407,#14408,#14409,#14410,#14411,#14412,#14413,#14414,#14415,#14416,
#14417,#14418,#14419,#14420,#14421,#14422,#14423,#14424,#14425,#14426,#14427,
#14428,#14429,#14430,#14431,#14432,#14433,#14434,#14435,#14436,#14437,#14438,
#14439,#14440,#14441,#14442,#14443,#14444,#14445,#14446,#14447,#14448,#14449,
#14450,#14451,#14452,#14453,#14454,#14455,#14456,#14457,#14458,#14459,#14460,
#14461,#14462,#14463,#14464,#14465,#14466,#14467,#14468,#14469,#14470,#14471,
#14472,#14473,#14474,#14475,#14476,#14477,#14478,#14479,#14480,#14481,#14482,
#14483,#14484,#14485,#14486,#14487,#14488),.UNSPECIFIED.,.F.,.F.,(4,3,3,
3,3,3,3,3,3,3,3,3,3,3,3,3,3,3,3,3,3,3,3,3,3,3,3,3,3,4),(-0.413490722097494,
-0.390374461965417,-0.376956788739721,-0.364612854506389,-0.357223081629536,
-0.353167632297454,-0.329816475302324,-0.3110173587975,-0.300922997939596,
-0.297410089408388,-0.274622870919242,-0.252197899216542,-0.232987043189295,
-0.22435563742345,-0.220563464855743,-0.216970640358496,-0.195389510666055,
-0.179453841006409,-0.15736082632792,-0.146597972574468,-0.141428288189789,
-0.120027659580677,-0.0986007772958362,-0.077592352147286,-0.0725581786302476,
-0.0680299217253234,-0.0474235785525696,-0.0274062962751784,-0.00761976281229705,
0.),.UNSPECIFIED.);
#1425=B_SPLINE_CURVE_WITH_KNOTS('',3,(#14490,#14491,#14492,#14493,#14494,
#14495,#14496,#14497),.UNSPECIFIED.,.F.,.F.,(4,2,2,4),(-0.139393279070508,
-0.0696441449762668,-0.0347017080904481,-0.000337482562019728),
 .UNSPECIFIED.);
#1426=B_SPLINE_CURVE_WITH_KNOTS('',3,(#14498,#14499,#14500,#14501),
 .UNSPECIFIED.,.F.,.F.,(4,4),(-0.00186151085722638,0.),.UNSPECIFIED.);
#1427=B_SPLINE_CURVE_WITH_KNOTS('',3,(#14506,#14507,#14508,#14509,#14510,
#14511,#14512,#14513),.UNSPECIFIED.,.F.,.F.,(4,2,2,4),(0.000337254956516375,
0.0347017162006212,0.0696441548061046,0.139393290074209),.UNSPECIFIED.);
#1428=B_SPLINE_CURVE_WITH_KNOTS('',3,(#14540,#14541,#14542,#14543,#14544,
#14545,#14546,#14547,#14548,#14549,#14550,#14551,#14552,#14553,#14554,#14555,
#14556,#14557,#14558,#14559,#14560,#14561,#14562,#14563,#14564,#14565,#14566,
#14567,#14568,#14569,#14570,#14571,#14572,#14573,#14574,#14575,#14576,#14577,
#14578,#14579,#14580,#14581,#14582,#14583,#14584,#14585,#14586,#14587,#14588,
#14589,#14590,#14591,#14592,#14593,#14594,#14595,#14596,#14597,#14598,#14599,
#14600,#14601,#14602,#14603,#14604,#14605,#14606,#14607,#14608,#14609,#14610,
#14611,#14612,#14613,#14614,#14615,#14616,#14617,#14618,#14619,#14620,#14621,
#14622,#14623,#14624,#14625,#14626,#14627),.UNSPECIFIED.,.F.,.F.,(4,3,3,
3,3,3,3,3,3,3,3,3,3,3,3,3,3,3,3,3,3,3,3,3,3,3,3,3,3,4),(9.94883000103285E-15,
0.0196166916569847,0.0399302769784652,0.0573080150775109,0.0651965825194071,
0.0692472851263457,0.0727586240116996,0.0938497532114967,0.115302615032433,
0.136627386511764,0.139448576973331,0.143452860461702,0.147424687779491,
0.169517815215389,0.179453841006421,0.2010748625388,0.220290031668888,0.22390552179017,
0.245971799153012,0.26870301781468,0.291434236476348,0.297317452472671,
0.303372200521482,0.326746258433795,0.349433290040221,0.355210854434181,
0.360866724042728,0.37695678873974,0.400080606860445,0.414094136780462),
 .UNSPECIFIED.);
#1429=B_SPLINE_CURVE_WITH_KNOTS('',3,(#14629,#14630,#14631,#14632),
 .UNSPECIFIED.,.F.,.F.,(4,4),(0.,0.00186027720717915),.UNSPECIFIED.);
#1430=B_SPLINE_CURVE_WITH_KNOTS('',3,(#14634,#14635,#14636,#14637,#14638,
#14639,#14640,#14641,#14642,#14643,#14644,#14645,#14646,#14647,#14648,#14649,
#14650,#14651,#14652,#14653,#14654,#14655,#14656,#14657,#14658,#14659,#14660,
#14661,#14662,#14663,#14664,#14665,#14666,#14667,#14668,#14669,#14670,#14671,
#14672,#14673,#14674,#14675,#14676,#14677,#14678,#14679,#14680,#14681,#14682,
#14683,#14684,#14685,#14686,#14687,#14688,#14689,#14690,#14691,#14692,#14693,
#14694,#14695,#14696,#14697,#14698,#14699,#14700,#14701,#14702,#14703,#14704,
#14705,#14706,#14707,#14708,#14709,#14710,#14711,#14712,#14713,#14714,#14715),
 .UNSPECIFIED.,.F.,.F.,(4,3,3,3,3,3,3,3,3,3,3,3,3,3,3,3,3,3,3,3,3,3,3,3,
3,3,3,4),(-0.415993328865187,-0.395247681143785,-0.385217611626505,-0.368797025934534,
-0.36502116844561,-0.344384137832406,-0.326531494809057,-0.320844694700121,
-0.315794800692042,-0.294447216736322,-0.272640318795181,-0.255006113686598,
-0.246851849353904,-0.243114662305886,-0.220650412226071,-0.201793217244566,
-0.179843818695368,-0.168406146924892,-0.164760369659269,-0.142479944943098,
-0.119441369865257,-0.0964027947874157,-0.086570173338417,-0.0816436307916124,
-0.0579861482246397,-0.0343081270343868,-0.0108824362787603,0.),
 .UNSPECIFIED.);
#1431=B_SPLINE_CURVE_WITH_KNOTS('',3,(#14716,#14717,#14718,#14719),
 .UNSPECIFIED.,.F.,.F.,(4,4),(0.,0.780209350698613),.UNSPECIFIED.);
#1432=B_SPLINE_CURVE_WITH_KNOTS('',3,(#14921,#14922,#14923,#14924,#14925,
#14926,#14927,#14928,#14929,#14930,#14931,#14932,#14933,#14934,#14935,#14936,
#14937,#14938,#14939,#14940,#14941,#14942,#14943,#14944,#14945,#14946,#14947,
#14948,#14949,#14950,#14951,#14952,#14953,#14954,#14955,#14956,#14957,#14958,
#14959,#14960,#14961,#14962,#14963,#14964,#14965,#14966,#14967,#14968,#14969,
#14970,#14971,#14972,#14973,#14974,#14975,#14976,#14977,#14978,#14979,#14980,
#14981,#14982,#14983,#14984,#14985,#14986,#14987,#14988,#14989,#14990,#14991,
#14992,#14993,#14994,#14995,#14996,#14997,#14998,#14999,#15000,#15001,#15002,
#15003,#15004,#15005,#15006,#15007,#15008,#15009,#15010,#15011,#15012,#15013,
#15014,#15015,#15016,#15017,#15018,#15019,#15020,#15021,#15022,#15023,#15024,
#15025,#15026),.UNSPECIFIED.,.F.,.F.,(4,3,3,3,3,3,3,3,3,3,3,3,3,3,3,3,3,
3,3,3,3,3,3,3,3,3,3,3,3,3,3,3,3,3,3,4),(5.51919316556669E-5,0.0396105854411369,
0.0421684740053724,0.0820591227434645,0.123381779682084,0.164704436620703,
0.170094771591715,0.175319647983374,0.214784946467128,0.25429154179183,
0.293151938457061,0.325136464664712,0.334844260977463,0.340168266397053,
0.37840317841123,0.416167211420586,0.452998512977425,0.46134294969662,0.485996360447615,
0.493345060083779,0.499697573685857,0.536831195961491,0.574162340000071,
0.61108256799235,0.632520778240444,0.644430130512825,0.650618647569442,
0.655220962152611,0.658570235704578,0.695166161482855,0.731571524858071,
0.744958227452224,0.754067922795179,0.789881274989443,0.825088562680887,
0.847325527525853),.UNSPECIFIED.);
#1433=B_SPLINE_CURVE_WITH_KNOTS('',3,(#15028,#15029,#15030,#15031,#15032,
#15033,#15034,#15035,#15036,#15037,#15038,#15039,#15040,#15041,#15042,#15043,
#15044,#15045,#15046,#15047,#15048,#15049,#15050,#15051,#15052,#15053,#15054,
#15055,#15056,#15057,#15058,#15059,#15060,#15061,#15062,#15063,#15064,#15065,
#15066,#15067,#15068,#15069,#15070,#15071,#15072,#15073,#15074,#15075,#15076,
#15077,#15078,#15079,#15080,#15081,#15082,#15083,#15084,#15085,#15086,#15087,
#15088,#15089,#15090,#15091,#15092,#15093,#15094,#15095,#15096,#15097,#15098,
#15099,#15100,#15101,#15102,#15103,#15104,#15105,#15106,#15107,#15108,#15109,
#15110,#15111,#15112,#15113,#15114,#15115,#15116,#15117,#15118,#15119,#15120,
#15121,#15122,#15123,#15124),.UNSPECIFIED.,.F.,.F.,(4,3,3,3,3,3,3,3,3,3,
3,3,3,3,3,3,3,3,3,3,3,3,3,3,3,3,3,3,3,3,3,3,4),(-0.847325527525843,-0.811503753623457,
-0.776673059854492,-0.75974088209237,-0.750234800273659,-0.742631895672967,
-0.706740314620834,-0.670224472629315,-0.65436706634716,-0.6449569526527,
-0.607798067978851,-0.570230375047688,-0.532703103593353,-0.505758215660538,
-0.497488333365585,-0.491961441323387,-0.453421092889369,-0.422238544386844,
-0.384505330263272,-0.346772116139701,-0.33539303508032,-0.33016070262821,
-0.291919157074523,-0.252839602008931,-0.215142387780448,-0.175907489429898,
-0.170455452500928,-0.156701908810693,-0.116751637160037,-0.0766037057486563,
-0.0367647523419657,-0.00225557790275668,-1.20338083946995E-14),
 .UNSPECIFIED.);
#1434=B_SPLINE_CURVE_WITH_KNOTS('',3,(#15125,#15126,#15127,#15128),
 .UNSPECIFIED.,.F.,.F.,(4,4),(-0.00895779246149321,0.),.UNSPECIFIED.);
#1435=B_SPLINE_CURVE_WITH_KNOTS('',3,(#15322,#15323,#15324,#15325,#15326,
#15327,#15328,#15329,#15330,#15331,#15332,#15333,#15334,#15335,#15336,#15337,
#15338,#15339,#15340,#15341,#15342,#15343,#15344,#15345,#15346,#15347,#15348,
#15349,#15350,#15351,#15352,#15353,#15354,#15355,#15356,#15357,#15358,#15359,
#15360,#15361,#15362,#15363,#15364,#15365,#15366,#15367,#15368,#15369,#15370,
#15371,#15372,#15373,#15374,#15375,#15376,#15377,#15378,#15379,#15380,#15381,
#15382,#15383,#15384,#15385,#15386,#15387,#15388,#15389,#15390,#15391,#15392,
#15393,#15394,#15395,#15396,#15397,#15398,#15399,#15400,#15401,#15402,#15403,
#15404,#15405,#15406,#15407,#15408,#15409,#15410,#15411,#15412,#15413,#15414,
#15415,#15416,#15417,#15418),.UNSPECIFIED.,.F.,.F.,(4,3,3,3,3,3,3,3,3,3,
3,3,3,3,3,3,3,3,3,3,3,3,3,3,3,3,3,3,3,3,3,3,4),(0.,0.0357326537857237,0.0704068465260574,
0.106060821374739,0.14171479622342,0.147192652306303,0.152214352689264,
0.188520307438454,0.225451162932226,0.262649253600598,0.282094339758411,
0.294929882792059,0.30572005862029,0.343770262441978,0.381690975206976,
0.418209942863103,0.423963173602016,0.455960576699411,0.461085295912164,
0.499207673622447,0.537393570095102,0.576100145693367,0.613574806753294,
0.619086816026134,0.624483039944413,0.630147733446615,0.669254131242952,
0.708784888661744,0.727582209613668,0.735557703752757,0.775673392218803,
0.815702463241756,0.84421229055669),.UNSPECIFIED.);
#1436=B_SPLINE_CURVE_WITH_KNOTS('',3,(#15419,#15420,#15421,#15422),
 .UNSPECIFIED.,.F.,.F.,(4,4),(0.,0.00895786573059968),.UNSPECIFIED.);
#1437=B_SPLINE_CURVE_WITH_KNOTS('',3,(#15423,#15424,#15425,#15426,#15427,
#15428,#15429,#15430,#15431,#15432,#15433,#15434,#15435,#15436,#15437,#15438,
#15439,#15440,#15441,#15442,#15443,#15444,#15445,#15446,#15447,#15448,#15449,
#15450,#15451,#15452,#15453,#15454,#15455,#15456,#15457,#15458,#15459,#15460,
#15461,#15462,#15463,#15464,#15465,#15466,#15467,#15468,#15469,#15470,#15471,
#15472,#15473,#15474,#15475,#15476,#15477,#15478,#15479,#15480,#15481,#15482,
#15483,#15484,#15485,#15486,#15487,#15488,#15489,#15490,#15491,#15492,#15493,
#15494,#15495,#15496,#15497,#15498,#15499,#15500,#15501,#15502,#15503,#15504,
#15505,#15506,#15507,#15508,#15509,#15510,#15511,#15512,#15513,#15514,#15515,
#15516,#15517,#15518,#15519),.UNSPECIFIED.,.F.,.F.,(4,3,3,3,3,3,3,3,3,3,
3,3,3,3,3,3,3,3,3,3,3,3,3,3,3,3,3,3,3,3,3,3,4),(-0.844212290556731,-0.804914039435832,
-0.802217933301225,-0.761940655968895,-0.731371284183562,-0.724667747997382,
-0.685031612040754,-0.645191108298448,-0.631145243959577,-0.622466655133243,
-0.614790169492861,-0.575736023750926,-0.536900490369521,-0.498311999539644,
-0.459723508709767,-0.457469136431715,-0.452285602603943,-0.414914580184266,
-0.385002433230672,-0.347245920152347,-0.309123322414732,-0.301425288615579,
-0.29421526181017,-0.257399270414763,-0.220741128783992,-0.188385367654945,
-0.153950864306229,-0.147824231453246,-0.142510002622108,-0.106551008291469,
-0.0707579690466674,-0.0353789845233405,-1.35445026026053E-14),
 .UNSPECIFIED.);
#1697=VERTEX_POINT('',#7643);
#1698=VERTEX_POINT('',#7644);
#1699=VERTEX_POINT('',#7646);
#1700=VERTEX_POINT('',#7834);
#1701=VERTEX_POINT('',#7973);
#1702=VERTEX_POINT('',#7974);
#1703=VERTEX_POINT('',#8317);
#1704=VERTEX_POINT('',#8318);
#1705=VERTEX_POINT('',#8651);
#1706=VERTEX_POINT('',#8652);
#1707=VERTEX_POINT('',#8981);
#1708=VERTEX_POINT('',#8982);
#1709=VERTEX_POINT('',#9317);
#1710=VERTEX_POINT('',#9318);
#1711=VERTEX_POINT('',#9657);
#1712=VERTEX_POINT('',#9684);
#1713=VERTEX_POINT('',#9872);
#1714=VERTEX_POINT('',#9874);
#1715=VERTEX_POINT('',#10042);
#1716=VERTEX_POINT('',#10043);
#1717=VERTEX_POINT('',#10162);
#1718=VERTEX_POINT('',#10164);
#1719=VERTEX_POINT('',#10191);
#1720=VERTEX_POINT('',#10520);
#1721=VERTEX_POINT('',#10861);
#1722=VERTEX_POINT('',#11208);
#1723=VERTEX_POINT('',#11438);
#1724=VERTEX_POINT('',#11782);
#1725=VERTEX_POINT('',#12126);
#1726=VERTEX_POINT('',#12206);
#1727=VERTEX_POINT('',#12208);
#1728=VERTEX_POINT('',#12221);
#1729=VERTEX_POINT('',#12553);
#1730=VERTEX_POINT('',#12900);
#1731=VERTEX_POINT('',#13244);
#1732=VERTEX_POINT('',#13597);
#1733=VERTEX_POINT('',#14305);
#1734=VERTEX_POINT('',#14306);
#1735=VERTEX_POINT('',#14395);
#1736=VERTEX_POINT('',#14400);
#1737=VERTEX_POINT('',#14489);
#1738=VERTEX_POINT('',#14503);
#1739=VERTEX_POINT('',#14505);
#1740=VERTEX_POINT('',#14539);
#1741=VERTEX_POINT('',#14628);
#1742=VERTEX_POINT('',#14633);
#1743=VERTEX_POINT('',#14721);
#1744=VERTEX_POINT('',#14725);
#1745=VERTEX_POINT('',#15027);
#1746=VERTEX_POINT('',#15321);
#1747=VERTEX_POINT('',#15521);
#1748=VERTEX_POINT('',#15523);
#2163=EDGE_CURVE('',#1697,#1698,#1024,.T.);
#2164=EDGE_CURVE('',#1699,#1697,#1390,.T.);
#2165=EDGE_CURVE('',#1700,#1699,#248,.T.);
#2166=EDGE_CURVE('',#1700,#1698,#1391,.T.);
#2167=EDGE_CURVE('',#1701,#1702,#1025,.T.);
#2168=EDGE_CURVE('',#1697,#1701,#1392,.F.);
#2169=EDGE_CURVE('',#1698,#1702,#1393,.T.);
#2170=EDGE_CURVE('',#1703,#1704,#1026,.T.);
#2171=EDGE_CURVE('',#1701,#1703,#1394,.F.);
#2172=EDGE_CURVE('',#1702,#1704,#1395,.T.);
#2173=EDGE_CURVE('',#1705,#1706,#1027,.T.);
#2174=EDGE_CURVE('',#1703,#1705,#1396,.F.);
#2175=EDGE_CURVE('',#1704,#1706,#1397,.T.);
#2176=EDGE_CURVE('',#1707,#1708,#1028,.T.);
#2177=EDGE_CURVE('',#1705,#1707,#1398,.F.);
#2178=EDGE_CURVE('',#1706,#1708,#1399,.T.);
#2179=EDGE_CURVE('',#1709,#1710,#1029,.T.);
#2180=EDGE_CURVE('',#1707,#1709,#1400,.F.);
#2181=EDGE_CURVE('',#1708,#1710,#1401,.T.);
#2182=EDGE_CURVE('',#1710,#1711,#1402,.T.);
#2183=EDGE_CURVE('',#1711,#1712,#1403,.T.);
#2184=EDGE_CURVE('',#1713,#1712,#249,.T.);
#2185=EDGE_CURVE('',#1714,#1713,#1404,.T.);
#2186=EDGE_CURVE('',#1709,#1714,#1405,.F.);
#2187=EDGE_CURVE('',#1715,#1716,#1406,.T.);
#2188=EDGE_CURVE('',#1716,#1717,#250,.F.);
#2189=EDGE_CURVE('',#1717,#1718,#1407,.T.);
#2190=EDGE_CURVE('',#1718,#1719,#1408,.T.);
#2191=EDGE_CURVE('',#1719,#1720,#1409,.T.);
#2192=EDGE_CURVE('',#1720,#1721,#1410,.T.);
#2193=EDGE_CURVE('',#1721,#1722,#1411,.T.);
#2194=EDGE_CURVE('',#1722,#1723,#1412,.T.);
#2195=EDGE_CURVE('',#1723,#1724,#1413,.T.);
#2196=EDGE_CURVE('',#1724,#1725,#1414,.T.);
#2197=EDGE_CURVE('',#1726,#1725,#251,.F.);
#2198=EDGE_CURVE('',#1726,#1727,#1415,.T.);
#2199=EDGE_CURVE('',#1727,#1728,#1416,.T.);
#2200=EDGE_CURVE('',#1728,#1729,#1417,.T.);
#2201=EDGE_CURVE('',#1729,#1730,#1418,.T.);
#2202=EDGE_CURVE('',#1730,#1731,#1419,.T.);
#2203=EDGE_CURVE('',#1731,#1732,#1420,.T.);
#2204=EDGE_CURVE('',#1732,#1715,#1421,.T.);
#2205=EDGE_CURVE('',#1733,#1734,#1422,.T.);
#2206=EDGE_CURVE('',#1733,#1735,#1423,.T.);
#2207=EDGE_CURVE('',#1735,#1736,#1424,.T.);
#2208=EDGE_CURVE('',#1736,#1737,#1425,.T.);
#2209=EDGE_CURVE('',#1734,#1737,#1426,.T.);
#2210=EDGE_CURVE('',#1736,#1738,#252,.T.);
#2211=EDGE_CURVE('',#1738,#1739,#1427,.T.);
#2212=EDGE_CURVE('',#1737,#1739,#253,.T.);
#2213=EDGE_CURVE('',#1739,#1740,#1428,.T.);
#2214=EDGE_CURVE('',#1738,#1741,#1429,.T.);
#2215=EDGE_CURVE('',#1741,#1742,#1430,.T.);
#2216=EDGE_CURVE('',#1742,#1740,#1431,.T.);
#2217=EDGE_CURVE('',#1735,#1743,#254,.T.);
#2218=EDGE_CURVE('',#1743,#1742,#255,.T.);
#2219=EDGE_CURVE('',#1744,#1744,#256,.T.);
#2220=EDGE_CURVE('',#1744,#1743,#1030,.T.);
#2221=EDGE_CURVE('',#1740,#1733,#257,.T.);
#2222=EDGE_CURVE('',#1725,#1713,#1432,.T.);
#2223=EDGE_CURVE('',#1745,#1717,#1433,.T.);
#2224=EDGE_CURVE('',#1745,#1699,#1434,.T.);
#2225=EDGE_CURVE('',#1746,#1726,#1435,.T.);
#2226=EDGE_CURVE('',#1712,#1746,#1436,.T.);
#2227=EDGE_CURVE('',#1716,#1700,#1437,.T.);
#2228=EDGE_CURVE('',#1747,#1747,#258,.T.);
#2229=EDGE_CURVE('',#1747,#1748,#1031,.T.);
#2230=EDGE_CURVE('',#1748,#1748,#259,.T.);
#2987=ORIENTED_EDGE('',*,*,#2163,.F.);
#2988=ORIENTED_EDGE('',*,*,#2164,.F.);
#2989=ORIENTED_EDGE('',*,*,#2165,.F.);
#2990=ORIENTED_EDGE('',*,*,#2166,.T.);
#2991=ORIENTED_EDGE('',*,*,#2167,.F.);
#2992=ORIENTED_EDGE('',*,*,#2168,.F.);
#2993=ORIENTED_EDGE('',*,*,#2163,.T.);
#2994=ORIENTED_EDGE('',*,*,#2169,.T.);
#2995=ORIENTED_EDGE('',*,*,#2170,.F.);
#2996=ORIENTED_EDGE('',*,*,#2171,.F.);
#2997=ORIENTED_EDGE('',*,*,#2167,.T.);
#2998=ORIENTED_EDGE('',*,*,#2172,.T.);
#2999=ORIENTED_EDGE('',*,*,#2173,.F.);
#3000=ORIENTED_EDGE('',*,*,#2174,.F.);
#3001=ORIENTED_EDGE('',*,*,#2170,.T.);
#3002=ORIENTED_EDGE('',*,*,#2175,.T.);
#3003=ORIENTED_EDGE('',*,*,#2176,.F.);
#3004=ORIENTED_EDGE('',*,*,#2177,.F.);
#3005=ORIENTED_EDGE('',*,*,#2173,.T.);
#3006=ORIENTED_EDGE('',*,*,#2178,.T.);
#3007=ORIENTED_EDGE('',*,*,#2179,.F.);
#3008=ORIENTED_EDGE('',*,*,#2180,.F.);
#3009=ORIENTED_EDGE('',*,*,#2176,.T.);
#3010=ORIENTED_EDGE('',*,*,#2181,.T.);
#3011=ORIENTED_EDGE('',*,*,#2179,.T.);
#3012=ORIENTED_EDGE('',*,*,#2182,.T.);
#3013=ORIENTED_EDGE('',*,*,#2183,.T.);
#3014=ORIENTED_EDGE('',*,*,#2184,.F.);
#3015=ORIENTED_EDGE('',*,*,#2185,.F.);
#3016=ORIENTED_EDGE('',*,*,#2186,.F.);
#3017=ORIENTED_EDGE('',*,*,#2187,.T.);
#3018=ORIENTED_EDGE('',*,*,#2188,.T.);
#3019=ORIENTED_EDGE('',*,*,#2189,.T.);
#3020=ORIENTED_EDGE('',*,*,#2190,.T.);
#3021=ORIENTED_EDGE('',*,*,#2191,.T.);
#3022=ORIENTED_EDGE('',*,*,#2192,.T.);
#3023=ORIENTED_EDGE('',*,*,#2193,.T.);
#3024=ORIENTED_EDGE('',*,*,#2194,.T.);
#3025=ORIENTED_EDGE('',*,*,#2195,.T.);
#3026=ORIENTED_EDGE('',*,*,#2196,.T.);
#3027=ORIENTED_EDGE('',*,*,#2197,.F.);
#3028=ORIENTED_EDGE('',*,*,#2198,.T.);
#3029=ORIENTED_EDGE('',*,*,#2199,.T.);
#3030=ORIENTED_EDGE('',*,*,#2200,.T.);
#3031=ORIENTED_EDGE('',*,*,#2201,.T.);
#3032=ORIENTED_EDGE('',*,*,#2202,.T.);
#3033=ORIENTED_EDGE('',*,*,#2203,.T.);
#3034=ORIENTED_EDGE('',*,*,#2204,.T.);
#3035=ORIENTED_EDGE('',*,*,#2205,.F.);
#3036=ORIENTED_EDGE('',*,*,#2206,.T.);
#3037=ORIENTED_EDGE('',*,*,#2207,.T.);
#3038=ORIENTED_EDGE('',*,*,#2208,.T.);
#3039=ORIENTED_EDGE('',*,*,#2209,.F.);
#3040=ORIENTED_EDGE('',*,*,#2210,.T.);
#3041=ORIENTED_EDGE('',*,*,#2211,.T.);
#3042=ORIENTED_EDGE('',*,*,#2212,.F.);
#3043=ORIENTED_EDGE('',*,*,#2208,.F.);
#3044=ORIENTED_EDGE('',*,*,#2213,.F.);
#3045=ORIENTED_EDGE('',*,*,#2211,.F.);
#3046=ORIENTED_EDGE('',*,*,#2214,.T.);
#3047=ORIENTED_EDGE('',*,*,#2215,.T.);
#3048=ORIENTED_EDGE('',*,*,#2216,.T.);
#3049=ORIENTED_EDGE('',*,*,#2217,.T.);
#3050=ORIENTED_EDGE('',*,*,#2218,.T.);
#3051=ORIENTED_EDGE('',*,*,#2215,.F.);
#3052=ORIENTED_EDGE('',*,*,#2214,.F.);
#3053=ORIENTED_EDGE('',*,*,#2210,.F.);
#3054=ORIENTED_EDGE('',*,*,#2207,.F.);
#3055=ORIENTED_EDGE('',*,*,#2219,.F.);
#3056=ORIENTED_EDGE('',*,*,#2220,.T.);
#3057=ORIENTED_EDGE('',*,*,#2217,.F.);
#3058=ORIENTED_EDGE('',*,*,#2206,.F.);
#3059=ORIENTED_EDGE('',*,*,#2221,.F.);
#3060=ORIENTED_EDGE('',*,*,#2216,.F.);
#3061=ORIENTED_EDGE('',*,*,#2218,.F.);
#3062=ORIENTED_EDGE('',*,*,#2220,.F.);
#3063=ORIENTED_EDGE('',*,*,#2222,.F.);
#3064=ORIENTED_EDGE('',*,*,#2196,.F.);
#3065=ORIENTED_EDGE('',*,*,#2195,.F.);
#3066=ORIENTED_EDGE('',*,*,#2194,.F.);
#3067=ORIENTED_EDGE('',*,*,#2193,.F.);
#3068=ORIENTED_EDGE('',*,*,#2192,.F.);
#3069=ORIENTED_EDGE('',*,*,#2191,.F.);
#3070=ORIENTED_EDGE('',*,*,#2190,.F.);
#3071=ORIENTED_EDGE('',*,*,#2189,.F.);
#3072=ORIENTED_EDGE('',*,*,#2223,.F.);
#3073=ORIENTED_EDGE('',*,*,#2224,.T.);
#3074=ORIENTED_EDGE('',*,*,#2164,.T.);
#3075=ORIENTED_EDGE('',*,*,#2168,.T.);
#3076=ORIENTED_EDGE('',*,*,#2171,.T.);
#3077=ORIENTED_EDGE('',*,*,#2174,.T.);
#3078=ORIENTED_EDGE('',*,*,#2177,.T.);
#3079=ORIENTED_EDGE('',*,*,#2180,.T.);
#3080=ORIENTED_EDGE('',*,*,#2186,.T.);
#3081=ORIENTED_EDGE('',*,*,#2185,.T.);
#3082=ORIENTED_EDGE('',*,*,#2225,.F.);
#3083=ORIENTED_EDGE('',*,*,#2226,.F.);
#3084=ORIENTED_EDGE('',*,*,#2183,.F.);
#3085=ORIENTED_EDGE('',*,*,#2182,.F.);
#3086=ORIENTED_EDGE('',*,*,#2181,.F.);
#3087=ORIENTED_EDGE('',*,*,#2178,.F.);
#3088=ORIENTED_EDGE('',*,*,#2175,.F.);
#3089=ORIENTED_EDGE('',*,*,#2172,.F.);
#3090=ORIENTED_EDGE('',*,*,#2169,.F.);
#3091=ORIENTED_EDGE('',*,*,#2166,.F.);
#3092=ORIENTED_EDGE('',*,*,#2227,.F.);
#3093=ORIENTED_EDGE('',*,*,#2187,.F.);
#3094=ORIENTED_EDGE('',*,*,#2204,.F.);
#3095=ORIENTED_EDGE('',*,*,#2203,.F.);
#3096=ORIENTED_EDGE('',*,*,#2202,.F.);
#3097=ORIENTED_EDGE('',*,*,#2201,.F.);
#3098=ORIENTED_EDGE('',*,*,#2200,.F.);
#3099=ORIENTED_EDGE('',*,*,#2199,.F.);
#3100=ORIENTED_EDGE('',*,*,#2198,.F.);
#3101=ORIENTED_EDGE('',*,*,#2228,.F.);
#3102=ORIENTED_EDGE('',*,*,#2229,.T.);
#3103=ORIENTED_EDGE('',*,*,#2230,.T.);
#3104=ORIENTED_EDGE('',*,*,#2229,.F.);
#3105=ORIENTED_EDGE('',*,*,#2228,.T.);
#3106=ORIENTED_EDGE('',*,*,#2227,.T.);
#3107=ORIENTED_EDGE('',*,*,#2165,.T.);
#3108=ORIENTED_EDGE('',*,*,#2224,.F.);
#3109=ORIENTED_EDGE('',*,*,#2223,.T.);
#3110=ORIENTED_EDGE('',*,*,#2188,.F.);
#3111=ORIENTED_EDGE('',*,*,#2225,.T.);
#3112=ORIENTED_EDGE('',*,*,#2197,.T.);
#3113=ORIENTED_EDGE('',*,*,#2222,.T.);
#3114=ORIENTED_EDGE('',*,*,#2184,.T.);
#3115=ORIENTED_EDGE('',*,*,#2226,.T.);
#3116=ORIENTED_EDGE('',*,*,#2213,.T.);
#3117=ORIENTED_EDGE('',*,*,#2221,.T.);
#3118=ORIENTED_EDGE('',*,*,#2205,.T.);
#3119=ORIENTED_EDGE('',*,*,#2209,.T.);
#3120=ORIENTED_EDGE('',*,*,#2212,.T.);
#3121=ORIENTED_EDGE('',*,*,#2230,.F.);
#3122=ORIENTED_EDGE('',*,*,#2219,.T.);
#3607=B_SPLINE_SURFACE_WITH_KNOTS('',3,3,((#14281,#14282,#14283,#14284,
#14285,#14286),(#14287,#14288,#14289,#14290,#14291,#14292),(#14293,#14294,
#14295,#14296,#14297,#14298),(#14299,#14300,#14301,#14302,#14303,#14304)),
 .UNSPECIFIED.,.F.,.F.,.F.,(4,4),(4,1,1,4),(0.,0.0494711118308268),(16.7019134878289,
17.6517088926312,18.6014255011318,19.5511421096324),.UNSPECIFIED.);
#3608=B_SPLINE_SURFACE_WITH_KNOTS('',3,3,((#14515,#14516,#14517,#14518,
#14519,#14520),(#14521,#14522,#14523,#14524,#14525,#14526),(#14527,#14528,
#14529,#14530,#14531,#14532),(#14533,#14534,#14535,#14536,#14537,#14538)),
 .UNSPECIFIED.,.F.,.F.,.F.,(4,4),(4,1,1,4),(-7.87913040489834E-5,0.0493923155291723),
(13.3942556087771,14.3439722172777,15.2936888257783,16.2434842255829),
 .UNSPECIFIED.);
#3609=B_SPLINE_SURFACE_WITH_KNOTS('',3,3,((#14729,#14730,#14731,#14732,
#14733,#14734,#14735,#14736,#14737,#14738,#14739,#14740,#14741,#14742,#14743,
#14744,#14745,#14746,#14747,#14748,#14749,#14750,#14751,#14752,#14753,#14754,
#14755,#14756,#14757,#14758,#14759,#14760,#14761,#14762,#14763,#14764,#14765,
#14766,#14767,#14768,#14769,#14770,#14771,#14772,#14773,#14774,#14775,#14776),
(#14777,#14778,#14779,#14780,#14781,#14782,#14783,#14784,#14785,#14786,
#14787,#14788,#14789,#14790,#14791,#14792,#14793,#14794,#14795,#14796,#14797,
#14798,#14799,#14800,#14801,#14802,#14803,#14804,#14805,#14806,#14807,#14808,
#14809,#14810,#14811,#14812,#14813,#14814,#14815,#14816,#14817,#14818,#14819,
#14820,#14821,#14822,#14823,#14824),(#14825,#14826,#14827,#14828,#14829,
#14830,#14831,#14832,#14833,#14834,#14835,#14836,#14837,#14838,#14839,#14840,
#14841,#14842,#14843,#14844,#14845,#14846,#14847,#14848,#14849,#14850,#14851,
#14852,#14853,#14854,#14855,#14856,#14857,#14858,#14859,#14860,#14861,#14862,
#14863,#14864,#14865,#14866,#14867,#14868,#14869,#14870,#14871,#14872),
(#14873,#14874,#14875,#14876,#14877,#14878,#14879,#14880,#14881,#14882,
#14883,#14884,#14885,#14886,#14887,#14888,#14889,#14890,#14891,#14892,#14893,
#14894,#14895,#14896,#14897,#14898,#14899,#14900,#14901,#14902,#14903,#14904,
#14905,#14906,#14907,#14908,#14909,#14910,#14911,#14912,#14913,#14914,#14915,
#14916,#14917,#14918,#14919,#14920)),.UNSPECIFIED.,.F.,.F.,.F.,(4,4),(4,
1,1,1,1,1,1,1,1,1,1,1,1,1,1,1,1,1,1,1,1,1,1,1,1,1,1,1,1,1,1,1,1,1,1,1,1,
1,1,1,1,1,1,1,1,4),(-0.000683464176930082,0.0827553131308724),(8.31487785380719,
8.80643119756841,9.29798454132964,10.2810912288521,11.2641979163745,12.247304603897,
13.2304112914194,14.2135179789419,15.1966246664643,16.1797313539867,17.1628380415092,
18.1459447290316,19.1290514165541,20.1121581040765,21.095264791599,22.0783714791214,
23.0614781666439,24.0445848541663,25.0276915416888,26.0107982292112,26.9939049167336,
27.9770116042561,28.9601182917785,29.943224979301,30.9263316668234,31.9094383543459,
32.8925450418683,33.8756517293908,34.8587584169132,35.8418651044356,36.8249717919581,
37.8080784794805,38.791185167003,39.7742918545254,40.7573985420479,41.7405052295703,
42.7236119170928,43.7067186046152,44.6898252921376,45.6729319796601,46.6560386671825,
47.639145354705,48.6222520422274,49.6053587297499,50.0969120735111,50.5891488814492),
 .UNSPECIFIED.);
#3610=B_SPLINE_SURFACE_WITH_KNOTS('',3,3,((#15129,#15130,#15131,#15132,
#15133,#15134,#15135,#15136,#15137,#15138,#15139,#15140,#15141,#15142,#15143,
#15144,#15145,#15146,#15147,#15148,#15149,#15150,#15151,#15152,#15153,#15154,
#15155,#15156,#15157,#15158,#15159,#15160,#15161,#15162,#15163,#15164,#15165,
#15166,#15167,#15168,#15169,#15170,#15171,#15172,#15173,#15174,#15175,#15176),
(#15177,#15178,#15179,#15180,#15181,#15182,#15183,#15184,#15185,#15186,
#15187,#15188,#15189,#15190,#15191,#15192,#15193,#15194,#15195,#15196,#15197,
#15198,#15199,#15200,#15201,#15202,#15203,#15204,#15205,#15206,#15207,#15208,
#15209,#15210,#15211,#15212,#15213,#15214,#15215,#15216,#15217,#15218,#15219,
#15220,#15221,#15222,#15223,#15224),(#15225,#15226,#15227,#15228,#15229,
#15230,#15231,#15232,#15233,#15234,#15235,#15236,#15237,#15238,#15239,#15240,
#15241,#15242,#15243,#15244,#15245,#15246,#15247,#15248,#15249,#15250,#15251,
#15252,#15253,#15254,#15255,#15256,#15257,#15258,#15259,#15260,#15261,#15262,
#15263,#15264,#15265,#15266,#15267,#15268,#15269,#15270,#15271,#15272),
(#15273,#15274,#15275,#15276,#15277,#15278,#15279,#15280,#15281,#15282,
#15283,#15284,#15285,#15286,#15287,#15288,#15289,#15290,#15291,#15292,#15293,
#15294,#15295,#15296,#15297,#15298,#15299,#15300,#15301,#15302,#15303,#15304,
#15305,#15306,#15307,#15308,#15309,#15310,#15311,#15312,#15313,#15314,#15315,
#15316,#15317,#15318,#15319,#15320)),.UNSPECIFIED.,.F.,.F.,.F.,(4,4),(4,
1,1,1,1,1,1,1,1,1,1,1,1,1,1,1,1,1,1,1,1,1,1,1,1,1,1,1,1,1,1,1,1,1,1,1,1,
1,1,1,1,1,1,1,1,4),(-0.000359643560771195,0.0826961570524529),(11.6143855724915,
12.1066224675668,12.598175811328,13.5812824988505,14.5643891863729,15.5474958738954,
16.5306025614178,17.5137092489403,18.4968159364627,19.4799226239851,20.4630293115076,
21.44613599903,22.4292426865525,23.4123493740749,24.3954560615974,25.3785627491198,
26.3616694366423,27.3447761241647,28.3278828116872,29.3109894992096,30.294096186732,
31.2772028742545,32.2603095617769,33.2434162492994,34.2265229368218,35.2096296243443,
36.1927363118667,37.1758429993892,38.1589496869116,39.142056374434,40.1251630619565,
41.1082697494789,42.0913764370014,43.0744831245238,44.0575898120463,45.0406964995687,
46.0238031870912,47.0069098746136,47.9900165621361,48.9731232496585,49.956229937181,
50.9393366247034,51.9224433122258,52.9055499997483,53.3971033435095,53.8886566872707),
 .UNSPECIFIED.);
#3715=ADVANCED_FACE('',(#540),#382,.T.);
#3716=ADVANCED_FACE('',(#541),#383,.T.);
#3717=ADVANCED_FACE('',(#542),#384,.T.);
#3718=ADVANCED_FACE('',(#543),#385,.T.);
#3719=ADVANCED_FACE('',(#544),#386,.T.);
#3720=ADVANCED_FACE('',(#545),#387,.T.);
#3721=ADVANCED_FACE('',(#546),#388,.T.);
#3722=ADVANCED_FACE('',(#547),#389,.T.);
#3723=ADVANCED_FACE('',(#548),#3607,.T.);
#3724=ADVANCED_FACE('',(#549),#390,.F.);
#3725=ADVANCED_FACE('',(#550),#3608,.T.);
#3726=ADVANCED_FACE('',(#551),#190,.F.);
#3727=ADVANCED_FACE('',(#552),#391,.F.);
#3728=ADVANCED_FACE('',(#553),#3609,.F.);
#3729=ADVANCED_FACE('',(#554),#3610,.F.);
#3730=ADVANCED_FACE('',(#555),#392,.T.);
#3731=ADVANCED_FACE('',(#556,#139),#191,.T.);
#3732=ADVANCED_FACE('',(#557,#140),#192,.T.);
#3733=ADVANCED_FACE('',(#558,#141),#193,.F.);
#3839=CLOSED_SHELL('',(#3715,#3716,#3717,#3718,#3719,#3720,#3721,#3722,
#3723,#3724,#3725,#3726,#3727,#3728,#3729,#3730,#3731,#3732,#3733));
#4064=AXIS2_PLACEMENT_3D('',#7641,#4615,#4616);
#4065=AXIS2_PLACEMENT_3D('',#7642,#4617,#4618);
#4066=AXIS2_PLACEMENT_3D('',#7835,#4620,#4621);
#4067=AXIS2_PLACEMENT_3D('',#7972,#4622,#4623);
#4068=AXIS2_PLACEMENT_3D('',#8316,#4625,#4626);
#4069=AXIS2_PLACEMENT_3D('',#8650,#4628,#4629);
#4070=AXIS2_PLACEMENT_3D('',#8980,#4631,#4632);
#4071=AXIS2_PLACEMENT_3D('',#9316,#4634,#4635);
#4072=AXIS2_PLACEMENT_3D('',#9656,#4637,#4638);
#4073=AXIS2_PLACEMENT_3D('',#9873,#4639,#4640);
#4074=AXIS2_PLACEMENT_3D('',#10041,#4641,#4642);
#4075=AXIS2_PLACEMENT_3D('',#10163,#4643,#4644);
#4076=AXIS2_PLACEMENT_3D('',#12207,#4645,#4646);
#4077=AXIS2_PLACEMENT_3D('',#14502,#4647,#4648);
#4078=AXIS2_PLACEMENT_3D('',#14504,#4649,#4650);
#4079=AXIS2_PLACEMENT_3D('',#14514,#4651,#4652);
#4080=AXIS2_PLACEMENT_3D('',#14720,#4653,#4654);
#4081=AXIS2_PLACEMENT_3D('',#14722,#4655,#4656);
#4082=AXIS2_PLACEMENT_3D('',#14723,#4657,#4658);
#4083=AXIS2_PLACEMENT_3D('',#14724,#4659,#4660);
#4084=AXIS2_PLACEMENT_3D('',#14726,#4661,#4662);
#4085=AXIS2_PLACEMENT_3D('',#14728,#4664,#4665);
#4086=AXIS2_PLACEMENT_3D('',#15520,#4666,#4667);
#4087=AXIS2_PLACEMENT_3D('',#15522,#4668,#4669);
#4088=AXIS2_PLACEMENT_3D('',#15525,#4671,#4672);
#4089=AXIS2_PLACEMENT_3D('',#15526,#4673,#4674);
#4090=AXIS2_PLACEMENT_3D('',#15527,#4675,#4676);
#4091=AXIS2_PLACEMENT_3D('',#15528,#4677,#4678);
#4615=DIRECTION('axis',(0.,0.,1.));
#4616=DIRECTION('refdir',(1.,0.,0.));
#4617=DIRECTION('center_axis',(1.,0.,0.));
#4618=DIRECTION('ref_axis',(0.,0.704081661975572,-0.710119013454587));
#4619=DIRECTION('',(-1.,0.,0.));
#4620=DIRECTION('center_axis',(-1.,0.,0.));
#4621=DIRECTION('ref_axis',(0.,1.,2.1444273868172E-14));
#4622=DIRECTION('center_axis',(1.,0.,0.));
#4623=DIRECTION('ref_axis',(0.,0.704081661975572,-0.710119013454587));
#4624=DIRECTION('',(-1.,0.,0.));
#4625=DIRECTION('center_axis',(1.,0.,0.));
#4626=DIRECTION('ref_axis',(0.,0.704081661975572,-0.710119013454587));
#4627=DIRECTION('',(-1.,0.,0.));
#4628=DIRECTION('center_axis',(1.,0.,0.));
#4629=DIRECTION('ref_axis',(0.,0.704081661975572,-0.710119013454587));
#4630=DIRECTION('',(-1.,0.,0.));
#4631=DIRECTION('center_axis',(1.,0.,0.));
#4632=DIRECTION('ref_axis',(0.,0.704081661975572,-0.710119013454587));
#4633=DIRECTION('',(-1.,0.,0.));
#4634=DIRECTION('center_axis',(1.,0.,0.));
#4635=DIRECTION('ref_axis',(0.,0.704081661975572,-0.710119013454587));
#4636=DIRECTION('',(-1.,0.,0.));
#4637=DIRECTION('center_axis',(1.,0.,0.));
#4638=DIRECTION('ref_axis',(0.,0.704081661975572,-0.710119013454587));
#4639=DIRECTION('center_axis',(1.,0.,0.));
#4640=DIRECTION('ref_axis',(0.,1.,2.1444273868172E-14));
#4641=DIRECTION('center_axis',(1.,0.,0.));
#4642=DIRECTION('ref_axis',(0.,1.,0.));
#4643=DIRECTION('center_axis',(-1.,0.,0.));
#4644=DIRECTION('ref_axis',(0.,1.,0.));
#4645=DIRECTION('center_axis',(-1.,0.,0.));
#4646=DIRECTION('ref_axis',(0.,1.,0.));
#4647=DIRECTION('center_axis',(1.,0.,0.));
#4648=DIRECTION('ref_axis',(0.,-0.692346234554118,0.72156544505591));
#4649=DIRECTION('center_axis',(-1.,0.,0.));
#4650=DIRECTION('ref_axis',(0.,9.28774802075533E-14,-1.));
#4651=DIRECTION('center_axis',(-1.,0.,0.));
#4652=DIRECTION('ref_axis',(0.,9.28774802075533E-14,-1.));
#4653=DIRECTION('center_axis',(1.,0.,0.));
#4654=DIRECTION('ref_axis',(0.,0.,-1.));
#4655=DIRECTION('center_axis',(-1.,0.,0.));
#4656=DIRECTION('ref_axis',(0.,0.,-1.));
#4657=DIRECTION('center_axis',(-1.,0.,0.));
#4658=DIRECTION('ref_axis',(0.,0.,-1.));
#4659=DIRECTION('center_axis',(1.,0.,0.));
#4660=DIRECTION('ref_axis',(0.,0.,-1.));
#4661=DIRECTION('center_axis',(1.,0.,0.));
#4662=DIRECTION('ref_axis',(0.,0.,-1.));
#4663=DIRECTION('',(1.,0.,0.));
#4664=DIRECTION('center_axis',(-1.,0.,0.));
#4665=DIRECTION('ref_axis',(0.,0.,-1.));
#4666=DIRECTION('center_axis',(1.,0.,0.));
#4667=DIRECTION('ref_axis',(0.,1.,0.));
#4668=DIRECTION('center_axis',(1.,0.,0.));
#4669=DIRECTION('ref_axis',(0.,1.,0.));
#4670=DIRECTION('',(-1.,0.,0.));
#4671=DIRECTION('center_axis',(1.,0.,0.));
#4672=DIRECTION('ref_axis',(0.,1.,0.));
#4673=DIRECTION('center_axis',(1.,0.,0.));
#4674=DIRECTION('ref_axis',(0.,1.,0.));
#4675=DIRECTION('center_axis',(1.,0.,0.));
#4676=DIRECTION('ref_axis',(0.,1.,0.));
#4677=DIRECTION('center_axis',(1.,0.,0.));
#4678=DIRECTION('ref_axis',(0.,1.,0.));
#7641=CARTESIAN_POINT('',(0.,0.,0.));
#7642=CARTESIAN_POINT('Origin',(80.1322559480305,0.,0.));
#7643=CARTESIAN_POINT('',(83.3472004496623,-2.62083096187227,2.64334895679097));
#7644=CARTESIAN_POINT('',(83.0989050616807,-2.62063375225138,2.64301435574924));
#7645=CARTESIAN_POINT('',(80.1322559480305,-2.62112000711956,2.64359555733806));
#7646=CARTESIAN_POINT('',(82.4430344427077,-2.13746972315899,-3.04920351925858));
#7647=CARTESIAN_POINT('Ctrl Pts',(82.4430344427077,-2.13746972315899,-3.04920351925858));
#7648=CARTESIAN_POINT('Ctrl Pts',(82.448599020418,-2.05742239043371,-3.10508886440805));
#7649=CARTESIAN_POINT('Ctrl Pts',(82.4542421068107,-1.97502380466239,-3.15787593603748));
#7650=CARTESIAN_POINT('Ctrl Pts',(82.4599027186458,-1.8905590270017,-3.20738255279828));
#7651=CARTESIAN_POINT('Ctrl Pts',(82.4661987179127,-1.79661332047366,-3.26244614519996));
#7652=CARTESIAN_POINT('Ctrl Pts',(82.4725160793993,-1.70011081204737,-3.31345191940099));
#7653=CARTESIAN_POINT('Ctrl Pts',(82.4787882071852,-1.60145546459568,-3.36018801727306));
#7654=CARTESIAN_POINT('Ctrl Pts',(82.4851385165621,-1.50157038581804,-3.40750667701421));
#7655=CARTESIAN_POINT('Ctrl Pts',(82.4914422189564,-1.39947851936814,-3.45044862674078));
#7656=CARTESIAN_POINT('Ctrl Pts',(82.4976522109053,-1.29561251865481,-3.4888308753646));
#7657=CARTESIAN_POINT('Ctrl Pts',(82.5037761074298,-1.19318651778106,-3.52668099190014));
#7658=CARTESIAN_POINT('Ctrl Pts',(82.5098088434891,-1.08903531916436,-3.56009707952411));
#7659=CARTESIAN_POINT('Ctrl Pts',(82.5157283399517,-0.983585676573463,-3.58893767538103));
#7660=CARTESIAN_POINT('Ctrl Pts',(82.5216461639355,-0.878165827446473,-3.61777012269206));
#7661=CARTESIAN_POINT('Ctrl Pts',(82.5274508110353,-0.771448321683715,-3.64202961671188));
#7662=CARTESIAN_POINT('Ctrl Pts',(82.5331437584232,-0.663870498101131,-3.66160866851016));
#7663=CARTESIAN_POINT('Ctrl Pts',(82.5388366319855,-0.556294069576837,-3.68118746640929));
#7664=CARTESIAN_POINT('Ctrl Pts',(82.5444178817885,-0.447857403542125,-3.69608582043075));
#7665=CARTESIAN_POINT('Ctrl Pts',(82.5499119917177,-0.339007936737362,-3.70623138116809));
#7666=CARTESIAN_POINT('Ctrl Pts',(82.5555437320619,-0.227431732122251,-3.71663109367008));
#7667=CARTESIAN_POINT('Ctrl Pts',(82.561083992165,-0.115421821891503,-3.72203652187028));
#7668=CARTESIAN_POINT('Ctrl Pts',(82.5665823292253,-0.00347010483924686,
-3.72241073611585));
#7669=CARTESIAN_POINT('Ctrl Pts',(82.5719534018203,0.105890378672952,-3.72277628880151));
#7670=CARTESIAN_POINT('Ctrl Pts',(82.5772848247073,0.215195189456353,-3.71834069411313));
#7671=CARTESIAN_POINT('Ctrl Pts',(82.5826411259721,0.323977809003443,-3.70911160173114));
#7672=CARTESIAN_POINT('Ctrl Pts',(82.5878495140364,0.429756418016825,-3.70013736891079));
#7673=CARTESIAN_POINT('Ctrl Pts',(82.5930817674659,0.535041662344979,-3.68663025460312));
#7674=CARTESIAN_POINT('Ctrl Pts',(82.5984092695587,0.639397738760414,-3.66864062923815));
#7675=CARTESIAN_POINT('Ctrl Pts',(82.5987552909183,0.64617566785591,-3.66747220273759));
#7676=CARTESIAN_POINT('Ctrl Pts',(82.5991017140848,0.652949694448339,-3.66628487290753));
#7677=CARTESIAN_POINT('Ctrl Pts',(82.5994485586168,0.659719706360457,-3.6650786559658));
#7678=CARTESIAN_POINT('Ctrl Pts',(82.6044019668751,0.756404617975652,-3.64785224928972));
#7679=CARTESIAN_POINT('Ctrl Pts',(82.6094418421539,0.85226762557606,-3.62677244801423));
#7680=CARTESIAN_POINT('Ctrl Pts',(82.6146291074746,0.946957722867219,-3.60191904664229));
#7681=CARTESIAN_POINT('Ctrl Pts',(82.6153947659428,0.960934311757064,-3.59825059784535));
#7682=CARTESIAN_POINT('Ctrl Pts',(82.616163635567,0.974885430209022,-3.59449997452717));
#7683=CARTESIAN_POINT('Ctrl Pts',(82.6169359122638,0.988810037286412,-3.59066747321032));
#7684=CARTESIAN_POINT('Ctrl Pts',(82.6169385232966,0.98885711575661,-3.59065451569575));
#7685=CARTESIAN_POINT('Ctrl Pts',(82.6169411343683,0.988904193923786,-3.59064155724526));
#7686=CARTESIAN_POINT('Ctrl Pts',(82.616943745479,0.988951271787904,-3.59062859785889));
#7687=CARTESIAN_POINT('Ctrl Pts',(82.6223437588327,1.08631255847876,-3.56382741315182));
#7688=CARTESIAN_POINT('Ctrl Pts',(82.6279228623114,1.18268025289156,-3.53292971855098));
#7689=CARTESIAN_POINT('Ctrl Pts',(82.6336067866526,1.27770342316418,-3.49806263639509));
#7690=CARTESIAN_POINT('Ctrl Pts',(82.634189838298,1.28745081113927,-3.49448600370269));
#7691=CARTESIAN_POINT('Ctrl Pts',(82.6347739929172,1.29718402569802,-3.49086764046184));
#7692=CARTESIAN_POINT('Ctrl Pts',(82.6353591703451,1.30690267098624,-3.48720770968247));
#7693=CARTESIAN_POINT('Ctrl Pts',(82.641641165732,1.41123424967816,-3.44791762914239));
#7694=CARTESIAN_POINT('Ctrl Pts',(82.6480404752863,1.51389054851696,-3.4038324220682));
#7695=CARTESIAN_POINT('Ctrl Pts',(82.6544691591425,1.61443137085044,-3.35516312012428));
#7696=CARTESIAN_POINT('Ctrl Pts',(82.6608915579549,1.71487389880572,-3.30654140003479));
#7697=CARTESIAN_POINT('Ctrl Pts',(82.6673429189712,1.81320529683611,-3.25334486330551));
#7698=CARTESIAN_POINT('Ctrl Pts',(82.673753583758,1.90901390837151,-3.19581575437501));
#7699=CARTESIAN_POINT('Ctrl Pts',(82.6801598752994,2.0047571609184,-3.13832589081409));
#7700=CARTESIAN_POINT('Ctrl Pts',(82.6865253269448,2.09798121640403,-3.07650952231491));
#7701=CARTESIAN_POINT('Ctrl Pts',(82.6928025349669,2.18829974073378,-3.01063669396523));
#7702=CARTESIAN_POINT('Ctrl Pts',(82.6990774796109,2.27858569883874,-2.94478761743559));
#7703=CARTESIAN_POINT('Ctrl Pts',(82.7052641575682,2.36596828259258,-2.87488506236255));
#7704=CARTESIAN_POINT('Ctrl Pts',(82.7113394306864,2.45008446654331,-2.80122550716461));
#7705=CARTESIAN_POINT('Ctrl Pts',(82.7174139832278,2.53419067363046,-2.72757468858904));
#7706=CARTESIAN_POINT('Ctrl Pts',(82.7233771574382,2.61503123368847,-2.6501677521564));
#7707=CARTESIAN_POINT('Ctrl Pts',(82.7292306714799,2.69226584882458,-2.56932746171694));
#7708=CARTESIAN_POINT('Ctrl Pts',(82.735084907537,2.76950999064356,-2.48847719984422));
#7709=CARTESIAN_POINT('Ctrl Pts',(82.740829536682,2.84314719537528,-2.40419267740033));
#7710=CARTESIAN_POINT('Ctrl Pts',(82.7464905348952,2.91286057875016,-2.31682369884723));
#7711=CARTESIAN_POINT('Ctrl Pts',(82.7521570798643,2.98264226865268,-2.22936911447127));
#7712=CARTESIAN_POINT('Ctrl Pts',(82.7577400007629,3.04849224778961,-2.13882391940644));
#7713=CARTESIAN_POINT('Ctrl Pts',(82.7632877940693,3.11011851311843,-2.04556718326659));
#7714=CARTESIAN_POINT('Ctrl Pts',(82.7688382903374,3.17177480361737,-1.9522650111531));
#7715=CARTESIAN_POINT('Ctrl Pts',(82.7743539191269,3.22920295013996,-1.85624852227942));
#7716=CARTESIAN_POINT('Ctrl Pts',(82.7799022412833,3.28214013584634,-1.75792741509752));
#7717=CARTESIAN_POINT('Ctrl Pts',(82.7854593714353,3.3351613596614,-1.6594502225518));
#7718=CARTESIAN_POINT('Ctrl Pts',(82.7910497493793,3.38367687065512,-1.55866097056305));
#7719=CARTESIAN_POINT('Ctrl Pts',(82.7967547537525,3.42745823752841,-1.45600343909067));
#7720=CARTESIAN_POINT('Ctrl Pts',(82.8020073577273,3.46776779149483,-1.36148653383001));
#7721=CARTESIAN_POINT('Ctrl Pts',(82.8073576638974,3.50406423704884,-1.26538626329073));
#7722=CARTESIAN_POINT('Ctrl Pts',(82.812873362228,3.53620220344326,-1.16807374112353));
#7723=CARTESIAN_POINT('Ctrl Pts',(82.8128756709941,3.53621565578332,-1.16803300795691));
#7724=CARTESIAN_POINT('Ctrl Pts',(82.8128779797893,3.53622910739548,-1.16799227457744));
#7725=CARTESIAN_POINT('Ctrl Pts',(82.8128802886134,3.53624255827976,-1.16795154098513));
#7726=CARTESIAN_POINT('Ctrl Pts',(82.8183364857455,3.56802959447665,-1.07169019891507));
#7727=CARTESIAN_POINT('Ctrl Pts',(82.8239655492868,3.59583022943719,-0.973972859449433));
#7728=CARTESIAN_POINT('Ctrl Pts',(82.8296926587345,3.61955415052866,-0.875165751197072));
#7729=CARTESIAN_POINT('Ctrl Pts',(82.8302450796905,3.62184249359063,-0.86563509394313));
#7730=CARTESIAN_POINT('Ctrl Pts',(82.8307984128648,3.62409292118861,-0.856094334891532));
#7731=CARTESIAN_POINT('Ctrl Pts',(82.8313525911108,3.62630536186244,-0.846543826418543));
#7732=CARTESIAN_POINT('Ctrl Pts',(82.8376442504153,3.65142349497653,-0.738115633984115));
#7733=CARTESIAN_POINT('Ctrl Pts',(82.8440442952487,3.67164363836166,-0.628425160901477));
#7734=CARTESIAN_POINT('Ctrl Pts',(82.8504661980963,3.68689646460076,-0.517952854476233));
#7735=CARTESIAN_POINT('Ctrl Pts',(82.8568818350485,3.70213440855105,-0.407588336649791));
#7736=CARTESIAN_POINT('Ctrl Pts',(82.8633189471795,3.71241508912789,-0.296443513022478));
#7737=CARTESIAN_POINT('Ctrl Pts',(82.869709517214,3.71771058909135,-0.184992936878773));
#7738=CARTESIAN_POINT('Ctrl Pts',(82.876095800766,3.72300253709186,-0.0736171163425392));
#7739=CARTESIAN_POINT('Ctrl Pts',(82.8824354149202,3.72331619094564,0.0380640758994348));
#7740=CARTESIAN_POINT('Ctrl Pts',(82.8886826470533,3.71866065339773,0.149581257438668));
#7741=CARTESIAN_POINT('Ctrl Pts',(82.8949276751545,3.71400675832982,0.261059095564304));
#7742=CARTESIAN_POINT('Ctrl Pts',(82.9010803057731,3.70438725083538,0.372373051082597));
#7743=CARTESIAN_POINT('Ctrl Pts',(82.9071190301882,3.68984615519603,0.483058114605687));
#7744=CARTESIAN_POINT('Ctrl Pts',(82.9131571001419,3.67530663548319,0.593731182366596));
#7745=CARTESIAN_POINT('Ctrl Pts',(82.9190812929002,3.65584656994163,0.703775474025912));
#7746=CARTESIAN_POINT('Ctrl Pts',(82.9248948207163,3.63154455459684,0.81273006150251));
#7747=CARTESIAN_POINT('Ctrl Pts',(82.9307091394138,3.60723923316746,0.921699471333437));
#7748=CARTESIAN_POINT('Ctrl Pts',(82.9364128470765,3.57809053510775,1.02957882216876));
#7749=CARTESIAN_POINT('Ctrl Pts',(82.9420332222564,3.54421269521027,1.13591151444198));
#7750=CARTESIAN_POINT('Ctrl Pts',(82.9476592811328,3.51030059579144,1.2423517373946));
#7751=CARTESIAN_POINT('Ctrl Pts',(82.9532020137706,3.47164958467528,1.34724206263577));
#7752=CARTESIAN_POINT('Ctrl Pts',(82.9587109769047,3.42841224504195,1.45013026888811));
#7753=CARTESIAN_POINT('Ctrl Pts',(82.9642227061628,3.38515319536202,1.5530701366851));
#7754=CARTESIAN_POINT('Ctrl Pts',(82.9697009311859,3.33730292490927,1.6540056815073));
#7755=CARTESIAN_POINT('Ctrl Pts',(82.9752139615805,3.28505590947795,1.75249199067341));
#7756=CARTESIAN_POINT('Ctrl Pts',(82.9807359802808,3.23272371183045,1.85113886943394));
#7757=CARTESIAN_POINT('Ctrl Pts',(82.9862933738097,3.1759800559052,1.94732817734345));
#7758=CARTESIAN_POINT('Ctrl Pts',(82.9919678899615,3.11506709186677,2.04062478348433));
#7759=CARTESIAN_POINT('Ctrl Pts',(82.9972893737137,3.05794374605924,2.12811706660311));
#7760=CARTESIAN_POINT('Ctrl Pts',(83.0027144147527,2.99715390579646,2.21306510187555));
#7761=CARTESIAN_POINT('Ctrl Pts',(83.0083144719426,2.93293887122742,2.29512480585364));
#7762=CARTESIAN_POINT('Ctrl Pts',(83.0083169090159,2.93291092566555,2.29516051718743));
#7763=CARTESIAN_POINT('Ctrl Pts',(83.0083193461223,2.93288297945502,2.29519622797522));
#7764=CARTESIAN_POINT('Ctrl Pts',(83.0083217832619,2.93285503259586,2.29523193821698));
#7765=CARTESIAN_POINT('Ctrl Pts',(83.013748510229,2.87062635440728,2.3747471757048));
#7766=CARTESIAN_POINT('Ctrl Pts',(83.019350976778,2.80499626954421,2.45177672341973));
#7767=CARTESIAN_POINT('Ctrl Pts',(83.0250542593079,2.73621649003507,2.52604381205996));
#7768=CARTESIAN_POINT('Ctrl Pts',(83.0256152719976,2.72945085482468,2.53334921538436));
#7769=CARTESIAN_POINT('Ctrl Pts',(83.0261772601821,2.72265478377114,2.54062787998606));
#7770=CARTESIAN_POINT('Ctrl Pts',(83.0267401525496,2.71582854307071,2.54787953697994));
#7771=CARTESIAN_POINT('Ctrl Pts',(83.0330173539257,2.6397044205996,2.62874777022077));
#7772=CARTESIAN_POINT('Ctrl Pts',(83.0394064576322,2.5598227077811,2.70625903217862));
#7773=CARTESIAN_POINT('Ctrl Pts',(83.045820175139,2.47654279495297,2.78008926792871));
#7774=CARTESIAN_POINT('Ctrl Pts',(83.052227397231,2.39334722284971,2.85384473300015));
#7775=CARTESIAN_POINT('Ctrl Pts',(83.0586588407085,2.30676053662994,2.92392692670572));
#7776=CARTESIAN_POINT('Ctrl Pts',(83.0650456575877,2.21716027063657,2.99004955358705));
#7777=CARTESIAN_POINT('Ctrl Pts',(83.0714278944391,2.12762425757619,3.05612476350296));
#7778=CARTESIAN_POINT('Ctrl Pts',(83.0777653772024,2.03507907421888,3.11824626719335));
#7779=CARTESIAN_POINT('Ctrl Pts',(83.0840115212539,1.93991852507007,3.17616147120232));
#7780=CARTESIAN_POINT('Ctrl Pts',(83.0902552902423,1.84479416021438,3.23405465326274));
#7781=CARTESIAN_POINT('Ctrl Pts',(83.0964077076695,1.74705645069182,3.28774480190484));
#7782=CARTESIAN_POINT('Ctrl Pts',(83.1024463695484,1.64711496019518,3.33701081475946));
#7783=CARTESIAN_POINT('Ctrl Pts',(83.1084842289857,1.54718675032443,3.3862702809488));
#7784=CARTESIAN_POINT('Ctrl Pts',(83.1144083654278,1.44505535153882,3.43110675608568));
#7785=CARTESIAN_POINT('Ctrl Pts',(83.1202210958824,1.34114609734128,3.47133016523115));
#7786=CARTESIAN_POINT('Ctrl Pts',(83.1260344917427,1.23722494824878,3.51155817890613));
#7787=CARTESIAN_POINT('Ctrl Pts',(83.1317365372578,1.13152552810977,3.54717194893531));
#7788=CARTESIAN_POINT('Ctrl Pts',(83.1373536485256,1.0244892779953,3.57801342989723));
#7789=CARTESIAN_POINT('Ctrl Pts',(83.1429763325976,0.917346835920189,3.60888550906611));
#7790=CARTESIAN_POINT('Ctrl Pts',(83.1485140843379,0.808864893437081,3.63497560174989));
#7791=CARTESIAN_POINT('Ctrl Pts',(83.1540156802369,0.699502403811492,3.65615992849922));
#7792=CARTESIAN_POINT('Ctrl Pts',(83.1595199628709,0.590086506405814,3.67735460073235));
#7793=CARTESIAN_POINT('Ctrl Pts',(83.1649883472167,0.479789205696713,3.69363837602126));
#7794=CARTESIAN_POINT('Ctrl Pts',(83.1704885251433,0.369086461722915,3.70492623568189));
#7795=CARTESIAN_POINT('Ctrl Pts',(83.1759976774181,0.258203089962481,3.7162325131435));
#7796=CARTESIAN_POINT('Ctrl Pts',(83.181539174532,0.146913031264152,3.72252607292026));
#7797=CARTESIAN_POINT('Ctrl Pts',(83.1871944214616,0.0357104127877853,3.72376672713407));
#7798=CARTESIAN_POINT('Ctrl Pts',(83.1922556540262,-0.0638117337991707,
3.72487706583133));
#7799=CARTESIAN_POINT('Ctrl Pts',(83.1974084980998,-0.163264124747811,3.72194044402702));
#7800=CARTESIAN_POINT('Ctrl Pts',(83.2027150991779,-0.262281572855464,3.71496438230409));
#7801=CARTESIAN_POINT('Ctrl Pts',(83.2031054575553,-0.269565385942157,3.7144512168909));
#7802=CARTESIAN_POINT('Ctrl Pts',(83.2034966479436,-0.27684686462192,3.71391620668298));
#7803=CARTESIAN_POINT('Ctrl Pts',(83.2038886950801,-0.284125872785762,3.71335936092993));
#7804=CARTESIAN_POINT('Ctrl Pts',(83.203891136264,-0.284171197431151,3.71335589358442));
#7805=CARTESIAN_POINT('Ctrl Pts',(83.2038935774811,-0.284216521980756,3.71335242539229));
#7806=CARTESIAN_POINT('Ctrl Pts',(83.2038960187314,-0.284261846434547,3.71334895635357));
#7807=CARTESIAN_POINT('Ctrl Pts',(83.2093252565624,-0.38506152120613,3.70563396047512));
#7808=CARTESIAN_POINT('Ctrl Pts',(83.2149301683938,-0.485673358945827,3.69370039164411));
#7809=CARTESIAN_POINT('Ctrl Pts',(83.2206360185141,-0.585726878726986,3.67760519262689));
#7810=CARTESIAN_POINT('Ctrl Pts',(83.2211983295403,-0.595587144278816,3.676019012183));
#7811=CARTESIAN_POINT('Ctrl Pts',(83.2217616208878,-0.605441957224624,3.67439244250633));
#7812=CARTESIAN_POINT('Ctrl Pts',(83.2223258210251,-0.615290943611994,3.6727255573895));
#7813=CARTESIAN_POINT('Ctrl Pts',(83.2286076879843,-0.724950651362645,3.65416627346153));
#7814=CARTESIAN_POINT('Ctrl Pts',(83.2350016713654,-0.833892609821066,3.63060534416091));
#7815=CARTESIAN_POINT('Ctrl Pts',(83.2414205881829,-0.941646888095381,3.60216349040293));
#7816=CARTESIAN_POINT('Ctrl Pts',(83.2478335756957,-1.04930163120416,3.57374790905536));
#7817=CARTESIAN_POINT('Ctrl Pts',(83.2542711057617,-1.15577102706027,3.54046075836396));
#7818=CARTESIAN_POINT('Ctrl Pts',(83.2606643943902,-1.26060657552585,3.50245879728538));
#7819=CARTESIAN_POINT('Ctrl Pts',(83.267053345539,-1.36537099908479,3.46448261835774));
#7820=CARTESIAN_POINT('Ctrl Pts',(83.2733979224415,-1.46850389809735,3.42179820146728));
#7821=CARTESIAN_POINT('Ctrl Pts',(83.2796516060403,-1.56957589780418,3.37459449492827));
#7822=CARTESIAN_POINT('Ctrl Pts',(83.2859035825247,-1.67062030713583,3.32740367393597));
#7823=CARTESIAN_POINT('Ctrl Pts',(83.292064632062,-1.76960498350736,3.27569609467376));
#7824=CARTESIAN_POINT('Ctrl Pts',(83.2981124330876,-1.86611799349614,3.21969128823285));
#7825=CARTESIAN_POINT('Ctrl Pts',(83.3041590631163,-1.96261231629155,3.16369732564241));
#7826=CARTESIAN_POINT('Ctrl Pts',(83.3100924911403,-2.05663590320112,3.10340778724449));
#7827=CARTESIAN_POINT('Ctrl Pts',(83.3159151518672,-2.14779403729,3.03907244084058));
#7828=CARTESIAN_POINT('Ctrl Pts',(83.3217404122008,-2.238992870176,2.97470837104039));
#7829=CARTESIAN_POINT('Ctrl Pts',(83.327454886879,-2.32732359545313,2.90629480158804));
#7830=CARTESIAN_POINT('Ctrl Pts',(83.3330851650687,-2.41240887718516,2.83411292117315));
#7831=CARTESIAN_POINT('Ctrl Pts',(83.3378403569136,-2.48426977360557,2.77314991410147));
#7832=CARTESIAN_POINT('Ctrl Pts',(83.3425359671718,-2.55381591599853,2.7094994265022));
#7833=CARTESIAN_POINT('Ctrl Pts',(83.3472004496623,-2.62083096187227,2.64334895679097));
#7834=CARTESIAN_POINT('',(82.4430005297901,2.16151778945158,-3.03095833168065));
#7835=CARTESIAN_POINT('Origin',(82.4430005297901,0.,0.));
#7836=CARTESIAN_POINT('Ctrl Pts',(82.4430005297901,2.16151778945158,-3.03095833168064));
#7837=CARTESIAN_POINT('Ctrl Pts',(82.4497525870341,2.2643871255196,-2.95759740897315));
#7838=CARTESIAN_POINT('Ctrl Pts',(82.4564309935575,2.36343920336681,-2.8790005193258));
#7839=CARTESIAN_POINT('Ctrl Pts',(82.463090623901,2.45821022550934,-2.79559583490443));
#7840=CARTESIAN_POINT('Ctrl Pts',(82.4697568618797,2.55307527874839,-2.71210839698148));
#7841=CARTESIAN_POINT('Ctrl Pts',(82.4764047311352,2.64365116871439,-2.62380392905304));
#7842=CARTESIAN_POINT('Ctrl Pts',(82.4830735939787,2.72951313809316,-2.53113618409738));
#7843=CARTESIAN_POINT('Ctrl Pts',(82.4897405696392,2.81535080988868,-2.43849466265212));
#7844=CARTESIAN_POINT('Ctrl Pts',(82.4964287755875,2.89647757511398,-2.34149239606588));
#7845=CARTESIAN_POINT('Ctrl Pts',(82.5031567095667,2.97250377452681,-2.24060427989571));
#7846=CARTESIAN_POINT('Ctrl Pts',(82.5098729756242,3.04839812547926,-2.13989112897292));
#7847=CARTESIAN_POINT('Ctrl Pts',(82.5166289021824,3.11920981016223,-2.03530546536337));
#7848=CARTESIAN_POINT('Ctrl Pts',(82.5234197668534,3.18458147885758,-1.9273417200709));
#7849=CARTESIAN_POINT('Ctrl Pts',(82.5290415570546,3.23869915375146,-1.83796436464048));
#7850=CARTESIAN_POINT('Ctrl Pts',(82.5346868339601,3.28908916023992,-1.74627221537606));
#7851=CARTESIAN_POINT('Ctrl Pts',(82.5403409406944,3.33556346134786,-1.65255871416402));
#7852=CARTESIAN_POINT('Ctrl Pts',(82.5403413804331,3.33556707580869,-1.65255142575362));
#7853=CARTESIAN_POINT('Ctrl Pts',(82.5403418201718,3.33557069024584,-1.65254413733098));
#7854=CARTESIAN_POINT('Ctrl Pts',(82.5403422599106,3.33557430465931,-1.65253684889611));
#7855=CARTESIAN_POINT('Ctrl Pts',(82.5464419928859,3.38571079068679,-1.55143703950375));
#7856=CARTESIAN_POINT('Ctrl Pts',(82.5525511172057,3.43126617851106,-1.44802709255062));
#7857=CARTESIAN_POINT('Ctrl Pts',(82.5586922252033,3.47204912375138,-1.34275980756767));
#7858=CARTESIAN_POINT('Ctrl Pts',(82.5648327804175,3.51282839797113,-1.23750199807418));
#7859=CARTESIAN_POINT('Ctrl Pts',(82.5710053901627,3.54883620716724,-1.13038720018602));
#7860=CARTESIAN_POINT('Ctrl Pts',(82.5772071341509,3.57991676752814,-1.02187841964011));
#7861=CARTESIAN_POINT('Ctrl Pts',(82.583411964925,3.61101279757595,-0.913315631159872));
#7862=CARTESIAN_POINT('Ctrl Pts',(82.5896459347367,3.63717667625632,-0.803357419154788));
#7863=CARTESIAN_POINT('Ctrl Pts',(82.5958801874174,3.65828700678163,-0.692478117868246));
#7864=CARTESIAN_POINT('Ctrl Pts',(82.6021161755057,3.6794032137175,-0.581567951489553));
#7865=CARTESIAN_POINT('Ctrl Pts',(82.6083523050562,3.69546292697117,-0.469736079958543));
#7866=CARTESIAN_POINT('Ctrl Pts',(82.6145349776752,3.70638020509523,-0.357469063727132));
#7867=CARTESIAN_POINT('Ctrl Pts',(82.6207234444741,3.71730771450215,-0.245096834860658));
#7868=CARTESIAN_POINT('Ctrl Pts',(82.6268580629749,3.72308283210855,-0.132288527659337));
#7869=CARTESIAN_POINT('Ctrl Pts',(82.6328635227856,3.72365829592863,-0.0195456358231097));
#7870=CARTESIAN_POINT('Ctrl Pts',(82.63531318067,3.72389303057484,0.0264427684947558));
#7871=CARTESIAN_POINT('Ctrl Pts',(82.6377411248295,3.72326308981242,0.0724201216892056));
#7872=CARTESIAN_POINT('Ctrl Pts',(82.6401414282941,3.72176735365084,0.11835168109134));
#7873=CARTESIAN_POINT('Ctrl Pts',(82.6401428334758,3.72176647801945,0.118378570268839));
#7874=CARTESIAN_POINT('Ctrl Pts',(82.6401442386485,3.72176560209123,0.118405459443261));
#7875=CARTESIAN_POINT('Ctrl Pts',(82.6401456438123,3.72176472586617,0.118432348614587));
#7876=CARTESIAN_POINT('Ctrl Pts',(82.645522635828,3.71841176773665,0.221326307545291));
#7877=CARTESIAN_POINT('Ctrl Pts',(82.6507682282706,3.7107094660618,0.324178372433314));
#7878=CARTESIAN_POINT('Ctrl Pts',(82.6559448084897,3.69870088117316,0.426600109422855));
#7879=CARTESIAN_POINT('Ctrl Pts',(82.6564326859769,3.69756910730466,0.436253057423465));
#7880=CARTESIAN_POINT('Ctrl Pts',(82.6569199504623,3.69639910806877,0.445902154317524));
#7881=CARTESIAN_POINT('Ctrl Pts',(82.6574066541737,3.69519093559596,0.455547057373284));
#7882=CARTESIAN_POINT('Ctrl Pts',(82.6630537803773,3.6811727510821,0.567454946103847));
#7883=CARTESIAN_POINT('Ctrl Pts',(82.6686259946562,3.66201198643677,0.678802678279904));
#7884=CARTESIAN_POINT('Ctrl Pts',(82.6741977677731,3.63781636838717,0.78909978021698));
#7885=CARTESIAN_POINT('Ctrl Pts',(82.6797659318231,3.61363642283602,0.89932543817782));
#7886=CARTESIAN_POINT('Ctrl Pts',(82.6853340641559,3.5844286005684,1.00850181621864));
#7887=CARTESIAN_POINT('Ctrl Pts',(82.6909619773351,3.55034171631595,1.11616037592857));
#7888=CARTESIAN_POINT('Ctrl Pts',(82.6965885352234,3.51626304072669,1.22379300974715));
#7889=CARTESIAN_POINT('Ctrl Pts',(82.702275109538,3.47730796553248,1.32990859917549));
#7890=CARTESIAN_POINT('Ctrl Pts',(82.7080619420672,3.43366074693369,1.43405961383778));
#7891=CARTESIAN_POINT('Ctrl Pts',(82.7138482053755,3.39001782168696,1.53820038370127));
#7892=CARTESIAN_POINT('Ctrl Pts',(82.7197348588063,3.34168387046001,1.64037701333392));
#7893=CARTESIAN_POINT('Ctrl Pts',(82.7257395141122,3.28887486217381,1.74016206022673));
#7894=CARTESIAN_POINT('Ctrl Pts',(82.7317449192916,3.23605925899219,1.83995956847735));
#7895=CARTESIAN_POINT('Ctrl Pts',(82.7378684178647,3.17876757442851,1.93736492912828));
#7896=CARTESIAN_POINT('Ctrl Pts',(82.7441034140718,3.11724548796642,2.0319698863094));
#7897=CARTESIAN_POINT('Ctrl Pts',(82.7503405809174,3.05570198333541,2.12660777906));
#7898=CARTESIAN_POINT('Ctrl Pts',(82.7566893021505,2.98992512603072,2.21844332399032));
#7899=CARTESIAN_POINT('Ctrl Pts',(82.7631184329245,2.92018983143804,2.3070868990241));
#7900=CARTESIAN_POINT('Ctrl Pts',(82.7695555892579,2.85036748545784,2.39584112887401));
#7901=CARTESIAN_POINT('Ctrl Pts',(82.7760732421521,2.77657669642733,2.48139537150511));
#7902=CARTESIAN_POINT('Ctrl Pts',(82.7826165146318,2.69912336244941,2.56337790417287));
#7903=CARTESIAN_POINT('Ctrl Pts',(82.7891640304413,2.62161979977606,2.6454136027336));
#7904=CARTESIAN_POINT('Ctrl Pts',(82.7957369546042,2.54044870904736,2.72387282576453));
#7905=CARTESIAN_POINT('Ctrl Pts',(82.8022593265139,2.45594916272644,2.79840375151851));
#7906=CARTESIAN_POINT('Ctrl Pts',(82.8087929615909,2.37130369824371,2.87306338110769));
#7907=CARTESIAN_POINT('Ctrl Pts',(82.8152754528664,2.28331793548545,2.94378083250582));
#7908=CARTESIAN_POINT('Ctrl Pts',(82.8216143153064,2.19236970908168,3.01022632126189));
#7909=CARTESIAN_POINT('Ctrl Pts',(82.8267383484441,2.11885151392845,3.0639376755409));
#7910=CARTESIAN_POINT('Ctrl Pts',(82.8317680624639,2.04339817135242,3.11485788892921));
#7911=CARTESIAN_POINT('Ctrl Pts',(82.8366503980456,1.96622925062276,3.16282692428072));
#7912=CARTESIAN_POINT('Ctrl Pts',(82.8366527886688,1.96619146505635,3.16285041219728));
#7913=CARTESIAN_POINT('Ctrl Pts',(82.8366551792591,1.96615367902892,3.16287389943928));
#7914=CARTESIAN_POINT('Ctrl Pts',(82.8366575698165,1.9661158925405,3.16289738600667));
#7915=CARTESIAN_POINT('Ctrl Pts',(82.841950133003,1.88245867630496,3.21489536012051));
#7916=CARTESIAN_POINT('Ctrl Pts',(82.8470813568417,1.7965374989223,3.26358628833678));
#7917=CARTESIAN_POINT('Ctrl Pts',(82.8521147636254,1.70866270441033,3.30879236920142));
#7918=CARTESIAN_POINT('Ctrl Pts',(82.8526922604478,1.69858058373519,3.3139789891538));
#7919=CARTESIAN_POINT('Ctrl Pts',(82.8532684696442,1.68847280233983,3.31911974325924));
#7920=CARTESIAN_POINT('Ctrl Pts',(82.8538434871523,1.67833987220444,3.32421436956907));
#7921=CARTESIAN_POINT('Ctrl Pts',(82.8594246728968,1.57998849259643,3.37366339561229));
#7922=CARTESIAN_POINT('Ctrl Pts',(82.864894200596,1.47926182311506,3.41876625740564));
#7923=CARTESIAN_POINT('Ctrl Pts',(82.8703338865973,1.37660580206139,3.45933022664339));
#7924=CARTESIAN_POINT('Ctrl Pts',(82.8757674440819,1.27406543642321,3.49984849527179));
#7925=CARTESIAN_POINT('Ctrl Pts',(82.881171656312,1.1696003477985,3.53583845902318));
#7926=CARTESIAN_POINT('Ctrl Pts',(82.8866144035847,1.06366249754844,3.56715439087171));
#7927=CARTESIAN_POINT('Ctrl Pts',(82.892094624789,0.956995253198249,3.59868593645864));
#7928=CARTESIAN_POINT('Ctrl Pts',(82.8976142242023,0.848835056519796,3.62547909822655));
#7929=CARTESIAN_POINT('Ctrl Pts',(82.9032230550498,0.739647643605751,3.6474276875812));
#7930=CARTESIAN_POINT('Ctrl Pts',(82.9087862130298,0.631349346870345,3.66919754895456));
#7931=CARTESIAN_POINT('Ctrl Pts',(82.9144372918968,0.522040595941809,3.68620165227875));
#7932=CARTESIAN_POINT('Ctrl Pts',(82.9202026482306,0.41217821478049,3.69837446221263));
#7933=CARTESIAN_POINT('Ctrl Pts',(82.9259668521448,0.302337793676463,3.71054483896056));
#7934=CARTESIAN_POINT('Ctrl Pts',(82.9318453637412,0.191944025268312,3.71788595476851));
#7935=CARTESIAN_POINT('Ctrl Pts',(82.9378405423052,0.081454649124195,3.72036809750293));
#7936=CARTESIAN_POINT('Ctrl Pts',(82.9438360708962,-0.0290411779126,3.72285038515659));
#7937=CARTESIAN_POINT('Ctrl Pts',(82.9499482803377,-0.139632588322064,3.72047315281383));
#7938=CARTESIAN_POINT('Ctrl Pts',(82.956154973994,-0.249861298021894,3.71324156078738));
#7939=CARTESIAN_POINT('Ctrl Pts',(82.9624522619302,-0.361698930465173,3.70590441483661));
#7940=CARTESIAN_POINT('Ctrl Pts',(82.968846785684,-0.473163183084761,3.69357000063643));
#7941=CARTESIAN_POINT('Ctrl Pts',(82.9752901691881,-0.583775300960439,3.6762807804806));
#7942=CARTESIAN_POINT('Ctrl Pts',(82.9816499159366,-0.692951645430586,3.65921597879699));
#7943=CARTESIAN_POINT('Ctrl Pts',(82.9880570189023,-0.801297825350726,3.63732405246524));
#7944=CARTESIAN_POINT('Ctrl Pts',(82.9944427688165,-0.908353516352129,3.61068347162499));
#7945=CARTESIAN_POINT('Ctrl Pts',(83.000954486814,-1.01752103452814,3.58351736708731));
#7946=CARTESIAN_POINT('Ctrl Pts',(83.0074437003446,-1.12534658989672,3.55141290154023));
#7947=CARTESIAN_POINT('Ctrl Pts',(83.0138181954763,-1.23134252417002,3.51449763874511));
#7948=CARTESIAN_POINT('Ctrl Pts',(83.0195255882697,-1.32624579398194,3.4814456243519));
#7949=CARTESIAN_POINT('Ctrl Pts',(83.0251405465292,-1.41968322053829,3.44453686041246));
#7950=CARTESIAN_POINT('Ctrl Pts',(83.0305879677352,-1.51130353807574,3.40389930429182));
#7951=CARTESIAN_POINT('Ctrl Pts',(83.03122468358,-1.52201247826612,3.39914942817618));
#7952=CARTESIAN_POINT('Ctrl Pts',(83.0318591105594,-1.53269665019523,3.3943486242449));
#7953=CARTESIAN_POINT('Ctrl Pts',(83.0324911287457,-1.5433555383646,3.38949710732856));
#7954=CARTESIAN_POINT('Ctrl Pts',(83.0324937959921,-1.54340052105906,3.38947663293202));
#7955=CARTESIAN_POINT('Ctrl Pts',(83.0324964631984,-1.54344550336794,3.38945615760467));
#7956=CARTESIAN_POINT('Ctrl Pts',(83.0324991303647,-1.54349048529117,3.38943568134652));
#7957=CARTESIAN_POINT('Ctrl Pts',(83.0378606707335,-1.63391319469024,3.34827428566594));
#7958=CARTESIAN_POINT('Ctrl Pts',(83.0430602772996,-1.72277948316394,3.30334766288235));
#7959=CARTESIAN_POINT('Ctrl Pts',(83.0481595952658,-1.80976892931888,3.25482279871221));
#7960=CARTESIAN_POINT('Ctrl Pts',(83.048771082511,-1.82020031193624,3.24900391553744));
#7961=CARTESIAN_POINT('Ctrl Pts',(83.0493811276336,-1.83060468026478,3.24313334652199));
#7962=CARTESIAN_POINT('Ctrl Pts',(83.0499898369316,-1.84098146169455,3.2372114256022));
#7963=CARTESIAN_POINT('Ctrl Pts',(83.0556710275469,-1.93782978234437,3.18194109925064));
#7964=CARTESIAN_POINT('Ctrl Pts',(83.0612364938514,-2.03227788805904,3.12219212008623));
#7965=CARTESIAN_POINT('Ctrl Pts',(83.0667674937821,-2.12391272180136,3.05824252474161));
#7966=CARTESIAN_POINT('Ctrl Pts',(83.0722929678339,-2.21545600555163,2.99435681978349));
#7967=CARTESIAN_POINT('Ctrl Pts',(83.0777844963081,-2.30419180547416,2.92627935066107));
#7968=CARTESIAN_POINT('Ctrl Pts',(83.0833097974269,-2.38974428256799,2.85431879316216));
#7969=CARTESIAN_POINT('Ctrl Pts',(83.0884653414204,-2.46957152635635,2.78717388793269));
#7970=CARTESIAN_POINT('Ctrl Pts',(83.0936503489239,-2.54662769771509,2.71664870107101));
#7971=CARTESIAN_POINT('Ctrl Pts',(83.0989050616807,-2.62063375225138,2.64301435574924));
#7972=CARTESIAN_POINT('Origin',(80.1322559480305,0.,0.));
#7973=CARTESIAN_POINT('',(84.5943437838656,-2.62112000711956,2.64359555733806));
#7974=CARTESIAN_POINT('',(84.3497092098018,-2.62112000711956,2.64359555733807));
#7975=CARTESIAN_POINT('',(80.1322559480305,-2.62112000711956,2.64359555733806));
#7976=CARTESIAN_POINT('Ctrl Pts',(84.5943437838656,-2.62112000711956,2.64359555733807));
#7977=CARTESIAN_POINT('Ctrl Pts',(84.5907408117248,-2.57694702423373,2.68739298652303));
#7978=CARTESIAN_POINT('Ctrl Pts',(84.5871743154747,-2.53166613263349,2.73009334161478));
#7979=CARTESIAN_POINT('Ctrl Pts',(84.5811736507666,-2.45240380688733,2.80116715995069));
#7980=CARTESIAN_POINT('Ctrl Pts',(84.5787120403164,-2.41896578754705,2.83009306267694));
#7981=CARTESIAN_POINT('Ctrl Pts',(84.5748329068826,-2.36462883644873,2.87543096642596));
#7982=CARTESIAN_POINT('Ctrl Pts',(84.5733911059468,-2.34405632918012,2.89222627317259));
#7983=CARTESIAN_POINT('Ctrl Pts',(84.570497528159,-2.30195399772164,2.92585407015743));
#7984=CARTESIAN_POINT('Ctrl Pts',(84.5690466230318,-2.28041520767029,2.94267239400238));
#7985=CARTESIAN_POINT('Ctrl Pts',(84.5650854642014,-2.22050570304682,2.98839919482867));
#7986=CARTESIAN_POINT('Ctrl Pts',(84.5626061580896,-2.18175658138579,3.01680525510096));
#7987=CARTESIAN_POINT('Ctrl Pts',(84.5569465167446,-2.09076601110375,3.08083783594035));
#7988=CARTESIAN_POINT('Ctrl Pts',(84.5537930363585,-2.03814459945658,3.11589979411636));
#7989=CARTESIAN_POINT('Ctrl Pts',(84.5420555568739,-1.83649143568314,3.24296702728022));
#7990=CARTESIAN_POINT('Ctrl Pts',(84.5337446102715,-1.681920586548,3.32576064655821));
#7991=CARTESIAN_POINT('Ctrl Pts',(84.5165780687902,-1.35560569201204,3.47195643619301));
#7992=CARTESIAN_POINT('Ctrl Pts',(84.5077333314623,-1.18387272711435,3.53420240092095));
#7993=CARTESIAN_POINT('Ctrl Pts',(84.495049550665,-0.942379610003741,3.60214864544964));
#7994=CARTESIAN_POINT('Ctrl Pts',(84.4915396137813,-0.875983334028462,3.6188681460994));
#7995=CARTESIAN_POINT('Ctrl Pts',(84.4858251648387,-0.768918511081819,3.64270944419393));
#7996=CARTESIAN_POINT('Ctrl Pts',(84.483657040799,-0.728525712587216,3.65100231182728));
#7997=CARTESIAN_POINT('Ctrl Pts',(84.4790522000956,-0.643282253999308,3.66703235779608));
#7998=CARTESIAN_POINT('Ctrl Pts',(84.4766113261429,-0.598410965966305,3.67462140115184));
#7999=CARTESIAN_POINT('Ctrl Pts',(84.4705284982565,-0.487423821088916,3.69130580891148));
#8000=CARTESIAN_POINT('Ctrl Pts',(84.466858368709,-0.42118283945894,3.69944925677698));
#8001=CARTESIAN_POINT('Ctrl Pts',(84.4531900791189,-0.177205120738837,3.72280554141741));
#8002=CARTESIAN_POINT('Ctrl Pts',(84.4428817201986,0.00132491966660819,
3.72701880396594));
#8003=CARTESIAN_POINT('Ctrl Pts',(84.4176185516819,0.430872740884897,3.70628865224356));
#8004=CARTESIAN_POINT('Ctrl Pts',(84.4025389352714,0.680418579246505,3.66868710253756));
#8005=CARTESIAN_POINT('Ctrl Pts',(84.3857993442423,0.967871972903168,3.59501292163595));
#8006=CARTESIAN_POINT('Ctrl Pts',(84.3832908958218,1.0112747769779,3.58304587461003));
#8007=CARTESIAN_POINT('Ctrl Pts',(84.3793566383167,1.08007433714672,3.56272659308978));
#8008=CARTESIAN_POINT('Ctrl Pts',(84.3779054069339,1.10561575140774,3.55488329816625));
#8009=CARTESIAN_POINT('Ctrl Pts',(84.3750120735372,1.15692516796013,3.53852061059081));
#8010=CARTESIAN_POINT('Ctrl Pts',(84.3735704836368,1.18268877458042,3.52999310297551));
#8011=CARTESIAN_POINT('Ctrl Pts',(84.369666264972,1.25291181379502,3.50589480711796));
#8012=CARTESIAN_POINT('Ctrl Pts',(84.3672331218709,1.29717376505416,3.48976030941729));
#8013=CARTESIAN_POINT('Ctrl Pts',(84.3617017477928,1.39851141047655,3.45062580757112));
#8014=CARTESIAN_POINT('Ctrl Pts',(84.3586286512319,1.45534754903912,3.42704198262726));
#8015=CARTESIAN_POINT('Ctrl Pts',(84.3474319657509,1.66283855011653,3.33485127933889));
#8016=CARTESIAN_POINT('Ctrl Pts',(84.3395572551233,1.80945719461367,3.25762708242629));
#8017=CARTESIAN_POINT('Ctrl Pts',(84.3222785632027,2.11635843277074,3.06884879462024));
#8018=CARTESIAN_POINT('Ctrl Pts',(84.3128680198459,2.27398901790162,2.95394178383975));
#8019=CARTESIAN_POINT('Ctrl Pts',(84.2995485779715,2.47411337241145,2.78250926605326));
#8020=CARTESIAN_POINT('Ctrl Pts',(84.296024258384,2.52507775260058,2.7363436182026));
#8021=CARTESIAN_POINT('Ctrl Pts',(84.2900547733815,2.60784893114347,2.65708370246044));
#8022=CARTESIAN_POINT('Ctrl Pts',(84.2876417712766,2.6403753795398,2.62476426777186));
#8023=CARTESIAN_POINT('Ctrl Pts',(84.2827389293107,2.70454585537788,2.55860215444187));
#8024=CARTESIAN_POINT('Ctrl Pts',(84.2802489902953,2.73617154133603,2.52475311775694));
#8025=CARTESIAN_POINT('Ctrl Pts',(84.2738535020615,2.81492993130633,2.43723968187162));
#8026=CARTESIAN_POINT('Ctrl Pts',(84.2699130170268,2.86116356024535,2.38279456297719));
#8027=CARTESIAN_POINT('Ctrl Pts',(84.2610516127332,2.96010191291042,2.2592499810353));
#8028=CARTESIAN_POINT('Ctrl Pts',(84.2561055503558,3.01201010057387,2.18956787623521));
#8029=CARTESIAN_POINT('Ctrl Pts',(84.2384670572311,3.18596455336875,1.93814433452625));
#8030=CARTESIAN_POINT('Ctrl Pts',(84.2254299849798,3.29437700720137,1.74752503198462));
#8031=CARTESIAN_POINT('Ctrl Pts',(84.2050634053166,3.43866463914452,1.43207700898199));
#8032=CARTESIAN_POINT('Ctrl Pts',(84.197632015305,3.48588192004519,1.31297034717319));
#8033=CARTESIAN_POINT('Ctrl Pts',(84.1883292545763,3.53907756980524,1.15553096761608));
#8034=CARTESIAN_POINT('Ctrl Pts',(84.186218585374,3.55072936347778,1.11921538327329));
#8035=CARTESIAN_POINT('Ctrl Pts',(84.1827469091141,3.56923052915444,1.05835246769119));
#8036=CARTESIAN_POINT('Ctrl Pts',(84.1813699096741,3.5763894418461,1.03390290296337));
#8037=CARTESIAN_POINT('Ctrl Pts',(84.1784375573012,3.59125482878852,0.981130805707437));
#8038=CARTESIAN_POINT('Ctrl Pts',(84.1768865136219,3.5988782753272,0.952787579275031));
#8039=CARTESIAN_POINT('Ctrl Pts',(84.1722852675025,3.62072785824913,0.867546396624193));
#8040=CARTESIAN_POINT('Ctrl Pts',(84.1692846266782,3.63394601047137,0.810397464662491));
#8041=CARTESIAN_POINT('Ctrl Pts',(84.1621020064946,3.6628001218698,0.670686262505496));
#8042=CARTESIAN_POINT('Ctrl Pts',(84.1579720029296,3.6770024320648,0.587859811889969));
#8043=CARTESIAN_POINT('Ctrl Pts',(84.1467325117819,3.70836212673273,0.358644363935539));
#8044=CARTESIAN_POINT('Ctrl Pts',(84.139729669639,3.71965033175558,0.211609151992778));
#8045=CARTESIAN_POINT('Ctrl Pts',(84.124338503213,3.72518013950449,-0.108550759841699));
#8046=CARTESIAN_POINT('Ctrl Pts',(84.1159340985949,3.71612293617322,-0.28137920340409));
#8047=CARTESIAN_POINT('Ctrl Pts',(84.1037517379495,3.68681766587235,-0.520450600870952));
#8048=CARTESIAN_POINT('Ctrl Pts',(84.1002635525532,3.67669451779837,-0.587715945053337));
#8049=CARTESIAN_POINT('Ctrl Pts',(84.0945748802005,3.65749669436818,-0.695183219553958));
#8050=CARTESIAN_POINT('Ctrl Pts',(84.0924101336644,3.64958704759242,-0.735578673081256));
#8051=CARTESIAN_POINT('Ctrl Pts',(84.0878047246451,3.63151184317475,-0.82040612110599));
#8052=CARTESIAN_POINT('Ctrl Pts',(84.0853597564598,3.62119688769866,-0.864799008206719));
#8053=CARTESIAN_POINT('Ctrl Pts',(84.0792494618808,3.59367471008639,-0.97410381368601));
#8054=CARTESIAN_POINT('Ctrl Pts',(84.0755553717232,3.57552166738603,-1.03875896391701));
#8055=CARTESIAN_POINT('Ctrl Pts',(84.0617433431509,3.50217466392701,-1.27522498261098));
#8056=CARTESIAN_POINT('Ctrl Pts',(84.0513076660164,3.4362649717634,-1.44343236607213));
#8057=CARTESIAN_POINT('Ctrl Pts',(84.0261620472898,3.25166356077067,-1.82942232898161));
#8058=CARTESIAN_POINT('Ctrl Pts',(84.0113476991096,3.12290440216804,-2.04146461653696));
#8059=CARTESIAN_POINT('Ctrl Pts',(83.9947986877853,2.9465686835436,-2.27567326465751));
#8060=CARTESIAN_POINT('Ctrl Pts',(83.992250802565,2.91841143345712,-2.31167274615398));
#8061=CARTESIAN_POINT('Ctrl Pts',(83.9882700771743,2.87266631583368,-2.36799006048822));
#8062=CARTESIAN_POINT('Ctrl Pts',(83.9868108414173,2.85550974501347,-2.3886508491862));
#8063=CARTESIAN_POINT('Ctrl Pts',(83.9839162008507,2.82065474515235,-2.42971266479577));
#8064=CARTESIAN_POINT('Ctrl Pts',(83.9824810306217,2.80295490985435,-2.45011034154927));
#8065=CARTESIAN_POINT('Ctrl Pts',(83.9786184637149,2.75423620677078,-2.50503584506203));
#8066=CARTESIAN_POINT('Ctrl Pts',(83.9762194626911,2.72279029923352,-2.53917998995266));
#8067=CARTESIAN_POINT('Ctrl Pts',(83.9657025807219,2.58016693270706,-2.68834400357289));
#8068=CARTESIAN_POINT('Ctrl Pts',(83.9579573855615,2.46227521480837,-2.79672371871057));
#8069=CARTESIAN_POINT('Ctrl Pts',(83.9372898075075,2.12742924115124,-3.06691400402808));
#8070=CARTESIAN_POINT('Ctrl Pts',(83.9244850361729,1.8992498215517,-3.21321606987893));
#8071=CARTESIAN_POINT('Ctrl Pts',(83.9074654178086,1.59864549381558,-3.36266012016666));
#8072=CARTESIAN_POINT('Ctrl Pts',(83.9041022933889,1.53928811529006,-3.39024216673092));
#8073=CARTESIAN_POINT('Ctrl Pts',(83.8983470982289,1.43807697698841,-3.43406667482501));
#8074=CARTESIAN_POINT('Ctrl Pts',(83.8959829439032,1.39659974414915,-3.4511430345628));
#8075=CARTESIAN_POINT('Ctrl Pts',(83.8910911230138,1.31105541559054,-3.48456733821529));
#8076=CARTESIAN_POINT('Ctrl Pts',(83.888561483009,1.26696713146479,-3.50083845017561));
#8077=CARTESIAN_POINT('Ctrl Pts',(83.8819218464268,1.15169707818524,-3.54091708785826));
#8078=CARTESIAN_POINT('Ctrl Pts',(83.8777714063153,1.08008484838386,-3.5634134787781));
#8079=CARTESIAN_POINT('Ctrl Pts',(83.8620761086517,0.810961695344269,-3.63909843807001));
#8080=CARTESIAN_POINT('Ctrl Pts',(83.850130364349,0.609870390883411,-3.67814332495648));
#8081=CARTESIAN_POINT('Ctrl Pts',(83.8256650263185,0.197744638436171,-3.72342813404117));
#8082=CARTESIAN_POINT('Ctrl Pts',(83.813185547929,-0.0127021723266912,-3.72865502766819));
#8083=CARTESIAN_POINT('Ctrl Pts',(83.7988497881874,-0.266593216618914,-3.71345513873554));
#8084=CARTESIAN_POINT('Ctrl Pts',(83.7963887885953,-0.31066345018899,-3.71002824325117));
#8085=CARTESIAN_POINT('Ctrl Pts',(83.7925102324633,-0.381099794141748,-3.70328715616226));
#8086=CARTESIAN_POINT('Ctrl Pts',(83.7910684184602,-0.407508778907855,-3.70047422913305));
#8087=CARTESIAN_POINT('Ctrl Pts',(83.7881754169206,-0.461015345136506,-3.6941952474613));
#8088=CARTESIAN_POINT('Ctrl Pts',(83.7867250952236,-0.488109207155726,-3.69071309735153));
#8089=CARTESIAN_POINT('Ctrl Pts',(83.7827650493563,-0.562731015880428,-3.68028643574708));
#8090=CARTESIAN_POINT('Ctrl Pts',(83.7802862832299,-0.610167954686656,-3.67271968916089));
#8091=CARTESIAN_POINT('Ctrl Pts',(83.7746277565682,-0.719664287696303,-3.65307356352266));
#8092=CARTESIAN_POINT('Ctrl Pts',(83.7714748625238,-0.781589598965452,-3.64032711402842));
#8093=CARTESIAN_POINT('Ctrl Pts',(83.7597393768794,-1.01371713957767,-3.58635006999138));
#8094=CARTESIAN_POINT('Ctrl Pts',(83.7514299816506,-1.18126728001109,-3.53470531796971));
#8095=CARTESIAN_POINT('Ctrl Pts',(83.734262346508,-1.51474822161404,-3.40554144912009));
#8096=CARTESIAN_POINT('Ctrl Pts',(83.7254148637551,-1.67984427710116,-3.32720466609754));
#8097=CARTESIAN_POINT('Ctrl Pts',(83.7127286246209,-1.89803730029192,-3.20328063003238));
#8098=CARTESIAN_POINT('Ctrl Pts',(83.7092194914655,-1.9566075785217,-3.16784444675353));
#8099=CARTESIAN_POINT('Ctrl Pts',(83.7035068916617,-2.04882692839932,-3.10851643418255));
#8100=CARTESIAN_POINT('Ctrl Pts',(83.7013398295392,-2.08311454545353,-3.08564414963074));
#8101=CARTESIAN_POINT('Ctrl Pts',(83.6967378012349,-2.15442032686303,-3.03634789720623));
#8102=CARTESIAN_POINT('Ctrl Pts',(83.6942986904656,-2.19134800058597,-3.00980550749131));
#8103=CARTESIAN_POINT('Ctrl Pts',(83.6882217606141,-2.28118322692421,-2.94270517858672));
#8104=CARTESIAN_POINT('Ctrl Pts',(83.6845558307243,-2.3335038180017,-2.90139101944681));
#8105=CARTESIAN_POINT('Ctrl Pts',(83.6709156615242,-2.52133057801611,-2.74470852758297));
#8106=CARTESIAN_POINT('Ctrl Pts',(83.6606325783451,-2.64961333819856,-2.62108187054481));
#8107=CARTESIAN_POINT('Ctrl Pts',(83.6353445582929,-2.93740380228922,-2.30093834212829));
#8108=CARTESIAN_POINT('Ctrl Pts',(83.6202104524724,-3.08670336957429,-2.09640841368864));
#8109=CARTESIAN_POINT('Ctrl Pts',(83.6034323350909,-3.23678601111543,-1.83959163132951));
#8110=CARTESIAN_POINT('Ctrl Pts',(83.600932154433,-3.25872507627587,-1.80044224502325));
#8111=CARTESIAN_POINT('Ctrl Pts',(83.5970082250196,-3.29257027843675,-1.73740040696266));
#8112=CARTESIAN_POINT('Ctrl Pts',(83.5955592352651,-3.30493615877901,-1.71376086497502));
#8113=CARTESIAN_POINT('Ctrl Pts',(83.5926682289649,-3.32936576094034,-1.66581137076539));
#8114=CARTESIAN_POINT('Ctrl Pts',(83.5912267649167,-3.34141987400688,-1.64149846404188));
#8115=CARTESIAN_POINT('Ctrl Pts',(83.5873199974801,-3.37369151385901,-1.57457836004272));
#8116=CARTESIAN_POINT('Ctrl Pts',(83.5848842973406,-3.39336753313681,-1.53171427209088));
#8117=CARTESIAN_POINT('Ctrl Pts',(83.5793456764399,-3.43686380337712,-1.43200286514232));
#8118=CARTESIAN_POINT('Ctrl Pts',(83.576268019616,-3.46009776651618,-1.37491420388966));
#8119=CARTESIAN_POINT('Ctrl Pts',(83.5650427675964,-3.54065691283645,-1.16197483124453));
#8120=CARTESIAN_POINT('Ctrl Pts',(83.557145716562,-3.58895597481763,-1.00291394112117));
#8121=CARTESIAN_POINT('Ctrl Pts',(83.5398542127997,-3.67044132321864,-0.651605608013829));
#8122=CARTESIAN_POINT('Ctrl Pts',(83.5304535338369,-3.69947586432838,-0.458911618107906));
#8123=CARTESIAN_POINT('Ctrl Pts',(83.5171433971881,-3.71821063906794,-0.196235217835148));
#8124=CARTESIAN_POINT('Ctrl Pts',(83.5136177975025,-3.72120138402812,-0.127507387027372));
#8125=CARTESIAN_POINT('Ctrl Pts',(83.5076470622219,-3.72301000902447,-0.012894329024348));
#8126=CARTESIAN_POINT('Ctrl Pts',(83.5052341495047,-3.72288642235409,0.0329580629838045));
#8127=CARTESIAN_POINT('Ctrl Pts',(83.5003324123124,-3.72093596767528,0.125088397827464));
#8128=CARTESIAN_POINT('Ctrl Pts',(83.4978435081746,-3.71909233999502,0.171357784670287));
#8129=CARTESIAN_POINT('Ctrl Pts',(83.491452845202,-3.71221623529657,0.288805760694303));
#8130=CARTESIAN_POINT('Ctrl Pts',(83.4875162445366,-3.70599967245431,0.359893926441016));
#8131=CARTESIAN_POINT('Ctrl Pts',(83.478664832102,-3.68770504074861,0.516940606885447));
#8132=CARTESIAN_POINT('Ctrl Pts',(83.4737249643479,-3.67465587394784,0.60274272375685));
#8133=CARTESIAN_POINT('Ctrl Pts',(83.4561240780356,-3.61826802281,0.902597144908889));
#8134=CARTESIAN_POINT('Ctrl Pts',(83.4431202777285,-3.55911362452114,1.11321397400137));
#8135=CARTESIAN_POINT('Ctrl Pts',(83.4227559890907,-3.43637599911366,1.43760235292464));
#8136=CARTESIAN_POINT('Ctrl Pts',(83.4152964168224,-3.38470505817501,1.55536396712365));
#8137=CARTESIAN_POINT('Ctrl Pts',(83.4059646572083,-3.3099141267479,1.70434552948618));
#8138=CARTESIAN_POINT('Ctrl Pts',(83.4038515566164,-3.29226035821143,1.73820228088201));
#8139=CARTESIAN_POINT('Ctrl Pts',(83.400375277444,-3.26194459398117,1.79422296840556));
#8140=CARTESIAN_POINT('Ctrl Pts',(83.3989961122763,-3.24957023338223,1.81653847426224));
#8141=CARTESIAN_POINT('Ctrl Pts',(83.3960545490362,-3.2224056020191,1.8643601574954));
#8142=CARTESIAN_POINT('Ctrl Pts',(83.3944965561383,-3.20754028295992,1.88982065381401));
#8143=CARTESIAN_POINT('Ctrl Pts',(83.3898687214094,-3.16200993093883,1.96571731311643));
#8144=CARTESIAN_POINT('Ctrl Pts',(83.3868488959017,-3.13044526266745,2.01560524622334));
#8145=CARTESIAN_POINT('Ctrl Pts',(83.3712610487424,-2.95873247827631,2.27322601385967));
#8146=CARTESIAN_POINT('Ctrl Pts',(83.3595107797603,-2.79905425345494,2.46717808435461));
#8147=CARTESIAN_POINT('Ctrl Pts',(83.3474186374517,-2.62109006714222,2.6436252424329));
#8148=CARTESIAN_POINT('Ctrl Pts',(83.098469847874,-2.62118125581997,2.64353482796011));
#8149=CARTESIAN_POINT('Ctrl Pts',(83.1019574372931,-2.67139426381132,2.59374641815623));
#8150=CARTESIAN_POINT('Ctrl Pts',(83.1054855024516,-2.72017682180231,2.5425391353066));
#8151=CARTESIAN_POINT('Ctrl Pts',(83.1118033862382,-2.80360914658851,2.4498087036034));
#8152=CARTESIAN_POINT('Ctrl Pts',(83.1145701895591,-2.83886818604681,2.40886155681767));
#8153=CARTESIAN_POINT('Ctrl Pts',(83.1195489931295,-2.8999395055749,2.3347342098428));
#8154=CARTESIAN_POINT('Ctrl Pts',(83.1217471863391,-2.92610477278024,2.30185656464413));
#8155=CARTESIAN_POINT('Ctrl Pts',(83.1263428990979,-2.97912168747791,2.23287380698539));
#8156=CARTESIAN_POINT('Ctrl Pts',(83.1287431365892,-3.00588638764174,2.19671078212789));
#8157=CARTESIAN_POINT('Ctrl Pts',(83.1342900267089,-3.06560342990674,2.11288888582904));
#8158=CARTESIAN_POINT('Ctrl Pts',(83.1374519743175,-3.09811109853042,2.06492880281431));
#8159=CARTESIAN_POINT('Ctrl Pts',(83.148563313287,-3.20703996006023,1.89585531750673));
#8160=CARTESIAN_POINT('Ctrl Pts',(83.1567055502609,-3.27757770863589,1.77111562965551));
#8161=CARTESIAN_POINT('Ctrl Pts',(83.1805745818944,-3.45938957611759,1.40135064081698));
#8162=CARTESIAN_POINT('Ctrl Pts',(83.1966664659931,-3.55153455995938,1.14793606527946));
#8163=CARTESIAN_POINT('Ctrl Pts',(83.2154312749336,-3.62998102702292,0.828105769791334));
#8164=CARTESIAN_POINT('Ctrl Pts',(83.2188306246917,-3.64294917084279,0.769053639683291));
#8165=CARTESIAN_POINT('Ctrl Pts',(83.2238258012988,-3.66021377351113,0.68015377327869));
#8166=CARTESIAN_POINT('Ctrl Pts',(83.2254702006369,-3.6655949308124,0.650528970569234));
#8167=CARTESIAN_POINT('Ctrl Pts',(83.2284883555675,-3.67491787875769,0.595408655076993));
#8168=CARTESIAN_POINT('Ctrl Pts',(83.229866451666,-3.67895484388861,0.569933479859903));
#8169=CARTESIAN_POINT('Ctrl Pts',(83.2332792816183,-3.68838969010322,0.50611107267406));
#8170=CARTESIAN_POINT('Ctrl Pts',(83.2352971474211,-3.69345457936936,0.467718311521839));
#8171=CARTESIAN_POINT('Ctrl Pts',(83.2444837245172,-3.71403965283023,0.290382084915086));
#8172=CARTESIAN_POINT('Ctrl Pts',(83.2513439070078,-3.72232551954412,0.150702549098464));
#8173=CARTESIAN_POINT('Ctrl Pts',(83.2681919147471,-3.72334351390773,-0.197669853681005));
#8174=CARTESIAN_POINT('Ctrl Pts',(83.2780459464207,-3.70642792281704,-0.40589729167305));
#8175=CARTESIAN_POINT('Ctrl Pts',(83.292421391106,-3.65820856846187,-0.695409382260557));
#8176=CARTESIAN_POINT('Ctrl Pts',(83.2966342957239,-3.64138841968838,-0.778699848403936));
#8177=CARTESIAN_POINT('Ctrl Pts',(83.3044683116323,-3.60549424227617,-0.929626687793152));
#8178=CARTESIAN_POINT('Ctrl Pts',(83.3080633501534,-3.58732638734039,-0.997438277824222));
#8179=CARTESIAN_POINT('Ctrl Pts',(83.314110590084,-3.55410677265165,-1.10874054839327));
#8180=CARTESIAN_POINT('Ctrl Pts',(83.3165284428942,-3.54014600293421,-1.15253919173449));
#8181=CARTESIAN_POINT('Ctrl Pts',(83.3214072886937,-3.51066315906593,-1.23943916059089));
#8182=CARTESIAN_POINT('Ctrl Pts',(83.3238676693217,-3.49514942245258,-1.2825348000298));
#8183=CARTESIAN_POINT('Ctrl Pts',(83.3301111863393,-3.45420154760582,-1.3900182892505));
#8184=CARTESIAN_POINT('Ctrl Pts',(83.333926226665,-3.42775991629598,-1.45400146985651));
#8185=CARTESIAN_POINT('Ctrl Pts',(83.3507392181853,-3.30519712661945,-1.72862338649515));
#8186=CARTESIAN_POINT('Ctrl Pts',(83.3643000622881,-3.19133799317504,-1.93075235536862));
#8187=CARTESIAN_POINT('Ctrl Pts',(83.3863460441463,-2.97886377352015,-2.23724221252285));
#8188=CARTESIAN_POINT('Ctrl Pts',(83.3947256290841,-2.89169761274429,-2.34882298150625));
#8189=CARTESIAN_POINT('Ctrl Pts',(83.4061974553829,-2.760946539539,-2.49785211217532));
#8190=CARTESIAN_POINT('Ctrl Pts',(83.4094494683065,-2.72253007393496,-2.53966956415872));
#8191=CARTESIAN_POINT('Ctrl Pts',(83.4151561746597,-2.65239991395943,-2.61258735767042));
#8192=CARTESIAN_POINT('Ctrl Pts',(83.4176295487401,-2.62105805935229,-2.6440296887582));
#8193=CARTESIAN_POINT('Ctrl Pts',(83.4215150864135,-2.57015340313916,-2.69330257512577));
#8194=CARTESIAN_POINT('Ctrl Pts',(83.4229520449323,-2.55095057477377,-2.71149747168903));
#8195=CARTESIAN_POINT('Ctrl Pts',(83.425816422974,-2.51186452435651,-2.74774915063062));
#8196=CARTESIAN_POINT('Ctrl Pts',(83.4272433384157,-2.49197664028869,-2.76579849128174));
#8197=CARTESIAN_POINT('Ctrl Pts',(83.4311030039209,-2.43710763392315,-2.81452275537215));
#8198=CARTESIAN_POINT('Ctrl Pts',(83.4335068401291,-2.40174315669938,-2.84476047159436));
#8199=CARTESIAN_POINT('Ctrl Pts',(83.4448235231234,-2.23020048565785,-2.98595484667776));
#8200=CARTESIAN_POINT('Ctrl Pts',(83.4532786251432,-2.08683938004369,-3.08785232799685));
#8201=CARTESIAN_POINT('Ctrl Pts',(83.4729921981318,-1.73555161988876,-3.30185778333071));
#8202=CARTESIAN_POINT('Ctrl Pts',(83.4842041296979,-1.523112111121,-3.40507356551663));
#8203=CARTESIAN_POINT('Ctrl Pts',(83.4997954177205,-1.23264609126699,-3.51354357105568));
#8204=CARTESIAN_POINT('Ctrl Pts',(83.5035931954064,-1.16217390122115,-3.53747872251818));
#8205=CARTESIAN_POINT('Ctrl Pts',(83.5098753902681,-1.04652385111574,-3.57292915595346));
#8206=CARTESIAN_POINT('Ctrl Pts',(83.5123186107983,-1.00176250625304,-3.58573654238083));
#8207=CARTESIAN_POINT('Ctrl Pts',(83.517142338507,-0.91390086306699,-3.60910250353065));
#8208=CARTESIAN_POINT('Ctrl Pts',(83.5195199898844,-0.87082865412088,-3.6197365781609));
#8209=CARTESIAN_POINT('Ctrl Pts',(83.5254148154727,-0.764678367436689,-3.64393970715429));
#8210=CARTESIAN_POINT('Ctrl Pts',(83.5289580955598,-0.70141954670096,-3.65664320313402));
#8211=CARTESIAN_POINT('Ctrl Pts',(83.5479238615281,-0.365804543954081,-3.71501147973908));
#8212=CARTESIAN_POINT('Ctrl Pts',(83.5642139243494,-0.0893565686471371,
-3.73190275534186));
#8213=CARTESIAN_POINT('Ctrl Pts',(83.5898004013558,0.343430837968755,-3.71020935333544));
#8214=CARTESIAN_POINT('Ctrl Pts',(83.5990423818078,0.499847423044,-3.69239179482749));
#8215=CARTESIAN_POINT('Ctrl Pts',(83.6105203297548,0.699897332124375,-3.65665441007835));
#8216=CARTESIAN_POINT('Ctrl Pts',(83.613082837461,0.744966860825984,-3.64773936833899));
#8217=CARTESIAN_POINT('Ctrl Pts',(83.6170720108416,0.815994442913929,-3.63231823246569));
#8218=CARTESIAN_POINT('Ctrl Pts',(83.618525703413,0.842066165854466,-3.6263628257679));
#8219=CARTESIAN_POINT('Ctrl Pts',(83.6214004812374,0.89406154780247,-3.61389482242231));
#8220=CARTESIAN_POINT('Ctrl Pts',(83.6228215560301,0.919983667154045,-3.60738298162023));
#8221=CARTESIAN_POINT('Ctrl Pts',(83.6266150080844,0.989681143346163,-3.58907425670544));
#8222=CARTESIAN_POINT('Ctrl Pts',(83.628960595293,1.0333159162256,-3.57675570138799));
#8223=CARTESIAN_POINT('Ctrl Pts',(83.6414295033508,1.26726159059395,-3.50607151516963));
#8224=CARTESIAN_POINT('Ctrl Pts',(83.6509518726035,1.45289962882292,-3.43330539136195));
#8225=CARTESIAN_POINT('Ctrl Pts',(83.6681803098899,1.77605319751593,-3.27570547661866));
#8226=CARTESIAN_POINT('Ctrl Pts',(83.6758611411785,1.91556437078074,-3.19612605474789));
#8227=CARTESIAN_POINT('Ctrl Pts',(83.6874804758913,2.11227274049254,-3.0664026497785));
#8228=CARTESIAN_POINT('Ctrl Pts',(83.6912346145942,2.17377257973285,-3.02311648994599));
#8229=CARTESIAN_POINT('Ctrl Pts',(83.6983168891236,2.28540184073791,-2.93937887298271));
#8230=CARTESIAN_POINT('Ctrl Pts',(83.7016271970787,2.33587384168366,-2.89943141161603));
#8231=CARTESIAN_POINT('Ctrl Pts',(83.7073396816165,2.41987311922688,-2.82933055505599));
#8232=CARTESIAN_POINT('Ctrl Pts',(83.7097158835423,2.45393504357483,-2.79983925849361));
#8233=CARTESIAN_POINT('Ctrl Pts',(83.7146355616783,2.52261031264785,-2.73816321795688));
#8234=CARTESIAN_POINT('Ctrl Pts',(83.7171810826185,2.55716264979442,-2.70592304127606));
#8235=CARTESIAN_POINT('Ctrl Pts',(83.7239392847304,2.64629262550365,-2.61952541337996));
#8236=CARTESIAN_POINT('Ctrl Pts',(83.7281952601577,2.69982054700934,-2.56432172474487));
#8237=CARTESIAN_POINT('Ctrl Pts',(83.7499826356791,2.96089874615753,-2.27782858776448));
#8238=CARTESIAN_POINT('Ctrl Pts',(83.7685664557161,3.14060217549853,-2.02286790716614));
#8239=CARTESIAN_POINT('Ctrl Pts',(83.7913395222776,3.32348096114568,-1.67914658047097));
#8240=CARTESIAN_POINT('Ctrl Pts',(83.7959013647612,3.35823024278104,-1.6085240608104));
#8241=CARTESIAN_POINT('Ctrl Pts',(83.8035730927915,3.41385405435936,-1.48580257627947));
#8242=CARTESIAN_POINT('Ctrl Pts',(83.8067219968625,3.43583708250895,-1.43423602341418));
#8243=CARTESIAN_POINT('Ctrl Pts',(83.8114037481945,3.46736274461901,-1.3553951230656));
#8244=CARTESIAN_POINT('Ctrl Pts',(83.8129792869184,3.47776559100389,-1.32847542011444));
#8245=CARTESIAN_POINT('Ctrl Pts',(83.8159006747901,3.49668773279909,-1.27776401491703));
#8246=CARTESIAN_POINT('Ctrl Pts',(83.8172501709169,3.50527947070012,-1.25400232286149));
#8247=CARTESIAN_POINT('Ctrl Pts',(83.8206378283228,3.52644405165829,-1.19355098730942));
#8248=CARTESIAN_POINT('Ctrl Pts',(83.8226583233178,3.53868700655612,-1.15674807351858));
#8249=CARTESIAN_POINT('Ctrl Pts',(83.832175310705,3.59433678777667,-0.980302663840718));
#8250=CARTESIAN_POINT('Ctrl Pts',(83.8393301461734,3.63006939470891,-0.838363577227186));
#8251=CARTESIAN_POINT('Ctrl Pts',(83.8591030060327,3.70652575609342,-0.43583518847978));
#8252=CARTESIAN_POINT('Ctrl Pts',(83.8714977090779,3.72807209196568,-0.172514621926704));
#8253=CARTESIAN_POINT('Ctrl Pts',(83.8888317027794,3.71960678134602,0.174170126791537));
#8254=CARTESIAN_POINT('Ctrl Pts',(83.8930627672214,3.71477717642392,0.257369625331266));
#8255=CARTESIAN_POINT('Ctrl Pts',(83.8998792990313,3.70274152684063,0.388470659618078));
#8256=CARTESIAN_POINT('Ctrl Pts',(83.9024091253234,3.69738531732284,0.436515523721091));
#8257=CARTESIAN_POINT('Ctrl Pts',(83.9073165782005,3.68532016697538,0.528443356015807));
#8258=CARTESIAN_POINT('Ctrl Pts',(83.9096892948221,3.67875885246777,0.572337480869173));
#8259=CARTESIAN_POINT('Ctrl Pts',(83.9153561201397,3.66139506238959,0.675809973773638));
#8260=CARTESIAN_POINT('Ctrl Pts',(83.9186702680425,3.64992094283978,0.735261488809868));
#8261=CARTESIAN_POINT('Ctrl Pts',(83.9321545299543,3.5980313441256,0.972826353178651));
#8262=CARTESIAN_POINT('Ctrl Pts',(83.9426699958443,3.54598801609364,1.14811863760818));
#8263=CARTESIAN_POINT('Ctrl Pts',(83.9644612541729,3.41438841777966,1.4954905599786));
#8264=CARTESIAN_POINT('Ctrl Pts',(83.9757187198851,3.33413283906783,1.66676284064558));
#8265=CARTESIAN_POINT('Ctrl Pts',(83.9905065180707,3.20904654541324,1.88816522702087));
#8266=CARTESIAN_POINT('Ctrl Pts',(83.9942737545092,3.17536818971835,1.94426984887022));
#8267=CARTESIAN_POINT('Ctrl Pts',(84.0007659516136,3.11380640399068,2.04095495915585));
#8268=CARTESIAN_POINT('Ctrl Pts',(84.0035169292162,3.08656435114939,2.08192421076682));
#8269=CARTESIAN_POINT('Ctrl Pts',(84.0077316415476,3.04285854452846,2.14490881709202));
#8270=CARTESIAN_POINT('Ctrl Pts',(84.0092270970168,3.02695028868626,2.16730108620656));
#8271=CARTESIAN_POINT('Ctrl Pts',(84.0121155207422,2.99539878649255,2.21068743945296));
#8272=CARTESIAN_POINT('Ctrl Pts',(84.0135096803278,2.97977931604068,2.2316962412152));
#8273=CARTESIAN_POINT('Ctrl Pts',(84.0171429198265,2.93808905233098,2.2865531897942));
#8274=CARTESIAN_POINT('Ctrl Pts',(84.0193589832969,2.91165415692369,2.3201213619577));
#8275=CARTESIAN_POINT('Ctrl Pts',(84.0331645001209,2.74112215983529,2.52916375302575));
#8276=CARTESIAN_POINT('Ctrl Pts',(84.043938514612,2.58178926431126,2.69161738540142));
#8277=CARTESIAN_POINT('Ctrl Pts',(84.0640354844138,2.26206594690381,2.96291647623786));
#8278=CARTESIAN_POINT('Ctrl Pts',(84.0732971670363,2.10609487571415,3.07573956171173));
#8279=CARTESIAN_POINT('Ctrl Pts',(84.0866913559062,1.87902215522718,3.21459380845086));
#8280=CARTESIAN_POINT('Ctrl Pts',(84.0904684399076,1.81479155741648,3.25128717766199));
#8281=CARTESIAN_POINT('Ctrl Pts',(84.0967333798635,1.70836221644715,3.30795095421422));
#8282=CARTESIAN_POINT('Ctrl Pts',(84.099181069804,1.66680456630133,3.32908444794027));
#8283=CARTESIAN_POINT('Ctrl Pts',(84.1040267765092,1.5846661436843,3.36893109695096));
#8284=CARTESIAN_POINT('Ctrl Pts',(84.106422208452,1.54412359661742,3.38770506523166));
#8285=CARTESIAN_POINT('Ctrl Pts',(84.1123890302334,1.44334814511332,3.43218612408494));
#8286=CARTESIAN_POINT('Ctrl Pts',(84.1159875648216,1.38275769995227,3.45704149152967));
#8287=CARTESIAN_POINT('Ctrl Pts',(84.1346231266302,1.07004593541259,3.57578547106133));
#8288=CARTESIAN_POINT('Ctrl Pts',(84.1504697163957,0.808964811985726,3.64373144742515));
#8289=CARTESIAN_POINT('Ctrl Pts',(84.1733607915825,0.425332188804449,3.70028102280097));
#8290=CARTESIAN_POINT('Ctrl Pts',(84.1803548463131,0.307009869683719,3.71197174011133));
#8291=CARTESIAN_POINT('Ctrl Pts',(84.1901691407294,0.136813023962568,3.72059273318745));
#8292=CARTESIAN_POINT('Ctrl Pts',(84.1931099819025,0.0852480139100827,3.72213128235171));
#8293=CARTESIAN_POINT('Ctrl Pts',(84.1983339857973,-0.00770359895059893,
3.72297190193208));
#8294=CARTESIAN_POINT('Ctrl Pts',(84.2006317234332,-0.0490780697114772,
3.7226564105393));
#8295=CARTESIAN_POINT('Ctrl Pts',(84.2043143133982,-0.116360698631534,3.72102136698503));
#8296=CARTESIAN_POINT('Ctrl Pts',(84.2057196035041,-0.142274944869516,3.72012066996029));
#8297=CARTESIAN_POINT('Ctrl Pts',(84.2086055589493,-0.196043761138974,3.7176891255887));
#8298=CARTESIAN_POINT('Ctrl Pts',(84.2100840944507,-0.223894252864475,3.71611585521241));
#8299=CARTESIAN_POINT('Ctrl Pts',(84.2142380780444,-0.302891348751411,3.7107619683436));
#8300=CARTESIAN_POINT('Ctrl Pts',(84.2168772113505,-0.353982673149821,3.70623721594947));
#8301=CARTESIAN_POINT('Ctrl Pts',(84.2312323793825,-0.635473455039668,3.67543341903601));
#8302=CARTESIAN_POINT('Ctrl Pts',(84.2421805545492,-0.86313900884722,3.62872521974366));
#8303=CARTESIAN_POINT('Ctrl Pts',(84.2628928456695,-1.27586437786784,3.50297750772648));
#8304=CARTESIAN_POINT('Ctrl Pts',(84.272575472588,-1.46173922906316,3.42957582697454));
#8305=CARTESIAN_POINT('Ctrl Pts',(84.2858448571129,-1.69572079643334,3.31468530409074));
#8306=CARTESIAN_POINT('Ctrl Pts',(84.2889984231363,-1.74994183526802,3.28638261928115));
#8307=CARTESIAN_POINT('Ctrl Pts',(84.2945241585787,-1.84235607058178,3.23520796849765));
#8308=CARTESIAN_POINT('Ctrl Pts',(84.296874523898,-1.88088225065286,3.21296253094685));
#8309=CARTESIAN_POINT('Ctrl Pts',(84.3018192865424,-1.9602531737934,3.16521607253678));
#8310=CARTESIAN_POINT('Ctrl Pts',(84.3044173862902,-2.00102017821013,3.13960240254245));
#8311=CARTESIAN_POINT('Ctrl Pts',(84.3115244655315,-2.10996688056973,3.06816785156896));
#8312=CARTESIAN_POINT('Ctrl Pts',(84.3160856508743,-2.17714262819681,3.02087119439549));
#8313=CARTESIAN_POINT('Ctrl Pts',(84.3301561047506,-2.37617875549688,2.87064624215964));
#8314=CARTESIAN_POINT('Ctrl Pts',(84.3398805274516,-2.50259335409639,2.76111451017243));
#8315=CARTESIAN_POINT('Ctrl Pts',(84.3497092098018,-2.62112000711955,2.64359555733807));
#8316=CARTESIAN_POINT('Origin',(80.1322559480305,0.,0.));
#8317=CARTESIAN_POINT('',(85.8498933978656,-2.62112000702085,2.64359555743594));
#8318=CARTESIAN_POINT('',(85.6021262425917,-2.62112000711956,2.64359555733807));
#8319=CARTESIAN_POINT('',(80.1322559480305,-2.62112000711956,2.64359555733806));
#8320=CARTESIAN_POINT('Ctrl Pts',(85.8498933978656,-2.62112000692213,2.64359555753381));
#8321=CARTESIAN_POINT('Ctrl Pts',(85.8494125170131,-2.61469984289228,2.64996113805479));
#8322=CARTESIAN_POINT('Ctrl Pts',(85.848930638563,-2.60825646309207,2.65630335745762));
#8323=CARTESIAN_POINT('Ctrl Pts',(85.8458489244465,-2.56698787681799,2.69662909322084));
#8324=CARTESIAN_POINT('Ctrl Pts',(85.8432214558479,-2.53152355325839,2.72994934463062));
#8325=CARTESIAN_POINT('Ctrl Pts',(85.8359658805799,-2.43289520025543,2.81904010183764));
#8326=CARTESIAN_POINT('Ctrl Pts',(85.8312820259721,-2.36847745694498,2.87337417914566));
#8327=CARTESIAN_POINT('Ctrl Pts',(85.8114075654775,-2.09206654338741,3.0909027254847));
#8328=CARTESIAN_POINT('Ctrl Pts',(85.7955078393622,-1.86465625620216,3.23317943974336));
#8329=CARTESIAN_POINT('Ctrl Pts',(85.7714640352237,-1.49698235157898,3.41142758188823));
#8330=CARTESIAN_POINT('Ctrl Pts',(85.7632386578215,-1.36655037002493,3.46573806784839));
#8331=CARTESIAN_POINT('Ctrl Pts',(85.7531613681591,-1.19681762385791,3.52533594169434));
#8332=CARTESIAN_POINT('Ctrl Pts',(85.7510176185441,-1.16009569840774,3.53759015870344));
#8333=CARTESIAN_POINT('Ctrl Pts',(85.7475218576749,-1.09905520104518,3.55690679375909));
#8334=CARTESIAN_POINT('Ctrl Pts',(85.7461528219742,-1.07484430080951,3.56429770612739));
#8335=CARTESIAN_POINT('Ctrl Pts',(85.7432467446201,-1.02275182575708,3.57962098079737));
#8336=CARTESIAN_POINT('Ctrl Pts',(85.7417137672106,-0.994849938315332,3.58747562620802));
#8337=CARTESIAN_POINT('Ctrl Pts',(85.7372324883483,-0.91215881927862,3.6097149890045));
#8338=CARTESIAN_POINT('Ctrl Pts',(85.7343299480101,-0.857128003499739,3.62317653763189));
#8339=CARTESIAN_POINT('Ctrl Pts',(85.7274451946642,-0.72383229217003,3.65257587181262));
#8340=CARTESIAN_POINT('Ctrl Pts',(85.7235093567469,-0.645319034498762,3.66726166851202));
#8341=CARTESIAN_POINT('Ctrl Pts',(85.7121565910508,-0.414874513080685,3.702735200961));
#8342=CARTESIAN_POINT('Ctrl Pts',(85.7048734474978,-0.262059085519863,3.71667807391622));
#8343=CARTESIAN_POINT('Ctrl Pts',(85.6891413858099,0.0651469335017609,3.72624645831691));
#8344=CARTESIAN_POINT('Ctrl Pts',(85.6806827925711,0.239242970623695,3.71912800363517));
#8345=CARTESIAN_POINT('Ctrl Pts',(85.6684389236575,0.479841091312247,3.69232355566699));
#8346=CARTESIAN_POINT('Ctrl Pts',(85.6649480762204,0.547267475627297,3.68293338267451));
#8347=CARTESIAN_POINT('Ctrl Pts',(85.6592561784775,0.655002594250469,3.66490575877121));
#8348=CARTESIAN_POINT('Ctrl Pts',(85.657090943282,0.695492456425876,3.65743799486478));
#8349=CARTESIAN_POINT('Ctrl Pts',(85.6524853710776,0.78051783154468,3.64029338067007));
#8350=CARTESIAN_POINT('Ctrl Pts',(85.6500407449869,0.825015984046235,3.63046723746266));
#8351=CARTESIAN_POINT('Ctrl Pts',(85.6439332360755,0.934568833930955,3.60415752059903));
#8352=CARTESIAN_POINT('Ctrl Pts',(85.6402416538428,0.999377687447366,3.58672744926182));
#8353=CARTESIAN_POINT('Ctrl Pts',(85.6320561514306,1.13999146076088,3.54480303657727));
#8354=CARTESIAN_POINT('Ctrl Pts',(85.627543126425,1.2155518562535,3.51960816103044));
#8355=CARTESIAN_POINT('Ctrl Pts',(85.6126327662345,1.45916514393167,3.42959689751849));
#8356=CARTESIAN_POINT('Ctrl Pts',(85.6020007604734,1.62332641356021,3.35501140305426));
#8357=CARTESIAN_POINT('Ctrl Pts',(85.5814805775996,1.9285001938464,3.18869978857847));
#8358=CARTESIAN_POINT('Ctrl Pts',(85.5716190086118,2.06999904301061,3.09871431574759));
#8359=CARTESIAN_POINT('Ctrl Pts',(85.5595587943745,2.24207856363626,2.97221687858598));
#8360=CARTESIAN_POINT('Ctrl Pts',(85.5569896523303,2.27868544882367,2.94424565178728));
#8361=CARTESIAN_POINT('Ctrl Pts',(85.5529839106082,2.33585425333259,2.89885797228623));
#8362=CARTESIAN_POINT('Ctrl Pts',(85.551520386193,2.3567615918942,2.88188610521399));
#8363=CARTESIAN_POINT('Ctrl Pts',(85.548626061652,2.39819523930739,2.84749918324306));
#8364=CARTESIAN_POINT('Ctrl Pts',(85.5471953359125,2.41872051101255,2.8300853662804));
#8365=CARTESIAN_POINT('Ctrl Pts',(85.5433579601725,2.47381222978146,2.78230788623128));
#8366=CARTESIAN_POINT('Ctrl Pts',(85.5409791056765,2.50800849753616,2.75152282512411));
#8367=CARTESIAN_POINT('Ctrl Pts',(85.5306611561757,2.65588727662079,2.61334731541808));
#8368=CARTESIAN_POINT('Ctrl Pts',(85.5230790029957,2.76331656160075,2.49948204970793));
#8369=CARTESIAN_POINT('Ctrl Pts',(85.5022716823158,3.04002209971218,2.16647654460748));
#8370=CARTESIAN_POINT('Ctrl Pts',(85.4891887234473,3.19250624773465,1.93474797903165));
#8371=CARTESIAN_POINT('Ctrl Pts',(85.47187909144,3.34722883231301,1.63067569173227));
#8372=CARTESIAN_POINT('Ctrl Pts',(85.4685559607044,3.37503078443024,1.57232650732821));
#8373=CARTESIAN_POINT('Ctrl Pts',(85.4628483876903,3.41947367458326,1.47243552564367));
#8374=CARTESIAN_POINT('Ctrl Pts',(85.4604907503854,3.43691039258298,1.43126283925748));
#8375=CARTESIAN_POINT('Ctrl Pts',(85.4555942130232,3.47121720066883,1.34601092392358));
#8376=CARTESIAN_POINT('Ctrl Pts',(85.4530529585128,3.48799901786943,1.3019050804367));
#8377=CARTESIAN_POINT('Ctrl Pts',(85.4463380125565,3.52967032443349,1.18579024169859));
#8378=CARTESIAN_POINT('Ctrl Pts',(85.4421220719284,3.55319479678375,1.11331787986404));
#8379=CARTESIAN_POINT('Ctrl Pts',(85.4278154477226,3.62433610764735,0.868847195429822));
#8380=CARTESIAN_POINT('Ctrl Pts',(85.4174411252539,3.66180633316773,0.694169327647438));
#8381=CARTESIAN_POINT('Ctrl Pts',(85.392834817163,3.71988818380175,0.280396791140727));
#8382=CARTESIAN_POINT('Ctrl Pts',(85.3785385963413,3.73022116305746,0.0406324526124812));
#8383=CARTESIAN_POINT('Ctrl Pts',(85.3627570454361,3.71524903407227,-0.239802779125859));
#8384=CARTESIAN_POINT('Ctrl Pts',(85.3604583895618,3.71235311686573,-0.2810967342461));
#8385=CARTESIAN_POINT('Ctrl Pts',(85.3569101481204,3.70673782055373,-0.345705942664832));
#8386=CARTESIAN_POINT('Ctrl Pts',(85.3556376312755,3.70448572726458,-0.369057498967059));
#8387=CARTESIAN_POINT('Ctrl Pts',(85.3529187102068,3.69915127052956,-0.419385949559535));
#8388=CARTESIAN_POINT('Ctrl Pts',(85.3514764436293,3.6959942124392,-0.446353634928199));
#8389=CARTESIAN_POINT('Ctrl Pts',(85.3475682323122,3.6865454812577,-0.520072064656115));
#8390=CARTESIAN_POINT('Ctrl Pts',(85.3451318726982,3.67965970188688,-0.566742798567036));
#8391=CARTESIAN_POINT('Ctrl Pts',(85.3395916196952,3.66173418236234,-0.67406957710873));
#8392=CARTESIAN_POINT('Ctrl Pts',(85.3365129764802,3.65007103625863,-0.734608099702717));
#8393=CARTESIAN_POINT('Ctrl Pts',(85.3252800496085,3.60143289824589,-0.957161605531159));
#8394=CARTESIAN_POINT('Ctrl Pts',(85.3173762286619,3.55512653095226,-1.11694094788216));
#8395=CARTESIAN_POINT('Ctrl Pts',(85.3001054729591,3.43197222325973,-1.45535231424623));
#8396=CARTESIAN_POINT('Ctrl Pts',(85.2907327447734,3.35150841610452,-1.63213579751016));
#8397=CARTESIAN_POINT('Ctrl Pts',(85.2774557845002,3.22437572336044,-1.86198650195114));
#8398=CARTESIAN_POINT('Ctrl Pts',(85.2739322505664,3.18944771647931,-1.92120146302668));
#8399=CARTESIAN_POINT('Ctrl Pts',(85.2679636185365,3.12852335138933,-2.01824462694814));
#8400=CARTESIAN_POINT('Ctrl Pts',(85.2655506569088,3.10343033216894,-2.05662093359418));
#8401=CARTESIAN_POINT('Ctrl Pts',(85.2606475000304,3.05157019674382,-2.13282282073475));
#8402=CARTESIAN_POINT('Ctrl Pts',(85.2581571972093,3.02479292215194,-2.17063155993647));
#8403=CARTESIAN_POINT('Ctrl Pts',(85.2517598674181,2.95494613498814,-2.26545026047953));
#8404=CARTESIAN_POINT('Ctrl Pts',(85.2478178692362,2.91092957298447,-2.32173633867774));
#8405=CARTESIAN_POINT('Ctrl Pts',(85.2389523616222,2.80983480212235,-2.44361409664144));
#8406=CARTESIAN_POINT('Ctrl Pts',(85.2340036726254,2.75202409473727,-2.50854208009891));
#8407=CARTESIAN_POINT('Ctrl Pts',(85.2163467432131,2.54063045074661,-2.72985128265229));
#8408=CARTESIAN_POINT('Ctrl Pts',(85.2032930595409,2.37557168357753,-2.87463741791466));
#8409=CARTESIAN_POINT('Ctrl Pts',(85.1829314575854,2.0957060539676,-3.0794790603545));
#8410=CARTESIAN_POINT('Ctrl Pts',(85.1755199210211,1.98883749589948,-3.14955637642131));
#8411=CARTESIAN_POINT('Ctrl Pts',(85.1662368712596,1.84566411464876,-3.23324053975189));
#8412=CARTESIAN_POINT('Ctrl Pts',(85.1641273102985,1.81246198865685,-3.251968969095));
#8413=CARTESIAN_POINT('Ctrl Pts',(85.1606567965932,1.75660000656033,-3.28235782376432));
#8414=CARTESIAN_POINT('Ctrl Pts',(85.1592798801226,1.73409807999328,-3.29430120837918));
#8415=CARTESIAN_POINT('Ctrl Pts',(85.1563468197092,1.68539689389447,-3.31951308348748));
#8416=CARTESIAN_POINT('Ctrl Pts',(85.1547950039741,1.65916044506543,-3.33270408642881));
#8417=CARTESIAN_POINT('Ctrl Pts',(85.1501892710288,1.57999965504103,-3.37133750985229));
#8418=CARTESIAN_POINT('Ctrl Pts',(85.1471850461975,1.52662484611578,-3.39584051165289));
#8419=CARTESIAN_POINT('Ctrl Pts',(85.1399914619228,1.39539554547256,-3.45236465512013));
#8420=CARTESIAN_POINT('Ctrl Pts',(85.1358542780704,1.31699061623288,-3.48302848252433));
#8421=CARTESIAN_POINT('Ctrl Pts',(85.1160885191838,0.933256155186663,-3.61829266248534));
#8422=CARTESIAN_POINT('Ctrl Pts',(85.1010738685198,0.616260085628715,-3.68554414692541));
#8423=CARTESIAN_POINT('Ctrl Pts',(85.081350024612,0.227926993657657,-3.71636710174803));
#8424=CARTESIAN_POINT('Ctrl Pts',(85.077918962509,0.161169024941091,-3.71986007912614));
#8425=CARTESIAN_POINT('Ctrl Pts',(85.0720841124354,0.0492997851185086,-3.7226963920056));
#8426=CARTESIAN_POINT('Ctrl Pts',(85.0697102245506,0.00422829001023111,
-3.72302038483258));
#8427=CARTESIAN_POINT('Ctrl Pts',(85.0648293658586,-0.0874645238974345,
-3.72201449902313));
#8428=CARTESIAN_POINT('Ctrl Pts',(85.0623210719823,-0.134077060391818,-3.72062697016497));
#8429=CARTESIAN_POINT('Ctrl Pts',(85.0558113694728,-0.253683240855003,-3.71481612436998));
#8430=CARTESIAN_POINT('Ctrl Pts',(85.0517724667302,-0.326592447976102,-3.70911719869889));
#8431=CARTESIAN_POINT('Ctrl Pts',(85.0426394390116,-0.488565500018144,-3.69164399480658));
#8432=CARTESIAN_POINT('Ctrl Pts',(85.0375175152443,-0.577465003052578,-3.67878569470495));
#8433=CARTESIAN_POINT('Ctrl Pts',(85.0185665105707,-0.900075554077878,-3.62014172629223));
#8434=CARTESIAN_POINT('Ctrl Pts',(85.0043302629778,-1.1297127158424,-3.55517940493527));
#8435=CARTESIAN_POINT('Ctrl Pts',(84.9842332141465,-1.4503747442406,-3.43023749896758));
#8436=CARTESIAN_POINT('Ctrl Pts',(84.9781221854952,-1.54751443310165,-3.38752393648964));
#8437=CARTESIAN_POINT('Ctrl Pts',(84.9701580250113,-1.67545841412428,-3.32461110105688));
#8438=CARTESIAN_POINT('Ctrl Pts',(84.968141643808,-1.70797605986298,-3.30802325402185));
#8439=CARTESIAN_POINT('Ctrl Pts',(84.9647759067646,-1.76257341524357,-3.27915239787956));
#8440=CARTESIAN_POINT('Ctrl Pts',(84.9634127364409,-1.78478089016087,-3.26711842327509));
#8441=CARTESIAN_POINT('Ctrl Pts',(84.9604507297425,-1.83326785476274,-3.2402019091442));
#8442=CARTESIAN_POINT('Ctrl Pts',(84.9588574872331,-1.85949136645593,-3.22522424250651));
#8443=CARTESIAN_POINT('Ctrl Pts',(84.9539690640011,-1.94025208888828,-3.1777849298484));
#8444=CARTESIAN_POINT('Ctrl Pts',(84.9507330862616,-1.9941456363019,-3.14424541855897));
#8445=CARTESIAN_POINT('Ctrl Pts',(84.9428113759774,-2.12608845886024,-3.05737567525781));
#8446=CARTESIAN_POINT('Ctrl Pts',(84.9381929119439,-2.20301528826141,-3.00241959153895));
#8447=CARTESIAN_POINT('Ctrl Pts',(84.9185678173305,-2.52404053139152,-2.75409267142618));
#8448=CARTESIAN_POINT('Ctrl Pts',(84.9040006244252,-2.74542564463179,-2.5334644736033));
#8449=CARTESIAN_POINT('Ctrl Pts',(84.8849457241627,-2.97609980732259,-2.23736312836553));
#8450=CARTESIAN_POINT('Ctrl Pts',(84.8816530150491,-3.01412274848135,-2.18586991352904));
#8451=CARTESIAN_POINT('Ctrl Pts',(84.8759810676482,-3.07636478429085,-2.09686374878784));
#8452=CARTESIAN_POINT('Ctrl Pts',(84.8736277777281,-3.10127135509216,-2.05984796131509));
#8453=CARTESIAN_POINT('Ctrl Pts',(84.8687254047083,-3.15123777198564,-1.9826274510979));
#8454=CARTESIAN_POINT('Ctrl Pts',(84.8661736556554,-3.17620736358856,-1.94237422021055));
#8455=CARTESIAN_POINT('Ctrl Pts',(84.8593933479696,-3.23981416807579,-1.83532687415292));
#8456=CARTESIAN_POINT('Ctrl Pts',(84.8551209844165,-3.27715318897931,-1.76779138506349));
#8457=CARTESIAN_POINT('Ctrl Pts',(84.8406379902645,-3.39471293336672,-1.5386171887275));
#8458=CARTESIAN_POINT('Ctrl Pts',(84.8301386052237,-3.4652740466142,-1.37232769270576));
#8459=CARTESIAN_POINT('Ctrl Pts',(84.8056972840747,-3.59917856461861,-0.979672419790579));
#8460=CARTESIAN_POINT('Ctrl Pts',(84.7917089799957,-3.65372708853327,-0.751087971367));
#8461=CARTESIAN_POINT('Ctrl Pts',(84.7761637898157,-3.6922597031176,-0.477332705893551));
#8462=CARTESIAN_POINT('Ctrl Pts',(84.773832210272,-3.69740553180429,-0.435684348529494));
#8463=CARTESIAN_POINT('Ctrl Pts',(84.7702461400659,-3.70433890339234,-0.370534279777525));
#8464=CARTESIAN_POINT('Ctrl Pts',(84.7689679393714,-3.70660923130903,-0.347088510558622));
#8465=CARTESIAN_POINT('Ctrl Pts',(84.7662511585116,-3.71100372807919,-0.296728288935771));
#8466=CARTESIAN_POINT('Ctrl Pts',(84.764816477005,-3.71305798167571,-0.26980893158297));
#8467=CARTESIAN_POINT('Ctrl Pts',(84.7609547658138,-3.7178467677859,-0.196561671039895));
#8468=CARTESIAN_POINT('Ctrl Pts',(84.7585561428848,-3.72000825464481,-0.150199973066388));
#8469=CARTESIAN_POINT('Ctrl Pts',(84.7480399856682,-3.725762785653,0.0560879511793481));
#8470=CARTESIAN_POINT('Ctrl Pts',(84.7402953519644,-3.71991330361409,0.216118305932106));
#8471=CARTESIAN_POINT('Ctrl Pts',(84.7196210529788,-3.67652162113854,0.644360685837346));
#8472=CARTESIAN_POINT('Ctrl Pts',(84.706809428085,-3.62002126997029,0.909642036300186));
#8473=CARTESIAN_POINT('Ctrl Pts',(84.6897819242686,-3.51478315774588,1.22859606302154));
#8474=CARTESIAN_POINT('Ctrl Pts',(84.6864194839653,-3.4926473395465,1.29017938518824));
#8475=CARTESIAN_POINT('Ctrl Pts',(84.680665728801,-3.45262706651849,1.39292656799413));
#8476=CARTESIAN_POINT('Ctrl Pts',(84.678302336898,-3.43560009997883,1.43440921947389));
#8477=CARTESIAN_POINT('Ctrl Pts',(84.6734124454185,-3.39921069412584,1.51869697851222));
#8478=CARTESIAN_POINT('Ctrl Pts',(84.6708839801748,-3.37977900674372,1.56146324022775));
#8479=CARTESIAN_POINT('Ctrl Pts',(84.6642485205864,-3.3272339736198,1.67152804813198));
#8480=CARTESIAN_POINT('Ctrl Pts',(84.6601011402097,-3.29288799246592,1.73821158647624));
#8481=CARTESIAN_POINT('Ctrl Pts',(84.6443755031387,-3.15716404466941,1.9832442718456));
#8482=CARTESIAN_POINT('Ctrl Pts',(84.6323932353672,-3.04312485252166,2.15413962831931));
#8483=CARTESIAN_POINT('Ctrl Pts',(84.6115974044267,-2.82400503823443,2.43013714234308));
#8484=CARTESIAN_POINT('Ctrl Pts',(84.6028710314319,-2.72566535082345,2.5399390463136));
#8485=CARTESIAN_POINT('Ctrl Pts',(84.5943437838656,-2.62112000711956,2.64359555733806));
#8486=CARTESIAN_POINT('Ctrl Pts',(84.3497092098018,-2.62112000711955,2.64359555733807));
#8487=CARTESIAN_POINT('Ctrl Pts',(84.3577004554073,-2.71748852950729,2.5480463492204));
#8488=CARTESIAN_POINT('Ctrl Pts',(84.365757290069,-2.80864298662617,2.44721717317302));
#8489=CARTESIAN_POINT('Ctrl Pts',(84.378282986981,-2.94331207403744,2.2807655878376));
#8490=CARTESIAN_POINT('Ctrl Pts',(84.3828151482965,-2.99055360111133,2.21846069663541));
#8491=CARTESIAN_POINT('Ctrl Pts',(84.390442269409,-3.06808161814511,2.10923052520778));
#8492=CARTESIAN_POINT('Ctrl Pts',(84.393575905211,-3.09933847243202,2.06302687334104));
#8493=CARTESIAN_POINT('Ctrl Pts',(84.398236970433,-3.1451185658393,1.99196473508324));
#8494=CARTESIAN_POINT('Ctrl Pts',(84.3998068298419,-3.16041033343989,1.96761300259467));
#8495=CARTESIAN_POINT('Ctrl Pts',(84.4027208307145,-3.18858935888161,1.92156243169386));
#8496=CARTESIAN_POINT('Ctrl Pts',(84.4040685559681,-3.20154053814446,1.8999059123873));
#8497=CARTESIAN_POINT('Ctrl Pts',(84.4074519783387,-3.23381177980607,1.84467591264155));
#8498=CARTESIAN_POINT('Ctrl Pts',(84.4094700285399,-3.25283037852324,1.81092865817188));
#8499=CARTESIAN_POINT('Ctrl Pts',(84.4189161458612,-3.34047683614565,1.64956827490823));
#8500=CARTESIAN_POINT('Ctrl Pts',(84.4260088191148,-3.40214805511126,1.51830711116934));
#8501=CARTESIAN_POINT('Ctrl Pts',(84.4457737514687,-3.5543492488893,1.13818079816658));
#8502=CARTESIAN_POINT('Ctrl Pts',(84.4582131877736,-3.62622229714311,0.882815693192156));
#8503=CARTESIAN_POINT('Ctrl Pts',(84.4756120260174,-3.68439296953167,0.539544530916548));
#8504=CARTESIAN_POINT('Ctrl Pts',(84.4798574960193,-3.6955815612717,0.45665689540217));
#8505=CARTESIAN_POINT('Ctrl Pts',(84.4866918215267,-3.70882498821928,0.325311041065684));
#8506=CARTESIAN_POINT('Ctrl Pts',(84.4892245110254,-3.71274070412883,0.277067228053662));
#8507=CARTESIAN_POINT('Ctrl Pts',(84.4941341970363,-3.71844122889094,0.184475332889858));
#8508=CARTESIAN_POINT('Ctrl Pts',(84.49650620346,-3.72037573016654,0.140144642224046));
#8509=CARTESIAN_POINT('Ctrl Pts',(84.5021659787817,-3.72307235548542,0.0353799168115024));
#8510=CARTESIAN_POINT('Ctrl Pts',(84.5054736299707,-3.72315605913826,-0.0250576881961806));
#8511=CARTESIAN_POINT('Ctrl Pts',(84.5187103097967,-3.71767503342044,-0.2637322802509));
#8512=CARTESIAN_POINT('Ctrl Pts',(84.528966141924,-3.70077963699944,-0.441452222203766));
#8513=CARTESIAN_POINT('Ctrl Pts',(84.5539098353549,-3.63021470532582,-0.861144180428359));
#8514=CARTESIAN_POINT('Ctrl Pts',(84.5687358205277,-3.5650100027144,-1.100333979738));
#8515=CARTESIAN_POINT('Ctrl Pts',(84.5860047827334,-3.45657226886276,-1.38351087688137));
#8516=CARTESIAN_POINT('Ctrl Pts',(84.5891468768715,-3.43540104393102,-1.43527505765983));
#8517=CARTESIAN_POINT('Ctrl Pts',(84.5938171831602,-3.40158227314799,-1.51292211716394));
#8518=CARTESIAN_POINT('Ctrl Pts',(84.5953881106254,-3.38978813633711,-1.53916593948071));
#8519=CARTESIAN_POINT('Ctrl Pts',(84.5983022019282,-3.36708913967751,-1.58814798598555));
#8520=CARTESIAN_POINT('Ctrl Pts',(84.5996489929479,-3.35625566347617,-1.61091627222005));
#8521=CARTESIAN_POINT('Ctrl Pts',(84.6030266625163,-3.32823629904781,-1.66829364567193));
#8522=CARTESIAN_POINT('Ctrl Pts',(84.6050400146791,-3.31074092722445,-1.70274933222232));
#8523=CARTESIAN_POINT('Ctrl Pts',(84.6143352715038,-3.22644452121061,-1.86255089688336));
#8524=CARTESIAN_POINT('Ctrl Pts',(84.621295403141,-3.15303681970801,-1.98428966050968));
#8525=CARTESIAN_POINT('Ctrl Pts',(84.6410406995129,-2.9222678718785,-2.32171658785509));
#8526=CARTESIAN_POINT('Ctrl Pts',(84.6535726410647,-2.74847053307372,-2.52505946236985));
#8527=CARTESIAN_POINT('Ctrl Pts',(84.6711004456712,-2.49323323700584,-2.76581526337683));
#8528=CARTESIAN_POINT('Ctrl Pts',(84.6753707331877,-2.43009454097619,-2.82145091888547));
#8529=CARTESIAN_POINT('Ctrl Pts',(84.6822352590092,-2.32767955726113,-2.90570593456938));
#8530=CARTESIAN_POINT('Ctrl Pts',(84.684772419124,-2.28963388115275,-2.93577851796405));
#8531=CARTESIAN_POINT('Ctrl Pts',(84.689684803421,-2.21569575173613,-2.9919101005782));
#8532=CARTESIAN_POINT('Ctrl Pts',(84.6920548953846,-2.17990363250114,-3.01808774572552));
#8533=CARTESIAN_POINT('Ctrl Pts',(84.6977002575918,-2.09442789028804,-3.07828922433657));
#8534=CARTESIAN_POINT('Ctrl Pts',(84.7009951214694,-2.04437055131551,-3.11175854094892));
#8535=CARTESIAN_POINT('Ctrl Pts',(84.7138159689729,-1.84903673016673,-3.235614518653));
#8536=CARTESIAN_POINT('Ctrl Pts',(84.7236391931043,-1.69841974330997,-3.31715201385182));
#8537=CARTESIAN_POINT('Ctrl Pts',(84.7479920122739,-1.31973323863029,-3.48958709120933));
#8538=CARTESIAN_POINT('Ctrl Pts',(84.7626834021544,-1.08724328582523,-3.56886772400347));
#8539=CARTESIAN_POINT('Ctrl Pts',(84.7802662201671,-0.787989325480175,-3.63893141087296));
#8540=CARTESIAN_POINT('Ctrl Pts',(84.7837813380466,-0.72697828232875,-3.65160956315452));
#8541=CARTESIAN_POINT('Ctrl Pts',(84.788879245049,-0.636239233871519,-3.66810063443953));
#8542=CARTESIAN_POINT('Ctrl Pts',(84.7905164355045,-0.606739391609856,-3.67309543222682));
#8543=CARTESIAN_POINT('Ctrl Pts',(84.7934955622171,-0.552320147496168,-3.6816359587587));
#8544=CARTESIAN_POINT('Ctrl Pts',(84.7948424467651,-0.527421237112505,-3.68528529960259));
#8545=CARTESIAN_POINT('Ctrl Pts',(84.7981117805102,-0.466297767530757,-3.69361175474456));
#8546=CARTESIAN_POINT('Ctrl Pts',(84.8000197813375,-0.430038303987633,-3.69800874167732));
#8547=CARTESIAN_POINT('Ctrl Pts',(84.8074312458977,-0.2872274003076,-3.71319763317618));
#8548=CARTESIAN_POINT('Ctrl Pts',(84.8127561092886,-0.180289135961944,-3.71992409687582));
#8549=CARTESIAN_POINT('Ctrl Pts',(84.8295767722506,0.164010041812477,-3.72669558947464));
#8550=CARTESIAN_POINT('Ctrl Pts',(84.8407015703705,0.401127396292304,-3.70867385745816));
#8551=CARTESIAN_POINT('Ctrl Pts',(84.8566556212839,0.723208151667462,-3.65292561192162));
#8552=CARTESIAN_POINT('Ctrl Pts',(84.8610836372155,0.81091037342776,-3.63446264516046));
#8553=CARTESIAN_POINT('Ctrl Pts',(84.8692698506329,0.968644445172736,-3.59526295199708));
#8554=CARTESIAN_POINT('Ctrl Pts',(84.8729975277859,1.03889539064298,-3.57559551007754));
#8555=CARTESIAN_POINT('Ctrl Pts',(84.8792037271173,1.15286583215779,-3.54004601070367));
#8556=CARTESIAN_POINT('Ctrl Pts',(84.8816436983426,1.19694685735142,-3.52538556101324));
#8557=CARTESIAN_POINT('Ctrl Pts',(84.886490907348,1.28301329301346,-3.4949613325953));
#8558=CARTESIAN_POINT('Ctrl Pts',(84.8888959258565,1.32501107292667,-3.47925613432383));
#8559=CARTESIAN_POINT('Ctrl Pts',(84.8949203771632,1.42841816444954,-3.43844291032733));
#8560=CARTESIAN_POINT('Ctrl Pts',(84.8985681039725,1.48945768424577,-3.4124453331493));
#8561=CARTESIAN_POINT('Ctrl Pts',(84.9188714965433,1.82056840812455,-3.26084410961349));
#8562=CARTESIAN_POINT('Ctrl Pts',(84.9365427251537,2.07548164509976,-3.10481899919088));
#8563=CARTESIAN_POINT('Ctrl Pts',(84.9626552100353,2.42337840902794,-2.82972643773906));
#8564=CARTESIAN_POINT('Ctrl Pts',(84.9711577592578,2.53231637770362,-2.73267173304806));
#8565=CARTESIAN_POINT('Ctrl Pts',(84.9814765709189,2.66245344852988,-2.60224678598559));
#8566=CARTESIAN_POINT('Ctrl Pts',(84.9836061385242,2.68919595971497,-2.5746013323696));
#8567=CARTESIAN_POINT('Ctrl Pts',(84.9870947643311,2.73290653688442,-2.52799059985835));
#8568=CARTESIAN_POINT('Ctrl Pts',(84.98847033308,2.75011683155746,-2.50925729281321));
#8569=CARTESIAN_POINT('Ctrl Pts',(84.9913815536242,2.78651257298235,-2.46881638364625));
#8570=CARTESIAN_POINT('Ctrl Pts',(84.992913315754,2.80563886685551,-2.4470589100318));
#8571=CARTESIAN_POINT('Ctrl Pts',(84.9974099448455,2.86162074513969,-2.38185636680735));
#8572=CARTESIAN_POINT('Ctrl Pts',(85.0003283673633,2.89773643270886,-2.33778468658485));
#8573=CARTESIAN_POINT('Ctrl Pts',(85.014595141253,3.07200872301441,-2.11487448634548));
#8574=CARTESIAN_POINT('Ctrl Pts',(85.025263459563,3.19470160523901,-1.92453347120085));
#8575=CARTESIAN_POINT('Ctrl Pts',(85.0455503079162,3.39036456633071,-1.55012447362178));
#8576=CARTESIAN_POINT('Ctrl Pts',(85.0550920206195,3.46742023690693,-1.3691039040602));
#8577=CARTESIAN_POINT('Ctrl Pts',(85.0681982570292,3.54921537247631,-1.12501547196317));
#8578=CARTESIAN_POINT('Ctrl Pts',(85.0713445184174,3.56717440162158,-1.06670325151074));
#8579=CARTESIAN_POINT('Ctrl Pts',(85.0768611809925,3.59572773802157,-0.965186795515472));
#8580=CARTESIAN_POINT('Ctrl Pts',(85.0792099544731,3.60699580127323,-0.922184678932751));
#8581=CARTESIAN_POINT('Ctrl Pts',(85.0841548803673,3.62886513226993,-0.832181493252355));
#8582=CARTESIAN_POINT('Ctrl Pts',(85.0867548084219,3.63932934391094,-0.785155920977204));
#8583=CARTESIAN_POINT('Ctrl Pts',(85.0938763811283,3.66520401854062,-0.657214252047274));
#8584=CARTESIAN_POINT('Ctrl Pts',(85.0984506497198,3.67884578387839,-0.57597165853698));
#8585=CARTESIAN_POINT('Ctrl Pts',(85.1201971604326,3.73001510605877,-0.194046773395387));
#8586=CARTESIAN_POINT('Ctrl Pts',(85.1383329859209,3.73343268950547,0.110022995888035));
#8587=CARTESIAN_POINT('Ctrl Pts',(85.1606273071064,3.69135320513746,0.488760773943125));
#8588=CARTESIAN_POINT('Ctrl Pts',(85.1651588822328,3.68027876254556,0.566149168926117));
#8589=CARTESIAN_POINT('Ctrl Pts',(85.1727849575409,3.65714219045148,0.698060312522502));
#8590=CARTESIAN_POINT('Ctrl Pts',(85.1759181489983,3.64627508776562,0.752765440411813));
#8591=CARTESIAN_POINT('Ctrl Pts',(85.180578271632,3.6279499348975,0.835268241075232));
#8592=CARTESIAN_POINT('Ctrl Pts',(85.1821476462709,3.62139242573309,0.863255911161775));
#8593=CARTESIAN_POINT('Ctrl Pts',(85.1850608573952,3.6084722332037,0.915659388230615));
#8594=CARTESIAN_POINT('Ctrl Pts',(85.1864082764962,3.6021844974211,0.940090864992261));
#8595=CARTESIAN_POINT('Ctrl Pts',(85.189790465781,3.58561875875767,1.00185056647336));
#8596=CARTESIAN_POINT('Ctrl Pts',(85.1918076082838,3.5750056380014,1.03908678907127));
#8597=CARTESIAN_POINT('Ctrl Pts',(85.2012233817883,3.52209533629159,1.21430592386757));
#8598=CARTESIAN_POINT('Ctrl Pts',(85.2082893755242,3.47237567034827,1.34992905627698));
#8599=CARTESIAN_POINT('Ctrl Pts',(85.228050436351,3.30938647909909,1.72541323725623));
#8600=CARTESIAN_POINT('Ctrl Pts',(85.2405086361155,3.17822363890271,1.95652291091477));
#8601=CARTESIAN_POINT('Ctrl Pts',(85.2579339182321,2.97478963610414,2.23975556040008));
#8602=CARTESIAN_POINT('Ctrl Pts',(85.2621847287796,2.9236656896391,2.30609106965398));
#8603=CARTESIAN_POINT('Ctrl Pts',(85.2690256378613,2.83951645805101,2.40797808491458));
#8604=CARTESIAN_POINT('Ctrl Pts',(85.2715593779106,2.80795742860439,2.44470590665879));
#8605=CARTESIAN_POINT('Ctrl Pts',(85.276469873513,2.74612615890726,2.51388685394495));
#8606=CARTESIAN_POINT('Ctrl Pts',(85.2788416094157,2.71597228670018,2.54643482269269));
#8607=CARTESIAN_POINT('Ctrl Pts',(85.2844987398314,2.64341813425008,2.62199447093899));
#8608=CARTESIAN_POINT('Ctrl Pts',(85.2878039586191,2.60053958050775,2.66452767958982));
#8609=CARTESIAN_POINT('Ctrl Pts',(85.3009510727438,2.42817135095783,2.8273824941198));
#8610=CARTESIAN_POINT('Ctrl Pts',(85.3111132211399,2.29122817946343,2.93945049721122));
#8611=CARTESIAN_POINT('Ctrl Pts',(85.3355376890594,1.95067241343988,3.17984457878125));
#8612=CARTESIAN_POINT('Ctrl Pts',(85.3499237879498,1.74154920764749,3.2990214802251));
#8613=CARTESIAN_POINT('Ctrl Pts',(85.3671719110249,1.46627061835471,3.42238247810924));
#8614=CARTESIAN_POINT('Ctrl Pts',(85.3706408725114,1.40951888663837,3.44614402891544));
#8615=CARTESIAN_POINT('Ctrl Pts',(85.3756862618091,1.32445425507946,3.47930674326803));
#8616=CARTESIAN_POINT('Ctrl Pts',(85.3773155803586,1.29657728535777,3.4897911034479));
#8617=CARTESIAN_POINT('Ctrl Pts',(85.3802883933489,1.24488745391756,3.50852642723065));
#8618=CARTESIAN_POINT('Ctrl Pts',(85.3816366357756,1.2211131419708,3.51687150448457));
#8619=CARTESIAN_POINT('Ctrl Pts',(85.3849201194898,1.1624357002611,3.53680123612462));
#8620=CARTESIAN_POINT('Ctrl Pts',(85.3868405748137,1.1274426798099,3.54811117949107));
#8621=CARTESIAN_POINT('Ctrl Pts',(85.39432346002,0.988772230521879,3.59067147057664));
#8622=CARTESIAN_POINT('Ctrl Pts',(85.3997035933605,0.883913423917103,3.61791272603219));
#8623=CARTESIAN_POINT('Ctrl Pts',(85.4165070274933,0.547295124935531,3.68985036652612));
#8624=CARTESIAN_POINT('Ctrl Pts',(85.4275725426963,0.312415017983476,3.71711310825143));
#8625=CARTESIAN_POINT('Ctrl Pts',(85.4434538194815,-0.0128580484193436,
3.72380125251899));
#8626=CARTESIAN_POINT('Ctrl Pts',(85.4478728500395,-0.102279230451825,3.72241841526964));
#8627=CARTESIAN_POINT('Ctrl Pts',(85.4560444523055,-0.264292125795481,3.71407069718364));
#8628=CARTESIAN_POINT('Ctrl Pts',(85.4597666907731,-0.33689463674357,3.70818993688117));
#8629=CARTESIAN_POINT('Ctrl Pts',(85.4659662624008,-0.455424664730702,3.69507939925444));
#8630=CARTESIAN_POINT('Ctrl Pts',(85.4684052134145,-0.501473151472571,3.68911206375881));
#8631=CARTESIAN_POINT('Ctrl Pts',(85.4732521370592,-0.591757709752645,3.67569065115112));
#8632=CARTESIAN_POINT('Ctrl Pts',(85.4756579284664,-0.635994548465437,3.6682951965924));
#8633=CARTESIAN_POINT('Ctrl Pts',(85.4816878000442,-0.745387140320439,3.64796889681492));
#8634=CARTESIAN_POINT('Ctrl Pts',(85.4853402917949,-0.810349054877533,3.6340903555459));
#8635=CARTESIAN_POINT('Ctrl Pts',(85.5036193579078,-1.12900026294455,3.55704460246404));
#8636=CARTESIAN_POINT('Ctrl Pts',(85.5189999316127,-1.37589025717203,3.46902002242128));
#8637=CARTESIAN_POINT('Ctrl Pts',(85.544206758291,-1.76074837595394,3.28421194118139));
#8638=CARTESIAN_POINT('Ctrl Pts',(85.5539554571805,-1.90506893466202,3.20265547685798));
#8639=CARTESIAN_POINT('Ctrl Pts',(85.565967208129,-2.08271525574832,3.08599533683943));
#8640=CARTESIAN_POINT('Ctrl Pts',(85.5685867403336,-2.12145466387256,3.05949351324118));
#8641=CARTESIAN_POINT('Ctrl Pts',(85.5726477696777,-2.18169799228777,3.01658612822444));
#8642=CARTESIAN_POINT('Ctrl Pts',(85.5741175277645,-2.20354104537659,3.00066741721889));
#8643=CARTESIAN_POINT('Ctrl Pts',(85.5770000971864,-2.2465081159201,2.96863178157696));
#8644=CARTESIAN_POINT('Ctrl Pts',(85.5784132700148,-2.26763667848559,2.95252389157424));
#8645=CARTESIAN_POINT('Ctrl Pts',(85.5821639308893,-2.32380862651915,2.90874109603037));
#8646=CARTESIAN_POINT('Ctrl Pts',(85.5844755973894,-2.3585305341952,2.88065883903243));
#8647=CARTESIAN_POINT('Ctrl Pts',(85.5920223549565,-2.47176554424096,2.78565673760962));
#8648=CARTESIAN_POINT('Ctrl Pts',(85.5971138283267,-2.54795439720703,2.71613912151622));
#8649=CARTESIAN_POINT('Ctrl Pts',(85.6021262425917,-2.62112000711955,2.64359555733807));
#8650=CARTESIAN_POINT('Origin',(80.1322559480305,0.,0.));
#8651=CARTESIAN_POINT('',(87.0941439893651,-2.62112000711956,2.64359555733806));
#8652=CARTESIAN_POINT('',(86.8469367975355,-2.62112000721926,2.64359555723921));
#8653=CARTESIAN_POINT('',(80.1322559480305,-2.62112000711956,2.64359555733806));
#8654=CARTESIAN_POINT('Ctrl Pts',(87.0941439893651,-2.62112000711957,2.64359555733806));
#8655=CARTESIAN_POINT('Ctrl Pts',(87.0855458142099,-2.49744654314825,2.76621756351642));
#8656=CARTESIAN_POINT('Ctrl Pts',(87.0772681399053,-2.36524967169369,2.88008032166457));
#8657=CARTESIAN_POINT('Ctrl Pts',(87.0605578850035,-2.08604351812172,3.08829126272275));
#8658=CARTESIAN_POINT('Ctrl Pts',(87.0521479914016,-1.93950230334968,3.18236478723634));
#8659=CARTESIAN_POINT('Ctrl Pts',(87.0395835805447,-1.72012288643451,3.3023997723711));
#8660=CARTESIAN_POINT('Ctrl Pts',(87.0356995618198,-1.65221271376186,3.33689364085472));
#8661=CARTESIAN_POINT('Ctrl Pts',(87.0292966197469,-1.54059216483121,3.38934648306319));
#8662=CARTESIAN_POINT('Ctrl Pts',(87.0268211357132,-1.49751281774564,3.40859925751116));
#8663=CARTESIAN_POINT('Ctrl Pts',(87.0219464273946,-1.41291903643471,3.44449221701694));
#8664=CARTESIAN_POINT('Ctrl Pts',(87.0195503982968,-1.37144762996148,3.46121337138111));
#8665=CARTESIAN_POINT('Ctrl Pts',(87.0136303326449,-1.26930686870819,3.50027233558901));
#8666=CARTESIAN_POINT('Ctrl Pts',(87.0100805014871,-1.2083390665222,3.5217839726998));
#8667=CARTESIAN_POINT('Ctrl Pts',(86.9910935314529,-0.883827305684616,3.62686483882435));
#8668=CARTESIAN_POINT('Ctrl Pts',(86.9747910710472,-0.612172398951544,3.68245894365571));
#8669=CARTESIAN_POINT('Ctrl Pts',(86.9492481355891,-0.181110045307059,3.72163175568538));
#8670=CARTESIAN_POINT('Ctrl Pts',(86.9400597739562,-0.0245551509792661,
3.72595586967313));
#8671=CARTESIAN_POINT('Ctrl Pts',(86.9286263086855,0.177800686849849,3.71878632787191));
#8672=CARTESIAN_POINT('Ctrl Pts',(86.926060076226,0.223753597108814,3.71630455387948));
#8673=CARTESIAN_POINT('Ctrl Pts',(86.9220577646374,0.296496939635402,3.71102164552349));
#8674=CARTESIAN_POINT('Ctrl Pts',(86.9205948334473,0.323322155030927,3.70878079174956));
#8675=CARTESIAN_POINT('Ctrl Pts',(86.9177005830546,0.376927776711304,3.70371678215515));
#8676=CARTESIAN_POINT('Ctrl Pts',(86.9162693581982,0.403706589376467,3.70089362559444));
#8677=CARTESIAN_POINT('Ctrl Pts',(86.9124289256373,0.476200554206788,3.69245470844862));
#8678=CARTESIAN_POINT('Ctrl Pts',(86.9100475899422,0.52184709918323,3.68628060608361));
#8679=CARTESIAN_POINT('Ctrl Pts',(86.899175514567,0.732624250476652,3.65377721208441));
#8680=CARTESIAN_POINT('Ctrl Pts',(86.8910971414764,0.895988548172275,3.61718670001727));
#8681=CARTESIAN_POINT('Ctrl Pts',(86.8744182602416,1.22921093762203,3.51858006566514));
#8682=CARTESIAN_POINT('Ctrl Pts',(86.8658427885335,1.39812651832833,3.45493925542693));
#8683=CARTESIAN_POINT('Ctrl Pts',(86.8530708880048,1.63408538865602,3.34589008561808));
#8684=CARTESIAN_POINT('Ctrl Pts',(86.8491067696959,1.70531474899676,3.31015350233701));
#8685=CARTESIAN_POINT('Ctrl Pts',(86.8416761654682,1.83434276782321,3.24014818450169));
#8686=CARTESIAN_POINT('Ctrl Pts',(86.8382311025853,1.89246610934146,3.20654720497949));
#8687=CARTESIAN_POINT('Ctrl Pts',(86.8323560041769,1.98846977638627,3.14752796879192));
#8688=CARTESIAN_POINT('Ctrl Pts',(86.8299557942694,2.02684961967723,3.12295128777444));
#8689=CARTESIAN_POINT('Ctrl Pts',(86.8253386860813,2.09902248733288,3.07484420626856));
#8690=CARTESIAN_POINT('Ctrl Pts',(86.8231268162471,2.13289533227587,3.05144549593877));
#8691=CARTESIAN_POINT('Ctrl Pts',(86.8172040828554,2.22170691097764,2.987894860217));
#8692=CARTESIAN_POINT('Ctrl Pts',(86.8134583231719,2.27594290557852,2.94679153842116));
#8693=CARTESIAN_POINT('Ctrl Pts',(86.7999739708529,2.46436073570031,2.79569147128593));
#8694=CARTESIAN_POINT('Ctrl Pts',(86.7899487314597,2.59193573283884,2.67783923171364));
#8695=CARTESIAN_POINT('Ctrl Pts',(86.7690419502058,2.83593423743576,2.41860859997289));
#8696=CARTESIAN_POINT('Ctrl Pts',(86.7581711286196,2.95110229501105,2.2766612136569));
#8697=CARTESIAN_POINT('Ctrl Pts',(86.7438168938777,3.09221996613475,2.07393308105799));
#8698=CARTESIAN_POINT('Ctrl Pts',(86.7401076603712,3.12766820662185,2.02007797819577));
#8699=CARTESIAN_POINT('Ctrl Pts',(86.7337005448251,3.18741922823247,1.92395410053711));
#8700=CARTESIAN_POINT('Ctrl Pts',(86.7309776181362,3.21232367313618,1.88207804592705));
#8701=CARTESIAN_POINT('Ctrl Pts',(86.7267910275827,3.24997017146413,1.8158511716907));
#8702=CARTESIAN_POINT('Ctrl Pts',(86.7252964880628,3.26327615389606,1.79182879465593));
#8703=CARTESIAN_POINT('Ctrl Pts',(86.7223949737257,3.28887393801994,1.74438393210358));
#8704=CARTESIAN_POINT('Ctrl Pts',(86.7209870866751,3.30118415167598,1.72097365703609));
#8705=CARTESIAN_POINT('Ctrl Pts',(86.7172923381192,3.33314992697423,1.6585792244819));
#8706=CARTESIAN_POINT('Ctrl Pts',(86.7150297520048,3.35237159841283,1.61937594701949));
#8707=CARTESIAN_POINT('Ctrl Pts',(86.7016058151657,3.46380921807279,1.38160213446989));
#8708=CARTESIAN_POINT('Ctrl Pts',(86.6911928349078,3.5390588576568,1.17553355900645));
#8709=CARTESIAN_POINT('Ctrl Pts',(86.6712553906552,3.64680107102452,0.773662735985019));
#8710=CARTESIAN_POINT('Ctrl Pts',(86.6617749004971,3.682638297044,0.579551741808528));
#8711=CARTESIAN_POINT('Ctrl Pts',(86.6480995000784,3.71065098688795,0.309090854882502));
#8712=CARTESIAN_POINT('Ctrl Pts',(86.6442794901657,3.71611411609218,0.234441560619471));
#8713=CARTESIAN_POINT('Ctrl Pts',(86.637954043388,3.72133730444894,0.112782134637251));
#8714=CARTESIAN_POINT('Ctrl Pts',(86.6354899524438,3.72246350967918,0.0658506124230024));
#8715=CARTESIAN_POINT('Ctrl Pts',(86.6306181853865,3.72292984258869,-0.0259455538119476));
#8716=CARTESIAN_POINT('Ctrl Pts',(86.6282132695279,3.72234692770063,-0.0708018320245675));
#8717=CARTESIAN_POINT('Ctrl Pts',(86.6222334684651,3.71891762206235,-0.181151179838617));
#8718=CARTESIAN_POINT('Ctrl Pts',(86.6186315471276,3.71515172672389,-0.246598758624096));
#8719=CARTESIAN_POINT('Ctrl Pts',(86.5999624281649,3.68707407142453,-0.580536440304655));
#8720=CARTESIAN_POINT('Ctrl Pts',(86.5840822472199,3.63537925501826,-0.84588304490476));
#8721=CARTESIAN_POINT('Ctrl Pts',(86.5611812354376,3.52039994896723,-1.21642328869146));
#8722=CARTESIAN_POINT('Ctrl Pts',(86.5542092673796,3.47990959831581,-1.32783008563802));
#8723=CARTESIAN_POINT('Ctrl Pts',(86.5432894830621,3.40670773263547,-1.50275492081419));
#8724=CARTESIAN_POINT('Ctrl Pts',(86.5392488224445,3.37736341988888,-1.56759287309867));
#8725=CARTESIAN_POINT('Ctrl Pts',(86.5335063120669,3.33204517640462,-1.66053673718823));
#8726=CARTESIAN_POINT('Ctrl Pts',(86.5317340939855,3.31753676844222,-1.68933633279597));
#8727=CARTESIAN_POINT('Ctrl Pts',(86.5286256196694,3.29111200434737,-1.74013650741525));
#8728=CARTESIAN_POINT('Ctrl Pts',(86.5272812609262,3.27934546303361,-1.76221074074115));
#8729=CARTESIAN_POINT('Ctrl Pts',(86.524193199337,3.25152834733825,-1.81315241292133));
#8730=CARTESIAN_POINT('Ctrl Pts',(86.5224591029323,3.23531483432639,-1.84192734305363));
#8731=CARTESIAN_POINT('Ctrl Pts',(86.5164848776486,3.17748564426446,-1.94143955722141));
#8732=CARTESIAN_POINT('Ctrl Pts',(86.5123482894765,3.13391364560317,-2.01101702693795));
#8733=CARTESIAN_POINT('Ctrl Pts',(86.5011751645571,3.00785475746478,-2.19825142923168));
#8734=CARTESIAN_POINT('Ctrl Pts',(86.4942971452716,2.92080247638701,-2.31266427673389));
#8735=CARTESIAN_POINT('Ctrl Pts',(86.476657115048,2.68129050520715,-2.59228889376987));
#8736=CARTESIAN_POINT('Ctrl Pts',(86.4659001356468,2.52010626921958,-2.74924276152791));
#8737=CARTESIAN_POINT('Ctrl Pts',(86.4510622207759,2.29208630246345,-2.93427823933306));
#8738=CARTESIAN_POINT('Ctrl Pts',(86.4475189598073,2.23719533916555,-2.97634081802612));
#8739=CARTESIAN_POINT('Ctrl Pts',(86.4415267348762,2.14395401163627,-3.04375383942596));
#8740=CARTESIAN_POINT('Ctrl Pts',(86.4391104961513,2.10624754203616,-3.06996698458039));
#8741=CARTESIAN_POINT('Ctrl Pts',(86.4342085831539,2.02961037666456,-3.12116777702791));
#8742=CARTESIAN_POINT('Ctrl Pts',(86.4317229695238,1.99067965192145,-3.14614062603514));
#8743=CARTESIAN_POINT('Ctrl Pts',(86.4253550603507,1.89082744138003,-3.20759731251835));
#8744=CARTESIAN_POINT('Ctrl Pts',(86.4214384455877,1.82931065731527,-3.24307424058499));
#8745=CARTESIAN_POINT('Ctrl Pts',(86.4126426001675,1.6909784732218,-3.31766235986218));
#8746=CARTESIAN_POINT('Ctrl Pts',(86.4077388505561,1.6137443779867,-3.35590812804808));
#8747=CARTESIAN_POINT('Ctrl Pts',(86.3903949579205,1.3397470159581,-3.47994289762899));
#8748=CARTESIAN_POINT('Ctrl Pts',(86.3776233269253,1.13695734666717,-3.55137196653923));
#8749=CARTESIAN_POINT('Ctrl Pts',(86.3572043491199,0.800513779599716,-3.63808950096067));
#8750=CARTESIAN_POINT('Ctrl Pts',(86.3494805354369,0.670172311482159,-3.66434057082682));
#8751=CARTESIAN_POINT('Ctrl Pts',(86.3398764920265,0.500509054171064,-3.6891527259522));
#8752=CARTESIAN_POINT('Ctrl Pts',(86.3377392959107,0.462234053200812,-3.69414361669377));
#8753=CARTESIAN_POINT('Ctrl Pts',(86.3342510052988,0.398756464235332,-3.70141873879962));
#8754=CARTESIAN_POINT('Ctrl Pts',(86.3328830382304,0.373596380933726,-3.70404282859394));
#8755=CARTESIAN_POINT('Ctrl Pts',(86.3299755315039,0.319503941624645,-3.70912762325093));
#8756=CARTESIAN_POINT('Ctrl Pts',(86.3284401324259,0.290566378758705,-3.7115066724205));
#8757=CARTESIAN_POINT('Ctrl Pts',(86.3239429777239,0.204836103919728,-3.71754599313455));
#8758=CARTESIAN_POINT('Ctrl Pts',(86.321027476268,0.147982107180997,-3.72024299851896));
#8759=CARTESIAN_POINT('Ctrl Pts',(86.3141036958413,0.010717398369314,-3.72360251318449));
#8760=CARTESIAN_POINT('Ctrl Pts',(86.3101425053642,-0.0696974670677866,
-3.72296574440098));
#8761=CARTESIAN_POINT('Ctrl Pts',(86.2988048492034,-0.302427154719188,-3.71357879905024));
#8762=CARTESIAN_POINT('Ctrl Pts',(86.2915584193212,-0.454303501826466,-3.69807246864518));
#8763=CARTESIAN_POINT('Ctrl Pts',(86.2758715214262,-0.776365967934107,-3.64504530329007));
#8764=CARTESIAN_POINT('Ctrl Pts',(86.2674205407036,-0.945729228336533,-3.60481471541688));
#8765=CARTESIAN_POINT('Ctrl Pts',(86.2551853331724,-1.17660564015992,-3.53257679335916));
#8766=CARTESIAN_POINT('Ctrl Pts',(86.251694871993,-1.240987424411,-3.51047705085387));
#8767=CARTESIAN_POINT('Ctrl Pts',(86.2460034296643,-1.34328348412648,-3.47219699865792));
#8768=CARTESIAN_POINT('Ctrl Pts',(86.243838252034,-1.38159893956311,-3.45712983709102));
#8769=CARTESIAN_POINT('Ctrl Pts',(86.2392326614329,-1.46178118124307,-3.42405313610928));
#8770=CARTESIAN_POINT('Ctrl Pts',(86.2367879566774,-1.50358273210469,-3.40590411226489));
#8771=CARTESIAN_POINT('Ctrl Pts',(86.230679935572,-1.60609712198144,-3.35914027804693));
#8772=CARTESIAN_POINT('Ctrl Pts',(86.2269879089592,-1.66638761677131,-3.32964305925615));
#8773=CARTESIAN_POINT('Ctrl Pts',(86.2091932976294,-1.94901758955779,-3.18176654702833));
#8774=CARTESIAN_POINT('Ctrl Pts',(86.1944006840025,-2.15973722932481,-3.04266536129845));
#8775=CARTESIAN_POINT('Ctrl Pts',(86.169216171285,-2.49005394618175,-2.77290553420489));
#8776=CARTESIAN_POINT('Ctrl Pts',(86.1589138222307,-2.61739951071717,-2.65303619659709));
#8777=CARTESIAN_POINT('Ctrl Pts',(86.1464179422017,-2.76740547728743,-2.49048141597456));
#8778=CARTESIAN_POINT('Ctrl Pts',(86.1438229378442,-2.79830545385776,-2.45571124720149));
#8779=CARTESIAN_POINT('Ctrl Pts',(86.1397867243744,-2.84611253359111,-2.39984185863699));
#8780=CARTESIAN_POINT('Ctrl Pts',(86.1383179396979,-2.86345459783929,-2.37912281216687));
#8781=CARTESIAN_POINT('Ctrl Pts',(86.135422842045,-2.89756431081678,-2.33745766745448));
#8782=CARTESIAN_POINT('Ctrl Pts',(86.1339964309089,-2.91433411785479,-2.31651548893668));
#8783=CARTESIAN_POINT('Ctrl Pts',(86.1301855823582,-2.95897452684444,-2.25951631268135));
#8784=CARTESIAN_POINT('Ctrl Pts',(86.1278282771566,-2.98641260020816,-2.22312490629823));
#8785=CARTESIAN_POINT('Ctrl Pts',(86.1177217422589,-3.10277442550558,-2.06274948649478));
#8786=CARTESIAN_POINT('Ctrl Pts',(86.1103128245743,-3.18470336629118,-1.9338604285908));
#8787=CARTESIAN_POINT('Ctrl Pts',(86.0893523808962,-3.39548635608141,-1.55234841437216));
#8788=CARTESIAN_POINT('Ctrl Pts',(86.0759722848772,-3.50372002701962,-1.28959309939659));
#8789=CARTESIAN_POINT('Ctrl Pts',(86.0583532071486,-3.59851601870318,-0.95582858137754));
#8790=CARTESIAN_POINT('Ctrl Pts',(86.0550750166787,-3.61434444646365,-0.894113770380368));
#8791=CARTESIAN_POINT('Ctrl Pts',(86.049420014835,-3.6385418137654,-0.788585608670715));
#8792=CARTESIAN_POINT('Ctrl Pts',(86.0470687449336,-3.64772129451368,-0.744971761561947));
#8793=CARTESIAN_POINT('Ctrl Pts',(86.0421633000119,-3.66505384275882,-0.65459902877039));
#8794=CARTESIAN_POINT('Ctrl Pts',(86.03960630646,-3.6731000857277,-0.607828133473039));
#8795=CARTESIAN_POINT('Ctrl Pts',(86.0327933663423,-3.69194846270976,-0.484161597884745));
#8796=CARTESIAN_POINT('Ctrl Pts',(86.0284928312978,-3.70124232502587,-0.407062600228721));
#8797=CARTESIAN_POINT('Ctrl Pts',(86.0157266400444,-3.72134441612083,-0.180998079736236));
#8798=CARTESIAN_POINT('Ctrl Pts',(86.00708730696,-3.72560846721092,-0.0316144148200146));
#8799=CARTESIAN_POINT('Ctrl Pts',(85.9829417602206,-3.71260889016869,0.379658115342805));
#8800=CARTESIAN_POINT('Ctrl Pts',(85.9672084493833,-3.67666745044717,0.640100566253484));
#8801=CARTESIAN_POINT('Ctrl Pts',(85.9500084052455,-3.60326383863187,0.936605028838768));
#8802=CARTESIAN_POINT('Ctrl Pts',(85.9476014631639,-3.59213557664529,0.978417899278217));
#8803=CARTESIAN_POINT('Ctrl Pts',(85.9437865281443,-3.57305475768065,1.0453911774968));
#8804=CARTESIAN_POINT('Ctrl Pts',(85.942355579981,-3.56555942007055,1.07067696332788));
#8805=CARTESIAN_POINT('Ctrl Pts',(85.9394608085896,-3.54968239526689,1.12222193286415));
#8806=CARTESIAN_POINT('Ctrl Pts',(85.9379982970298,-3.5412766259267,1.1484716473878));
#8807=CARTESIAN_POINT('Ctrl Pts',(85.9339651033083,-3.5170479086983,1.22133726669736));
#8808=CARTESIAN_POINT('Ctrl Pts',(85.9314272721966,-3.50059031158341,1.26773759560353));
#8809=CARTESIAN_POINT('Ctrl Pts',(85.9256035099715,-3.46013458732882,1.37499597964378));
#8810=CARTESIAN_POINT('Ctrl Pts',(85.922346730334,-3.43544292963202,1.43557580391519));
#8811=CARTESIAN_POINT('Ctrl Pts',(85.9098687232766,-3.33347722772846,1.66802227806513));
#8812=CARTESIAN_POINT('Ctrl Pts',(85.9009550103049,-3.24479486307189,1.83457905393513));
#8813=CARTESIAN_POINT('Ctrl Pts',(85.8831081412568,-3.04614358579844,2.14783213426471));
#8814=CARTESIAN_POINT('Ctrl Pts',(85.8742064509636,-2.93721218060871,2.29454792517636));
#8815=CARTESIAN_POINT('Ctrl Pts',(85.8618214218512,-2.77832321480123,2.4786021816896));
#8816=CARTESIAN_POINT('Ctrl Pts',(85.8586911844676,-2.7375610733881,2.52355057492965));
#8817=CARTESIAN_POINT('Ctrl Pts',(85.8536571674366,-2.67121701921286,2.59320833759869));
#8818=CARTESIAN_POINT('Ctrl Pts',(85.8517829969788,-2.6463477451317,2.61858230270289));
#8819=CARTESIAN_POINT('Ctrl Pts',(85.8498933978656,-2.62112000692213,2.64359555753381));
#8820=CARTESIAN_POINT('Ctrl Pts',(85.6021262425917,-2.62112000711955,2.64359555733807));
#8821=CARTESIAN_POINT('Ctrl Pts',(85.6094336418923,-2.72778523837051,2.53783718181052));
#8822=CARTESIAN_POINT('Ctrl Pts',(85.6165766468792,-2.82802492016228,2.42564775805759));
#8823=CARTESIAN_POINT('Ctrl Pts',(85.631059435394,-3.01482777074672,2.18917000253605));
#8824=CARTESIAN_POINT('Ctrl Pts',(85.6383827669007,-3.10109853402161,2.0651478457525));
#8825=CARTESIAN_POINT('Ctrl Pts',(85.6499475555827,-3.22115097676676,1.86800332638407));
#8826=CARTESIAN_POINT('Ctrl Pts',(85.6540125321464,-3.2604934775963,1.7984524490018));
#8827=CARTESIAN_POINT('Ctrl Pts',(85.6606274941131,-3.31971414153624,1.685420721973));
#8828=CARTESIAN_POINT('Ctrl Pts',(85.663127751281,-3.34104607253202,1.64272817647168));
#8829=CARTESIAN_POINT('Ctrl Pts',(85.6680204254946,-3.38072824485395,1.55933831538893));
#8830=CARTESIAN_POINT('Ctrl Pts',(85.6704089298305,-3.39917880517853,1.51869768774041));
#8831=CARTESIAN_POINT('Ctrl Pts',(85.6761871584105,-3.4416012977448,1.42060633759097));
#8832=CARTESIAN_POINT('Ctrl Pts',(85.6795991351301,-3.46487106473743,1.36286820248788));
#8833=CARTESIAN_POINT('Ctrl Pts',(85.6993150376519,-3.58926161707752,1.03041519021633));
#8834=CARTESIAN_POINT('Ctrl Pts',(85.7166162947478,-3.65913445793586,0.745145018366971));
#8835=CARTESIAN_POINT('Ctrl Pts',(85.7425680414504,-3.71289027342828,0.308322627895861));
#8836=CARTESIAN_POINT('Ctrl Pts',(85.7512068635102,-3.72219052180465,0.16099850843398));
#8837=CARTESIAN_POINT('Ctrl Pts',(85.7620585756323,-3.72288832280654,-0.0313838469468115));
#8838=CARTESIAN_POINT('Ctrl Pts',(85.764559677511,-3.7222392938679,-0.0762718669992173));
#8839=CARTESIAN_POINT('Ctrl Pts',(85.7684811559764,-3.719912513768,-0.147738788510013));
#8840=CARTESIAN_POINT('Ctrl Pts',(85.7699268382657,-3.71876124636725,-0.174329434053604));
#8841=CARTESIAN_POINT('Ctrl Pts',(85.7728061260819,-3.71586915988495,-0.227841053166634));
#8842=CARTESIAN_POINT('Ctrl Pts',(85.774239283814,-3.71412070667581,-0.25475993083399));
#8843=CARTESIAN_POINT('Ctrl Pts',(85.7781128636817,-3.70854875306549,-0.328194805047213));
#8844=CARTESIAN_POINT('Ctrl Pts',(85.7805244048689,-3.70414278585925,-0.374662886594448));
#8845=CARTESIAN_POINT('Ctrl Pts',(85.7919118354511,-3.67886027487737,-0.596772586514175));
#8846=CARTESIAN_POINT('Ctrl Pts',(85.8004266269106,-3.64635636776082,-0.77087340925476));
#8847=CARTESIAN_POINT('Ctrl Pts',(85.8202265783356,-3.54187050008689,-1.1703530285236));
#8848=CARTESIAN_POINT('Ctrl Pts',(85.8314676291454,-3.46057341830572,-1.39247852813938));
#8849=CARTESIAN_POINT('Ctrl Pts',(85.8470483893948,-3.32711278545684,-1.67170178882832));
#8850=CARTESIAN_POINT('Ctrl Pts',(85.8508021503739,-3.29347234355921,-1.73703926029697));
#8851=CARTESIAN_POINT('Ctrl Pts',(85.8570397865017,-3.23539841569795,-1.84207259083393));
#8852=CARTESIAN_POINT('Ctrl Pts',(85.859484281786,-3.21211345711308,-1.88238179540526));
#8853=CARTESIAN_POINT('Ctrl Pts',(85.8643318984126,-3.16496500330118,-1.960578486863));
#8854=CARTESIAN_POINT('Ctrl Pts',(85.8667326135437,-3.14116167662022,-1.99849307303521));
#8855=CARTESIAN_POINT('Ctrl Pts',(85.8727291437289,-3.08063142688979,-2.09115340586547));
#8856=CARTESIAN_POINT('Ctrl Pts',(85.8763526716693,-3.04312407427268,-2.14536889191235));
#8857=CARTESIAN_POINT('Ctrl Pts',(85.8948305632577,-2.84732189912131,-2.41292093141666));
#8858=CARTESIAN_POINT('Ctrl Pts',(85.9104691885054,-2.6679702717156,-2.60985217437065));
#8859=CARTESIAN_POINT('Ctrl Pts',(85.9332557825219,-2.3791123891087,-2.86586661738805));
#8860=CARTESIAN_POINT('Ctrl Pts',(85.9403461461548,-2.2851721077665,-2.94131906360297));
#8861=CARTESIAN_POINT('Ctrl Pts',(85.9502774370432,-2.1456865749998,-3.04263007028026));
#8862=CARTESIAN_POINT('Ctrl Pts',(85.9532414755997,-2.10299942242138,-3.07228945197199));
#8863=CARTESIAN_POINT('Ctrl Pts',(85.9585019421841,-2.02504584653918,-3.12406593159353));
#8864=CARTESIAN_POINT('Ctrl Pts',(85.9608132193774,-1.99000313488291,-3.14650384279586));
#8865=CARTESIAN_POINT('Ctrl Pts',(85.9645119501369,-1.93248120565692,-3.18198975367186));
#8866=CARTESIAN_POINT('Ctrl Pts',(85.9659201486685,-1.91022903451263,-3.19539787347497));
#8867=CARTESIAN_POINT('Ctrl Pts',(85.9688053762752,-1.86385742251669,-3.2226816725322));
#8868=CARTESIAN_POINT('Ctrl Pts',(85.9702804018078,-1.83971955252277,-3.23652185477435));
#8869=CARTESIAN_POINT('Ctrl Pts',(85.9744133253612,-1.7709565529244,-3.27493133210099));
#8870=CARTESIAN_POINT('Ctrl Pts',(85.9770354763526,-1.7259778334231,-3.2988578828701));
#8871=CARTESIAN_POINT('Ctrl Pts',(85.9913962102537,-1.47328754320206,-3.42669343696744));
#8872=CARTESIAN_POINT('Ctrl Pts',(86.0023611623734,-1.25668145724071,-3.51191889495602));
#8873=CARTESIAN_POINT('Ctrl Pts',(86.0224058116583,-0.855528912435574,-3.62784625069497));
#8874=CARTESIAN_POINT('Ctrl Pts',(86.0313873383303,-0.67394581621557,-3.66592250707809));
#8875=CARTESIAN_POINT('Ctrl Pts',(86.0441784881778,-0.423336707274367,-3.69921830298302));
#8876=CARTESIAN_POINT('Ctrl Pts',(86.0476436447068,-0.356152264758712,-3.70628990756546));
#8877=CARTESIAN_POINT('Ctrl Pts',(86.0535345720127,-0.243460576768844,-3.71505908397342));
#8878=CARTESIAN_POINT('Ctrl Pts',(86.0559297652706,-0.198046579904935,-3.71775663057157));
#8879=CARTESIAN_POINT('Ctrl Pts',(86.0605245883197,-0.111771546996656,-3.72129602543825));
#8880=CARTESIAN_POINT('Ctrl Pts',(86.062718975586,-0.0709236341024881,-3.72229857049041));
#8881=CARTESIAN_POINT('Ctrl Pts',(86.0685621080425,0.0368633114303421,-3.72316919094131));
#8882=CARTESIAN_POINT('Ctrl Pts',(86.0722442827751,0.103794409393507,-3.72190457606413));
#8883=CARTESIAN_POINT('Ctrl Pts',(86.0941793525446,0.496607901386395,-3.7038789046566));
#8884=CARTESIAN_POINT('Ctrl Pts',(86.1136801770067,0.819152171839487,-3.64613029422204));
#8885=CARTESIAN_POINT('Ctrl Pts',(86.1375922385336,1.2080275068535,-3.52225056611702));
#8886=CARTESIAN_POINT('Ctrl Pts',(86.1423511341087,1.28525028754994,-3.4948122104607));
#8887=CARTESIAN_POINT('Ctrl Pts',(86.1503077796218,1.41512175976555,-3.44377935810376));
#8888=CARTESIAN_POINT('Ctrl Pts',(86.1535483492848,1.46824235355526,-3.42146911900172));
#8889=CARTESIAN_POINT('Ctrl Pts',(86.1583322558526,1.54737228766557,-3.38605263095209));
#8890=CARTESIAN_POINT('Ctrl Pts',(86.1599212756287,1.57377897847635,-3.37386028920838));
#8891=CARTESIAN_POINT('Ctrl Pts',(86.1628637434502,1.62297218004048,-3.3504438299677));
#8892=CARTESIAN_POINT('Ctrl Pts',(86.1642209587629,1.64579089228138,-3.33929407351586));
#8893=CARTESIAN_POINT('Ctrl Pts',(86.1675859750896,1.70263623960033,-3.31079387499808));
#8894=CARTESIAN_POINT('Ctrl Pts',(86.1695771275474,1.7365140551866,-3.29315128736327));
#8895=CARTESIAN_POINT('Ctrl Pts',(86.1782735935378,1.88512324673912,-3.21282876333205));
#8896=CARTESIAN_POINT('Ctrl Pts',(86.1847083241853,1.99678613245855,-3.14464763955368));
#8897=CARTESIAN_POINT('Ctrl Pts',(86.2015442129889,2.28344904665274,-2.94817254448311));
#8898=CARTESIAN_POINT('Ctrl Pts',(86.2117574812673,2.45121262745509,-2.81023468303297));
#8899=CARTESIAN_POINT('Ctrl Pts',(86.2265866333393,2.66775178280323,-2.59796852548684));
#8900=CARTESIAN_POINT('Ctrl Pts',(86.2308674078235,2.7273536437863,-2.53532661106948));
#8901=CARTESIAN_POINT('Ctrl Pts',(86.2388140401587,2.83190804503613,-2.41748217291102));
#8902=CARTESIAN_POINT('Ctrl Pts',(86.2424523992356,2.87756139807176,-2.36295637280083));
#8903=CARTESIAN_POINT('Ctrl Pts',(86.2485508544632,2.95020599584887,-2.27096436095651));
#8904=CARTESIAN_POINT('Ctrl Pts',(86.2509751781328,2.97811225675103,-2.23424297828305));
#8905=CARTESIAN_POINT('Ctrl Pts',(86.2558502219406,3.03225768743813,-2.16017662162868));
#8906=CARTESIAN_POINT('Ctrl Pts',(86.2582999697757,3.05850661325295,-2.12284873900441));
#8907=CARTESIAN_POINT('Ctrl Pts',(86.2644827682683,3.1223423238136,-2.02842731126995));
#8908=CARTESIAN_POINT('Ctrl Pts',(86.2682464472412,3.1590541912884,-1.97076501299057));
#8909=CARTESIAN_POINT('Ctrl Pts',(86.2822501270715,3.28784219863828,-1.75562815569611));
#8910=CARTESIAN_POINT('Ctrl Pts',(86.2928126484244,3.36988997447111,-1.59247156208578));
#8911=CARTESIAN_POINT('Ctrl Pts',(86.3170740741648,3.52769265559509,-1.21129572531365));
#8912=CARTESIAN_POINT('Ctrl Pts',(86.330827827552,3.59582661525552,-0.990903577231676));
#8913=CARTESIAN_POINT('Ctrl Pts',(86.3469111478564,3.65404661263854,-0.713868381899681));
#8914=CARTESIAN_POINT('Ctrl Pts',(86.3498767838918,3.66382000005905,-0.661882362797964));
#8915=CARTESIAN_POINT('Ctrl Pts',(86.3543427455874,3.67710126324904,-0.58188409825047));
#8916=CARTESIAN_POINT('Ctrl Pts',(86.3558806472766,3.68140369666507,-0.554012387597388));
#8917=CARTESIAN_POINT('Ctrl Pts',(86.3587906965812,3.68903056385189,-0.500584685683449));
#8918=CARTESIAN_POINT('Ctrl Pts',(86.3601652289537,3.69240705149697,-0.475038645460873));
#8919=CARTESIAN_POINT('Ctrl Pts',(86.3636623313721,3.70040048840102,-0.409315460613231));
#8920=CARTESIAN_POINT('Ctrl Pts',(86.3657651577478,3.70462863856448,-0.369093247543778));
#8921=CARTESIAN_POINT('Ctrl Pts',(86.3774551740364,3.72474632319961,-0.142212282328467));
#8922=CARTESIAN_POINT('Ctrl Pts',(86.3864782020954,3.72718561104498,0.0453848181484849));
#8923=CARTESIAN_POINT('Ctrl Pts',(86.4074123558229,3.69993653230495,0.481062296494694));
#8924=CARTESIAN_POINT('Ctrl Pts',(86.4192745286475,3.65945858145486,0.727533263752532));
#8925=CARTESIAN_POINT('Ctrl Pts',(86.4353032379562,3.57706323554412,1.03347413285861));
#8926=CARTESIAN_POINT('Ctrl Pts',(86.4387756551994,3.55768013100455,1.09834491365597));
#8927=CARTESIAN_POINT('Ctrl Pts',(86.4444386148511,3.52374258830148,1.20157597714243));
#8928=CARTESIAN_POINT('Ctrl Pts',(86.4465937620554,3.51030368249267,1.24028808776818));
#8929=CARTESIAN_POINT('Ctrl Pts',(86.4511780388182,3.48064771360083,1.32136919929824));
#8930=CARTESIAN_POINT('Ctrl Pts',(86.4536114262528,3.46428980163189,1.36367921236376));
#8931=CARTESIAN_POINT('Ctrl Pts',(86.4596894967195,3.42194913328693,1.46751176925353));
#8932=CARTESIAN_POINT('Ctrl Pts',(86.4633625899263,3.39507696853425,1.52865243643085));
#8933=CARTESIAN_POINT('Ctrl Pts',(86.4771067756071,3.28989239037969,1.75149959088456));
#8934=CARTESIAN_POINT('Ctrl Pts',(86.4874932118722,3.20155688499758,1.90818348412831));
#8935=CARTESIAN_POINT('Ctrl Pts',(86.5127059823591,2.96436471724337,2.26575471392178));
#8936=CARTESIAN_POINT('Ctrl Pts',(86.5276458020231,2.80591308779361,2.45926046121373));
#8937=CARTESIAN_POINT('Ctrl Pts',(86.5442816273993,2.59721298358559,2.66747180694048));
#8938=CARTESIAN_POINT('Ctrl Pts',(86.5468075871259,2.56454887025487,2.69889061886849));
#8939=CARTESIAN_POINT('Ctrl Pts',(86.5507583584423,2.51173992788472,2.74786153182594));
#8940=CARTESIAN_POINT('Ctrl Pts',(86.5522090861148,2.49196660515143,2.76580603000567));
#8941=CARTESIAN_POINT('Ctrl Pts',(86.5550886980006,2.45190159524077,2.80138693408787));
#8942=CARTESIAN_POINT('Ctrl Pts',(86.5565173153271,2.43160854413421,2.81901936172574));
#8943=CARTESIAN_POINT('Ctrl Pts',(86.5603630523863,2.3759150417036,2.86636196805136));
#8944=CARTESIAN_POINT('Ctrl Pts',(86.562751992318,2.34014861075166,2.8956360371964));
#8945=CARTESIAN_POINT('Ctrl Pts',(86.5732100843242,2.17896634044315,3.02262261702539));
#8946=CARTESIAN_POINT('Ctrl Pts',(86.5809104931853,2.04790355723857,3.11291513339007));
#8947=CARTESIAN_POINT('Ctrl Pts',(86.6016278425068,1.67782827902271,3.33434938986421));
#8948=CARTESIAN_POINT('Ctrl Pts',(86.6145200852957,1.4295853158366,3.44808209823842));
#8949=CARTESIAN_POINT('Ctrl Pts',(86.6316253027507,1.10939474106273,3.55420110107961));
#8950=CARTESIAN_POINT('Ctrl Pts',(86.6349699444393,1.04710146829464,3.57304912306805));
#8951=CARTESIAN_POINT('Ctrl Pts',(86.6406945523442,0.941309170392913,3.60205444601581));
#8952=CARTESIAN_POINT('Ctrl Pts',(86.6430469381703,0.898062482272044,3.61307939838748));
#8953=CARTESIAN_POINT('Ctrl Pts',(86.6479142931884,0.809119127503158,3.63405836451464));
#8954=CARTESIAN_POINT('Ctrl Pts',(86.650431221566,0.763412311686202,3.64393404641464));
#8955=CARTESIAN_POINT('Ctrl Pts',(86.6570346075175,0.644302817319845,3.6673302281978));
#8956=CARTESIAN_POINT('Ctrl Pts',(86.6611610442062,0.570660559141779,3.67950847044678));
#8957=CARTESIAN_POINT('Ctrl Pts',(86.6754693191187,0.318019203136027,3.71352107942811));
#8958=CARTESIAN_POINT('Ctrl Pts',(86.6859467858589,0.137838618860974,3.72456226785177));
#8959=CARTESIAN_POINT('Ctrl Pts',(86.7107371972345,-0.28313509616538,3.71976547674153));
#8960=CARTESIAN_POINT('Ctrl Pts',(86.7251150891141,-0.523029518351199,3.69367991143006));
#8961=CARTESIAN_POINT('Ctrl Pts',(86.7409546000593,-0.799030907163151,3.63622214874936));
#8962=CARTESIAN_POINT('Ctrl Pts',(86.7432402383791,-0.839189095120821,3.62716471148247));
#8963=CARTESIAN_POINT('Ctrl Pts',(86.7467696285501,-0.90187715937815,3.61192888146062));
#8964=CARTESIAN_POINT('Ctrl Pts',(86.7480360551279,-0.924512311830358,3.60620156278309));
#8965=CARTESIAN_POINT('Ctrl Pts',(86.7507417433643,-0.973218841064589,3.59338871458555));
#8966=CARTESIAN_POINT('Ctrl Pts',(86.7521769135995,-0.99927006793809,3.58623155772152));
#8967=CARTESIAN_POINT('Ctrl Pts',(86.7560628418112,-1.07030241605493,3.56588241436927));
#8968=CARTESIAN_POINT('Ctrl Pts',(86.7584844057759,-1.11511711927446,3.55212314570359));
#8969=CARTESIAN_POINT('Ctrl Pts',(86.7692768214476,-1.31648417581484,3.48611146000874));
#8970=CARTESIAN_POINT('Ctrl Pts',(86.7772513941482,-1.46972730278891,3.42432677312787));
#8971=CARTESIAN_POINT('Ctrl Pts',(86.7977626258426,-1.8545619878887,3.23855701052766));
#8972=CARTESIAN_POINT('Ctrl Pts',(86.8102101350408,-2.07802282709313,3.09991344118273));
#8973=CARTESIAN_POINT('Ctrl Pts',(86.8268524963812,-2.33741100034856,2.89823658910978));
#8974=CARTESIAN_POINT('Ctrl Pts',(86.8302577577166,-2.38866603906616,2.8561406466196));
#8975=CARTESIAN_POINT('Ctrl Pts',(86.8360539529182,-2.47263967099234,2.7833308232452));
#8976=CARTESIAN_POINT('Ctrl Pts',(86.8384155708165,-2.5059774204876,2.75335329266576));
#8977=CARTESIAN_POINT('Ctrl Pts',(86.8428292837073,-2.56662102961766,2.69680823427543));
#8978=CARTESIAN_POINT('Ctrl Pts',(86.8448742045467,-2.59407595105526,2.67040968790267));
#8979=CARTESIAN_POINT('Ctrl Pts',(86.8469367975355,-2.62112000731897,2.64359555714035));
#8980=CARTESIAN_POINT('Origin',(80.1322559480305,0.,0.));
#8981=CARTESIAN_POINT('',(88.3477258685014,-2.62111999776108,2.64359556661698));
#8982=CARTESIAN_POINT('',(88.102942454071,-2.6211200160691,2.64359554846461));
#8983=CARTESIAN_POINT('',(80.1322559480305,-2.62112000711956,2.64359555733806));
#8984=CARTESIAN_POINT('Ctrl Pts',(88.3477258692703,-2.62111999772913,2.64359556664866));
#8985=CARTESIAN_POINT('Ctrl Pts',(88.346587856507,-2.60731572712132,2.65728247481293));
#8986=CARTESIAN_POINT('Ctrl Pts',(88.3454476547785,-2.59340290379044,2.67086259508366));
#8987=CARTESIAN_POINT('Ctrl Pts',(88.3352752980427,-2.46852116444019,2.79086171869281));
#8988=CARTESIAN_POINT('Ctrl Pts',(88.3261407576867,-2.35116788088766,2.8904178255313));
#8989=CARTESIAN_POINT('Ctrl Pts',(88.3124828443607,-2.16425177741569,3.03005159902215));
#8990=CARTESIAN_POINT('Ctrl Pts',(88.307866055008,-2.0989946068456,3.07561720664413));
#8991=CARTESIAN_POINT('Ctrl Pts',(88.3001131433989,-1.9849836243823,3.14990480204794));
#8992=CARTESIAN_POINT('Ctrl Pts',(88.2969368685854,-1.93694395398754,3.17967121184207));
#8993=CARTESIAN_POINT('Ctrl Pts',(88.2922229086738,-1.86328757730245,3.22302116889539));
#8994=CARTESIAN_POINT('Ctrl Pts',(88.2906415544796,-1.83816087605693,3.23741729646948));
#8995=CARTESIAN_POINT('Ctrl Pts',(88.2877114230548,-1.79075337008403,3.26384910984428));
#8996=CARTESIAN_POINT('Ctrl Pts',(88.2863589147069,-1.76851376001106,3.27595295141795));
#8997=CARTESIAN_POINT('Ctrl Pts',(88.282969248976,-1.71192040711382,3.3060094374264));
#8998=CARTESIAN_POINT('Ctrl Pts',(88.2809496976411,-1.67740573065636,3.32365463346486));
#8999=CARTESIAN_POINT('Ctrl Pts',(88.2716171754733,-1.51461038919857,3.40369962527841));
#9000=CARTESIAN_POINT('Ctrl Pts',(88.264628658243,-1.3830773880799,3.45923681301132));
#9001=CARTESIAN_POINT('Ctrl Pts',(88.2448762116589,-0.997765129077215,3.59642419566466));
#9002=CARTESIAN_POINT('Ctrl Pts',(88.2323609131233,-0.738007829348195,3.65857139934818));
#9003=CARTESIAN_POINT('Ctrl Pts',(88.2148579950487,-0.39052967315798,3.70316208239336));
#9004=CARTESIAN_POINT('Ctrl Pts',(88.210594226684,-0.306883504553843,3.7110300557328));
#9005=CARTESIAN_POINT('Ctrl Pts',(88.2037301592572,-0.174522952423965,3.7189746302174));
#9006=CARTESIAN_POINT('Ctrl Pts',(88.2011865391862,-0.12594877912364,3.72093633119087));
#9007=CARTESIAN_POINT('Ctrl Pts',(88.1962544367835,-0.0327782771470576,
3.72287265153038));
#9008=CARTESIAN_POINT('Ctrl Pts',(88.1938709705507,0.0118066390679314,3.72299819609961));
#9009=CARTESIAN_POINT('Ctrl Pts',(88.1881803952586,0.117154107394293,3.72140250392247));
#9010=CARTESIAN_POINT('Ctrl Pts',(88.1848531310075,0.177892132621967,3.71899388089514));
#9011=CARTESIAN_POINT('Ctrl Pts',(88.1710246036501,0.426733978994542,3.70301607101617));
#9012=CARTESIAN_POINT('Ctrl Pts',(88.1601521792555,0.613714655913062,3.67665197761381));
#9013=CARTESIAN_POINT('Ctrl Pts',(88.1341127710137,1.04689980084175,3.58160124693435));
#9014=CARTESIAN_POINT('Ctrl Pts',(88.1188294509274,1.28965654346071,3.50152250269973));
#9015=CARTESIAN_POINT('Ctrl Pts',(88.1018992440904,1.56350875938017,3.37880812117282));
#9016=CARTESIAN_POINT('Ctrl Pts',(88.0993844281695,1.60435261156045,3.35960667518108));
#9017=CARTESIAN_POINT('Ctrl Pts',(88.0954427303683,1.66882526709724,3.32785286592769));
#9018=CARTESIAN_POINT('Ctrl Pts',(88.0939902673595,1.69268449029694,3.31578072058256));
#9019=CARTESIAN_POINT('Ctrl Pts',(88.0910968820672,1.74047197227789,3.29095123199137));
#9020=CARTESIAN_POINT('Ctrl Pts',(88.0896564256769,1.76439497419444,3.27818748109516));
#9021=CARTESIAN_POINT('Ctrl Pts',(88.0857594842002,1.82938598120682,3.24259494668789));
#9022=CARTESIAN_POINT('Ctrl Pts',(88.0833322943385,1.87016571719005,3.21924768018041));
#9023=CARTESIAN_POINT('Ctrl Pts',(88.068884183962,2.11366607786852,3.07364937988587));
#9024=CARTESIAN_POINT('Ctrl Pts',(88.0577067526452,2.30480616356035,2.93305199732271));
#9025=CARTESIAN_POINT('Ctrl Pts',(88.0373616804602,2.62083602712351,2.65049345396393));
#9026=CARTESIAN_POINT('Ctrl Pts',(88.0282955238868,2.75074743596031,2.51540814458643));
#9027=CARTESIAN_POINT('Ctrl Pts',(88.0153933280264,2.91321046399893,2.31876837962986));
#9028=CARTESIAN_POINT('Ctrl Pts',(88.011909171481,2.95503370283284,2.26522782595828));
#9029=CARTESIAN_POINT('Ctrl Pts',(88.0059874649759,3.02251039851757,2.17379573976275));
#9030=CARTESIAN_POINT('Ctrl Pts',(88.0035808828041,3.04897292264454,2.13652074716154));
#9031=CARTESIAN_POINT('Ctrl Pts',(87.9989644451124,3.09788237455742,2.06486734908438));
#9032=CARTESIAN_POINT('Ctrl Pts',(87.9967598932702,3.12046015448111,2.03058627490492));
#9033=CARTESIAN_POINT('Ctrl Pts',(87.990888679526,3.17852501389863,1.93916726351159));
#9034=CARTESIAN_POINT('Ctrl Pts',(87.9871882623625,3.21303729662564,1.88143070133032));
#9035=CARTESIAN_POINT('Ctrl Pts',(87.9692115249704,3.37079967232023,1.6004930987738));
#9036=CARTESIAN_POINT('Ctrl Pts',(87.9542264076569,3.47245280662494,1.36598264638312));
#9037=CARTESIAN_POINT('Ctrl Pts',(87.9282948771883,3.6049224318297,0.947287493582063));
#9038=CARTESIAN_POINT('Ctrl Pts',(87.9174353343064,3.64738881510277,0.767713351234325));
#9039=CARTESIAN_POINT('Ctrl Pts',(87.9048706635865,3.6826349352984,0.546485251920151));
#9040=CARTESIAN_POINT('Ctrl Pts',(87.9026678426373,3.68825791192327,0.507148916300196));
#9041=CARTESIAN_POINT('Ctrl Pts',(87.899090520988,3.69648295026552,0.442202865002715));
#9042=CARTESIAN_POINT('Ctrl Pts',(87.8976978945483,3.69945105548512,0.416643256640824));
#9043=CARTESIAN_POINT('Ctrl Pts',(87.8947839748211,3.70516712812947,0.362528428296357));
#9044=CARTESIAN_POINT('Ctrl Pts',(87.8932659257446,3.70785048885437,0.333968805923628));
#9045=CARTESIAN_POINT('Ctrl Pts',(87.888881714609,3.71471764158372,0.250536614950347));
#9046=CARTESIAN_POINT('Ctrl Pts',(87.8860583531453,3.71801534607256,0.195597076424892));
#9047=CARTESIAN_POINT('Ctrl Pts',(87.8717588336557,3.72870709199075,-0.0872884408589406));
#9048=CARTESIAN_POINT('Ctrl Pts',(87.860992463612,3.7163622370887,-0.315506229440126));
#9049=CARTESIAN_POINT('Ctrl Pts',(87.8412415427638,3.65656600417579,-0.722477350248943));
#9050=CARTESIAN_POINT('Ctrl Pts',(87.8323523753767,3.61657803567469,-0.90155673379347));
#9051=CARTESIAN_POINT('Ctrl Pts',(87.8196687619998,3.54407232004291,-1.14147362436956));
#9052=CARTESIAN_POINT('Ctrl Pts',(87.8162103016999,3.52282567848555,-1.20544978385056));
#9053=CARTESIAN_POINT('Ctrl Pts',(87.810319289663,3.48430696121762,-1.31169874820459));
#9054=CARTESIAN_POINT('Ctrl Pts',(87.8079169551383,3.46797247398676,-1.35429512504218));
#9055=CARTESIAN_POINT('Ctrl Pts',(87.8033002693359,3.43543249828027,-1.43469935700815));
#9056=CARTESIAN_POINT('Ctrl Pts',(87.8010910421485,3.41937503467993,-1.47255997705303));
#9057=CARTESIAN_POINT('Ctrl Pts',(87.7951866308746,3.37520571745417,-1.57208326169403));
#9058=CARTESIAN_POINT('Ctrl Pts',(87.7914569550663,3.34603267134391,-1.63325563680947));
#9059=CARTESIAN_POINT('Ctrl Pts',(87.773730122849,3.20155359473576,-1.91607299895188));
#9060=CARTESIAN_POINT('Ctrl Pts',(87.7590583907905,3.06580608880852,-2.1265193430973));
#9061=CARTESIAN_POINT('Ctrl Pts',(87.7331941842299,2.79265302044164,-2.46888231530573));
#9062=CARTESIAN_POINT('Ctrl Pts',(87.7220909587528,2.66427557913464,-2.60690167157309));
#9063=CARTESIAN_POINT('Ctrl Pts',(87.7093010454555,2.49677905294502,-2.76161991728417));
#9064=CARTESIAN_POINT('Ctrl Pts',(87.7070953033339,2.46712398390289,-2.78814449170409));
#9065=CARTESIAN_POINT('Ctrl Pts',(87.7035146682175,2.41759252376815,-2.83103803354901));
#9066=CARTESIAN_POINT('Ctrl Pts',(87.7021215794946,2.39796175684534,-2.84768493883956));
#9067=CARTESIAN_POINT('Ctrl Pts',(87.6992082732441,2.35610691025416,-2.88243808785088));
#9068=CARTESIAN_POINT('Ctrl Pts',(87.6976912673471,2.333843749245,-2.90049350268027));
#9069=CARTESIAN_POINT('Ctrl Pts',(87.6933137481492,2.26832297691828,-2.95238791855217));
#9070=CARTESIAN_POINT('Ctrl Pts',(87.6904958355666,2.22452103846253,-2.98553014947108));
#9071=CARTESIAN_POINT('Ctrl Pts',(87.6750641580192,1.97690499052962,-3.16440951635625));
#9072=CARTESIAN_POINT('Ctrl Pts',(87.6633127464237,1.75950191262105,-3.29026060598769));
#9073=CARTESIAN_POINT('Ctrl Pts',(87.6445062691672,1.40355007066605,-3.45086835914533));
#9074=CARTESIAN_POINT('Ctrl Pts',(87.6376923877593,1.27287491077724,-3.50117568379083));
#9075=CARTESIAN_POINT('Ctrl Pts',(87.6267604194912,1.06545880880276,-3.567876727291));
#9076=CARTESIAN_POINT('Ctrl Pts',(87.6227883416597,0.990504878425316,-3.58940745204731));
#9077=CARTESIAN_POINT('Ctrl Pts',(87.6162786327747,0.868875630176352,-3.62024589949874));
#9078=CARTESIAN_POINT('Ctrl Pts',(87.6137873848618,0.82260013944826,-3.63104034349186));
#9079=CARTESIAN_POINT('Ctrl Pts',(87.6089072603084,0.732573704330497,-3.65023107138224));
#9080=CARTESIAN_POINT('Ctrl Pts',(87.6065221549785,0.688853593681906,-3.65873360651626));
#9081=CARTESIAN_POINT('Ctrl Pts',(87.6006769001158,0.582445234716014,-3.67745270055126));
#9082=CARTESIAN_POINT('Ctrl Pts',(87.597192496409,0.519629271381674,-3.68685307164331));
#9083=CARTESIAN_POINT('Ctrl Pts',(87.5778301442832,0.174046608762157,-3.72956225635493));
#9084=CARTESIAN_POINT('Ctrl Pts',(87.5610214887244,-0.111552353881226,-3.73194837453821));
#9085=CARTESIAN_POINT('Ctrl Pts',(87.5352772026974,-0.545508079798557,-3.68569212844711));
#9086=CARTESIAN_POINT('Ctrl Pts',(87.5263747800677,-0.695321001251356,-3.66038799570502));
#9087=CARTESIAN_POINT('Ctrl Pts',(87.5152408535746,-0.887475551411152,-3.61570505316617));
#9088=CARTESIAN_POINT('Ctrl Pts',(87.5127056261594,-0.931582009343133,-3.60459307092547));
#9089=CARTESIAN_POINT('Ctrl Pts',(87.5087398558478,-1.00134789561889,-3.58565038412658));
#9090=CARTESIAN_POINT('Ctrl Pts',(87.5072832297286,-1.02714441683141,-3.57834608842259));
#9091=CARTESIAN_POINT('Ctrl Pts',(87.5043895968151,-1.07879365815488,-3.5631170057493));
#9092=CARTESIAN_POINT('Ctrl Pts',(87.5029529059371,-1.10464339838951,-3.55518798431808));
#9093=CARTESIAN_POINT('Ctrl Pts',(87.4990789703153,-1.17481109445507,-3.53282586792528));
#9094=CARTESIAN_POINT('Ctrl Pts',(87.496670438977,-1.21894920573821,-3.51784066240796));
#9095=CARTESIAN_POINT('Ctrl Pts',(87.4853492505099,-1.42798956971148,-3.44246284939659));
#9096=CARTESIAN_POINT('Ctrl Pts',(87.4768912872865,-1.5887753397043,-3.37127684563644));
#9097=CARTESIAN_POINT('Ctrl Pts',(87.4570953244919,-1.95347062775764,-3.17790241386006));
#9098=CARTESIAN_POINT('Ctrl Pts',(87.4458047703275,-2.15188629174054,-3.04704589493396));
#9099=CARTESIAN_POINT('Ctrl Pts',(87.4301565258806,-2.39389600829121,-2.85194042830058));
#9100=CARTESIAN_POINT('Ctrl Pts',(87.4263906576682,-2.44989885521468,-2.80397878159573));
#9101=CARTESIAN_POINT('Ctrl Pts',(87.4201306550807,-2.53902055178811,-2.72294450809819));
#9102=CARTESIAN_POINT('Ctrl Pts',(87.417676125414,-2.57300595649805,-2.69085344233467));
#9103=CARTESIAN_POINT('Ctrl Pts',(87.4128060618507,-2.63850301323551,-2.62663163530267));
#9104=CARTESIAN_POINT('Ctrl Pts',(87.4103929083172,-2.67005410918231,-2.59455250770431));
#9105=CARTESIAN_POINT('Ctrl Pts',(87.4043585211274,-2.74669040756521,-2.5137550646244));
#9106=CARTESIAN_POINT('Ctrl Pts',(87.4007091077082,-2.79106752677081,-2.46438917875553));
#9107=CARTESIAN_POINT('Ctrl Pts',(87.3823534203921,-3.00455537231326,-2.21373485841248));
#9108=CARTESIAN_POINT('Ctrl Pts',(87.3668830067885,-3.15331321311218,-1.99613532522483));
#9109=CARTESIAN_POINT('Ctrl Pts',(87.3416509594145,-3.3559048006028,-1.61983012253875));
#9110=CARTESIAN_POINT('Ctrl Pts',(87.3319647392225,-3.42422324419902,-1.46991448869948));
#9111=CARTESIAN_POINT('Ctrl Pts',(87.3200127521161,-3.4989813131001,-1.27208394646723));
#9112=CARTESIAN_POINT('Ctrl Pts',(87.3173947588679,-3.51473241462857,-1.2278942309448));
#9113=CARTESIAN_POINT('Ctrl Pts',(87.3133314728247,-3.53825873204522,-1.1577249143893));
#9114=CARTESIAN_POINT('Ctrl Pts',(87.311858021571,-3.54659216653548,-1.13193901168864));
#9115=CARTESIAN_POINT('Ctrl Pts',(87.3089620675417,-3.56259210515531,-1.08051875309074));
#9116=CARTESIAN_POINT('Ctrl Pts',(87.3075393156371,-3.57026526575852,-1.05488828208453));
#9117=CARTESIAN_POINT('Ctrl Pts',(87.3037510938621,-3.59015699470958,-0.985739925626268));
#9118=CARTESIAN_POINT('Ctrl Pts',(87.3014121936805,-3.60186077134007,-0.942077371476803));
#9119=CARTESIAN_POINT('Ctrl Pts',(87.2863192786097,-3.67322439539774,-0.65503989190597));
#9120=CARTESIAN_POINT('Ctrl Pts',(87.2745319491281,-3.70898210585364,-0.406363048817564));
#9121=CARTESIAN_POINT('Ctrl Pts',(87.2562721399099,-3.72490374872104,-0.0266501069281622));
#9122=CARTESIAN_POINT('Ctrl Pts',(87.2500057611676,-3.72357860408172,0.102850190824901));
#9123=CARTESIAN_POINT('Ctrl Pts',(87.238928349933,-3.70967572988444,0.325493722224022));
#9124=CARTESIAN_POINT('Ctrl Pts',(87.2341985579693,-3.70031298148294,0.418715085825928));
#9125=CARTESIAN_POINT('Ctrl Pts',(87.2267679865319,-3.68053254130884,0.561319448893375));
#9126=CARTESIAN_POINT('Ctrl Pts',(87.2241421221132,-3.67260990985818,0.611011822737596));
#9127=CARTESIAN_POINT('Ctrl Pts',(87.2191521944317,-3.65584337743535,0.704009182172894));
#9128=CARTESIAN_POINT('Ctrl Pts',(87.2167956392945,-3.64723069725869,0.747347139286704));
#9129=CARTESIAN_POINT('Ctrl Pts',(87.2113778000089,-3.62587872103958,0.845605538925054));
#9130=CARTESIAN_POINT('Ctrl Pts',(87.2083021192094,-3.61265932591186,0.900409548344087));
#9131=CARTESIAN_POINT('Ctrl Pts',(87.1978515838246,-3.56412586457384,1.08329248893044));
#9132=CARTESIAN_POINT('Ctrl Pts',(87.1903089898278,-3.52320500320499,1.20976725898419));
#9133=CARTESIAN_POINT('Ctrl Pts',(87.1689867403307,-3.39126144318707,1.55359210349915));
#9134=CARTESIAN_POINT('Ctrl Pts',(87.154906767161,-3.28624325195498,1.76490753501621));
#9135=CARTESIAN_POINT('Ctrl Pts',(87.1369820493023,-3.12408132064938,2.02586788704766));
#9136=CARTESIAN_POINT('Ctrl Pts',(87.1328317942871,-3.08441911274939,2.0857575187262));
#9137=CARTESIAN_POINT('Ctrl Pts',(87.1257644639136,-3.01274413640612,2.18746605764376));
#9138=CARTESIAN_POINT('Ctrl Pts',(87.1228153393004,-2.98153105680148,2.22982243141839));
#9139=CARTESIAN_POINT('Ctrl Pts',(87.1183644403625,-2.93220890175546,2.29386464656165));
#9140=CARTESIAN_POINT('Ctrl Pts',(87.1168256235655,-2.91473429248608,2.31602853269854));
#9141=CARTESIAN_POINT('Ctrl Pts',(87.1139217341,-2.88090433879447,2.35794726614331));
#9142=CARTESIAN_POINT('Ctrl Pts',(87.1125540829754,-2.86459413087463,2.37773539443057));
#9143=CARTESIAN_POINT('Ctrl Pts',(87.1090495928073,-2.82186335034614,2.42849999482197));
#9144=CARTESIAN_POINT('Ctrl Pts',(87.106933070194,-2.79513598764554,2.45921533469826));
#9145=CARTESIAN_POINT('Ctrl Pts',(87.1012014979304,-2.72043575025773,2.54226997610862));
#9146=CARTESIAN_POINT('Ctrl Pts',(87.0976455027076,-2.67148468059826,2.59365907861286));
#9147=CARTESIAN_POINT('Ctrl Pts',(87.0941439893651,-2.62112000711957,2.64359555733806));
#9148=CARTESIAN_POINT('Ctrl Pts',(86.8469367975355,-2.62112000731897,2.64359555714035));
#9149=CARTESIAN_POINT('Ctrl Pts',(86.8473899349745,-2.62706139976061,2.63770467774389));
#9150=CARTESIAN_POINT('Ctrl Pts',(86.8478439237163,-2.63298296180103,2.63179374004676));
#9151=CARTESIAN_POINT('Ctrl Pts',(86.8522648269433,-2.69034510248191,2.57414713842212));
#9152=CARTESIAN_POINT('Ctrl Pts',(86.8562945859776,-2.74027159920205,2.52093253104793));
#9153=CARTESIAN_POINT('Ctrl Pts',(86.8654083654593,-2.84797960956079,2.39914845539768));
#9154=CARTESIAN_POINT('Ctrl Pts',(86.8705201335773,-2.90491158070205,2.32989018388121));
#9155=CARTESIAN_POINT('Ctrl Pts',(86.8894238697966,-3.10337451565115,2.06986359556756));
#9156=CARTESIAN_POINT('Ctrl Pts',(86.9036213542172,-3.22906402916566,1.86772681932388));
#9157=CARTESIAN_POINT('Ctrl Pts',(86.9237344933729,-3.38214556663351,1.55928838810713));
#9158=CARTESIAN_POINT('Ctrl Pts',(86.9298940203282,-3.42551618219064,1.46155088764665));
#9159=CARTESIAN_POINT('Ctrl Pts',(86.937903803101,-3.47797564028516,1.32811324295582));
#9160=CARTESIAN_POINT('Ctrl Pts',(86.939919987003,-3.49082824486581,1.29395428999919));
#9161=CARTESIAN_POINT('Ctrl Pts',(86.9432804599939,-3.51169022498739,1.23593381450495));
#9162=CARTESIAN_POINT('Ctrl Pts',(86.94463865535,-3.51996345481526,1.21217079316765));
#9163=CARTESIAN_POINT('Ctrl Pts',(86.9475820335882,-3.53755079811137,1.15995601156604));
#9164=CARTESIAN_POINT('Ctrl Pts',(86.9491618493022,-3.54676366908233,1.13147301686612));
#9165=CARTESIAN_POINT('Ctrl Pts',(86.9539823311102,-3.57411596005467,1.04329062954808));
#9166=CARTESIAN_POINT('Ctrl Pts',(86.9571659275947,-3.59109964713755,0.983241762208478));
#9167=CARTESIAN_POINT('Ctrl Pts',(86.9649254941717,-3.62942355092949,0.833459573771509));
#9168=CARTESIAN_POINT('Ctrl Pts',(86.9694375816899,-3.64895452789624,0.743305155814841));
#9169=CARTESIAN_POINT('Ctrl Pts',(86.984682524476,-3.70416359584887,0.433200717531767));
#9170=CARTESIAN_POINT('Ctrl Pts',(86.9951748666698,-3.72344507782224,0.210828040851256));
#9171=CARTESIAN_POINT('Ctrl Pts',(87.0118083870354,-3.72235777203515,-0.128304325582148));
#9172=CARTESIAN_POINT('Ctrl Pts',(87.017618646654,-3.71652864138321,-0.244583929871908));
#9173=CARTESIAN_POINT('Ctrl Pts',(87.0263791707301,-3.6999958379374,-0.414560098068529));
#9174=CARTESIAN_POINT('Ctrl Pts',(87.0292039653643,-3.69354043233271,-0.468602134953449));
#9175=CARTESIAN_POINT('Ctrl Pts',(87.0343673135872,-3.67975601811787,-0.565845783029031));
#9176=CARTESIAN_POINT('Ctrl Pts',(87.0366927238313,-3.67284448532002,-0.60909685082763));
#9177=CARTESIAN_POINT('Ctrl Pts',(87.0418271086227,-3.6560733939613,-0.703343308434649));
#9178=CARTESIAN_POINT('Ctrl Pts',(87.044645117817,-3.64590658019617,-0.75427403098112));
#9179=CARTESIAN_POINT('Ctrl Pts',(87.0532226561584,-3.61211666853835,-0.906844780102981));
#9180=CARTESIAN_POINT('Ctrl Pts',(87.0590780729086,-3.58528411650565,-1.00771488732806));
#9181=CARTESIAN_POINT('Ctrl Pts',(87.0738703301397,-3.50830042704802,-1.25481575578491));
#9182=CARTESIAN_POINT('Ctrl Pts',(87.0829257819692,-3.45321429435865,-1.39929973263157));
#9183=CARTESIAN_POINT('Ctrl Pts',(87.1044709741835,-3.30217946521773,-1.73171955214702));
#9184=CARTESIAN_POINT('Ctrl Pts',(87.1169832392531,-3.19891671648481,-1.91577225783769));
#9185=CARTESIAN_POINT('Ctrl Pts',(87.131342122091,-3.055880654736,-2.12659468478338));
#9186=CARTESIAN_POINT('Ctrl Pts',(87.13379710035,-3.03047911295223,-2.16263917643575));
#9187=CARTESIAN_POINT('Ctrl Pts',(87.1376642862929,-2.98882080052086,-2.21957600955985));
#9188=CARTESIAN_POINT('Ctrl Pts',(87.139100675472,-2.97297167492617,-2.24076035516961));
#9189=CARTESIAN_POINT('Ctrl Pts',(87.141979966135,-2.94039885077346,-2.28334394995256));
#9190=CARTESIAN_POINT('Ctrl Pts',(87.1434220714834,-2.92366425503528,-2.30473261094895));
#9191=CARTESIAN_POINT('Ctrl Pts',(87.147350631069,-2.87697309610368,-2.36308201632092));
#9192=CARTESIAN_POINT('Ctrl Pts',(87.1498067998886,-2.84653897727171,-2.39965561167959));
#9193=CARTESIAN_POINT('Ctrl Pts',(87.1554057637012,-2.7745569909931,-2.48286129514672));
#9194=CARTESIAN_POINT('Ctrl Pts',(87.1585224419049,-2.73251970072881,-2.52905188247201));
#9195=CARTESIAN_POINT('Ctrl Pts',(87.1700258842128,-2.57109607692522,-2.69769795905632));
#9196=CARTESIAN_POINT('Ctrl Pts',(87.1781497407726,-2.44447781565016,-2.81294190932959));
#9197=CARTESIAN_POINT('Ctrl Pts',(87.1953722239273,-2.16303389795497,-3.03569824269789));
#9198=CARTESIAN_POINT('Ctrl Pts',(87.2044691642374,-2.00707626905943,-3.1409897970051));
#9199=CARTESIAN_POINT('Ctrl Pts',(87.2174288270614,-1.78438228839504,-3.26795545598925));
#9200=CARTESIAN_POINT('Ctrl Pts',(87.2209380423758,-1.72399646643795,-3.30021036674723));
#9201=CARTESIAN_POINT('Ctrl Pts',(87.2268815658895,-1.6219157348871,-3.35117005119017));
#9202=CARTESIAN_POINT('Ctrl Pts',(87.2292839992155,-1.58070312253751,-3.37080535797707));
#9203=CARTESIAN_POINT('Ctrl Pts',(87.2341641362162,-1.49716651676246,-3.40873658367422));
#9204=CARTESIAN_POINT('Ctrl Pts',(87.2366419191941,-1.45484296903431,-3.42701391238433));
#9205=CARTESIAN_POINT('Ctrl Pts',(87.2430014108148,-1.34650799464527,-3.47142958889346));
#9206=CARTESIAN_POINT('Ctrl Pts',(87.2469175851446,-1.28007027387451,-3.49647341522531));
#9207=CARTESIAN_POINT('Ctrl Pts',(87.2557181200866,-1.1314156173652,-3.5477042615272));
#9208=CARTESIAN_POINT('Ctrl Pts',(87.2606271783031,-1.04892349588877,-3.57296303828486));
#9209=CARTESIAN_POINT('Ctrl Pts',(87.2780359194904,-0.7573864219849,-3.65126389773269));
#9210=CARTESIAN_POINT('Ctrl Pts',(87.2908705554386,-0.544682061964044,-3.68899360794475));
#9211=CARTESIAN_POINT('Ctrl Pts',(87.3113060964913,-0.198259845136661,-3.71981640525909));
#9212=CARTESIAN_POINT('Ctrl Pts',(87.3189883217274,-0.0660517408872298,
-3.7245111635414));
#9213=CARTESIAN_POINT('Ctrl Pts',(87.3285327134508,0.104382164702472,-3.72148294148486));
#9214=CARTESIAN_POINT('Ctrl Pts',(87.3306504181745,0.142618747206788,-3.72021384322786));
#9215=CARTESIAN_POINT('Ctrl Pts',(87.3341118551425,0.205956205848665,-3.71713362724989));
#9216=CARTESIAN_POINT('Ctrl Pts',(87.335472092754,0.231069883848536,-3.7156570350764));
#9217=CARTESIAN_POINT('Ctrl Pts',(87.3383670199711,0.285041684580131,-3.71193432525252));
#9218=CARTESIAN_POINT('Ctrl Pts',(87.3398975313162,0.313891695691506,-3.70960608486964));
#9219=CARTESIAN_POINT('Ctrl Pts',(87.3443859500546,0.399303504323378,-3.70170963038285));
#9220=CARTESIAN_POINT('Ctrl Pts',(87.3472976685906,0.455770077201023,-3.69518223395162));
#9221=CARTESIAN_POINT('Ctrl Pts',(87.3542148388467,0.591635461779865,-3.67631448184335));
#9222=CARTESIAN_POINT('Ctrl Pts',(87.3581732040126,0.670828372940872,-3.66269178521249));
#9223=CARTESIAN_POINT('Ctrl Pts',(87.3695118136425,0.898987413466158,-3.61579494022049));
#9224=CARTESIAN_POINT('Ctrl Pts',(87.3767616091401,1.04642569633715,-3.57591200447481));
#9225=CARTESIAN_POINT('Ctrl Pts',(87.3924580917532,1.35586109260056,-3.47142413618571));
#9226=CARTESIAN_POINT('Ctrl Pts',(87.4009153350006,1.51660414695282,-3.40426940925044));
#9227=CARTESIAN_POINT('Ctrl Pts',(87.413151299323,1.73275126561451,-3.29561162782169));
#9228=CARTESIAN_POINT('Ctrl Pts',(87.4166354898917,1.79260063763816,-3.26344376179476));
#9229=CARTESIAN_POINT('Ctrl Pts',(87.4223123148643,1.88711627543246,-3.20925878064477));
#9230=CARTESIAN_POINT('Ctrl Pts',(87.42446920123,1.92235780184505,-3.18827383797709));
#9231=CARTESIAN_POINT('Ctrl Pts',(87.4290528771893,1.99579526723477,-3.14288445497222));
#9232=CARTESIAN_POINT('Ctrl Pts',(87.4314838425139,2.03390646803325,-3.11835624694404));
#9233=CARTESIAN_POINT('Ctrl Pts',(87.4375462680497,2.12684690719819,-3.05611150919702));
#9234=CARTESIAN_POINT('Ctrl Pts',(87.4412058104457,2.18112920342523,-3.017609974659));
#9235=CARTESIAN_POINT('Ctrl Pts',(87.4548399513917,2.37669539652386,-2.87086365347971));
#9236=CARTESIAN_POINT('Ctrl Pts',(87.4651234889337,2.511185373091,-2.7539926250342));
#9237=CARTESIAN_POINT('Ctrl Pts',(87.4904133442831,2.81511217352789,-2.44904506187802));
#9238=CARTESIAN_POINT('Ctrl Pts',(87.5055487981762,2.97476267811515,-2.25243709313934));
#9239=CARTESIAN_POINT('Ctrl Pts',(87.5223244904424,3.13784274550207,-2.00370111649192));
#9240=CARTESIAN_POINT('Ctrl Pts',(87.5248209754313,3.16173304057958,-1.9657873198146));
#9241=CARTESIAN_POINT('Ctrl Pts',(87.5287370172134,3.19870503329672,-1.90469449549014));
#9242=CARTESIAN_POINT('Ctrl Pts',(87.5301817666119,3.21223229639277,-1.88179137674653));
#9243=CARTESIAN_POINT('Ctrl Pts',(87.5330610185432,3.23899009311629,-1.83535808010318));
#9244=CARTESIAN_POINT('Ctrl Pts',(87.534495039195,3.25221245292654,-1.81182514440652));
#9245=CARTESIAN_POINT('Ctrl Pts',(87.5383739224393,3.28763712018424,-1.74713937349005));
#9246=CARTESIAN_POINT('Ctrl Pts',(87.540789769645,3.30932250483166,-1.70570770003931));
#9247=CARTESIAN_POINT('Ctrl Pts',(87.5515227723301,3.40350230651728,-1.51720834710164));
#9248=CARTESIAN_POINT('Ctrl Pts',(87.5594486119933,3.46701881599291,-1.36584699771955));
#9249=CARTESIAN_POINT('Ctrl Pts',(87.5799943253291,3.60621670591948,-0.961128375247433));
#9250=CARTESIAN_POINT('Ctrl Pts',(87.5925193231542,3.66527614170109,-0.703070443728016));
#9251=CARTESIAN_POINT('Ctrl Pts',(87.6092424466115,3.70437464903941,-0.375295410529423));
#9252=CARTESIAN_POINT('Ctrl Pts',(87.6126376483127,3.71045476337085,-0.309455923773697));
#9253=CARTESIAN_POINT('Ctrl Pts',(87.6184219342769,3.71770851794193,-0.198790640705265));
#9254=CARTESIAN_POINT('Ctrl Pts',(87.6207819924242,3.71983135528355,-0.154041565688244));
#9255=CARTESIAN_POINT('Ctrl Pts',(87.6256423167465,3.72251100625336,-0.0627840324924113));
#9256=CARTESIAN_POINT('Ctrl Pts',(87.6281440655121,3.72300479016126,-0.0162817801131505));
#9257=CARTESIAN_POINT('Ctrl Pts',(87.6346530902917,3.72203305449251,0.103435917079885));
#9258=CARTESIAN_POINT('Ctrl Pts',(87.6386981812944,3.7192786903159,0.176618412499463));
#9259=CARTESIAN_POINT('Ctrl Pts',(87.6478545169702,3.70832644558581,0.339556927789161));
#9260=CARTESIAN_POINT('Ctrl Pts',(87.6529939378152,3.6990238332021,0.429191084747156));
#9261=CARTESIAN_POINT('Ctrl Pts',(87.6721183090258,3.65295445052668,0.756805650929006));
#9262=CARTESIAN_POINT('Ctrl Pts',(87.6865199576498,3.59638014142236,0.991398050306722));
#9263=CARTESIAN_POINT('Ctrl Pts',(87.7065985183614,3.48371450341881,1.31654396977808));
#9264=CARTESIAN_POINT('Ctrl Pts',(87.7125491408456,3.44581064111291,1.41277979517627));
#9265=CARTESIAN_POINT('Ctrl Pts',(87.7203414801692,3.38930755174152,1.54037956989887));
#9266=CARTESIAN_POINT('Ctrl Pts',(87.7223382706663,3.37418632449789,1.57322653852528));
#9267=CARTESIAN_POINT('Ctrl Pts',(87.7256771808073,3.34775228223228,1.62851259482424));
#9268=CARTESIAN_POINT('Ctrl Pts',(87.7270327616913,3.33668686240006,1.65106617637407));
#9269=CARTESIAN_POINT('Ctrl Pts',(87.7299833884142,3.31185024873655,1.70041850411334));
#9270=CARTESIAN_POINT('Ctrl Pts',(87.7315727822955,3.29798079244825,1.72716471941759));
#9271=CARTESIAN_POINT('Ctrl Pts',(87.7364598834056,3.2538675110606,1.8097645428743));
#9272=CARTESIAN_POINT('Ctrl Pts',(87.7396982039293,3.22251685282666,1.86501674445612));
#9273=CARTESIAN_POINT('Ctrl Pts',(87.7476331619983,3.14092599293388,2.00060599787278));
#9274=CARTESIAN_POINT('Ctrl Pts',(87.7522620855194,3.08900346766987,2.07987971926953));
#9275=CARTESIAN_POINT('Ctrl Pts',(87.7718710877152,2.85400839829867,2.41041824362851));
#9276=CARTESIAN_POINT('Ctrl Pts',(87.786415500584,2.64290191557751,2.64017927228636));
#9277=CARTESIAN_POINT('Ctrl Pts',(87.8054413772444,2.35686525737934,2.88238583047108));
#9278=CARTESIAN_POINT('Ctrl Pts',(87.8087330175567,2.30697716961592,2.92246773244327));
#9279=CARTESIAN_POINT('Ctrl Pts',(87.8143953933482,2.22072124691013,2.98818355318106));
#9280=CARTESIAN_POINT('Ctrl Pts',(87.8167400435671,2.18488112487688,3.01448802472819));
#9281=CARTESIAN_POINT('Ctrl Pts',(87.8216166108929,2.11015236783528,3.06730154094434));
#9282=CARTESIAN_POINT('Ctrl Pts',(87.8241510134052,2.07121501682897,3.09372749939246));
#9283=CARTESIAN_POINT('Ctrl Pts',(87.8308629366755,1.96789795484324,3.16102181846558));
#9284=CARTESIAN_POINT('Ctrl Pts',(87.8350829761815,1.90274755190945,3.20066116879983));
#9285=CARTESIAN_POINT('Ctrl Pts',(87.8477814453308,1.70618579254025,3.31213169953281));
#9286=CARTESIAN_POINT('Ctrl Pts',(87.8564383143798,1.57161604328785,3.37806195957758));
#9287=CARTESIAN_POINT('Ctrl Pts',(87.8807836924883,1.18859066375219,3.53786860470293));
#9288=CARTESIAN_POINT('Ctrl Pts',(87.8967136362589,0.933506570284459,3.61356258857102));
#9289=CARTESIAN_POINT('Ctrl Pts',(87.9140467192536,0.630578803360852,3.66920400504446));
#9290=CARTESIAN_POINT('Ctrl Pts',(87.9164190809944,0.588487007166788,3.67618973996398));
#9291=CARTESIAN_POINT('Ctrl Pts',(87.9201892596059,0.520389131938299,3.68629189672736));
#9292=CARTESIAN_POINT('Ctrl Pts',(87.9216092707534,0.494454620036324,3.68986009884771));
#9293=CARTESIAN_POINT('Ctrl Pts',(87.9244907451265,0.4411837282703,3.69661760871857));
#9294=CARTESIAN_POINT('Ctrl Pts',(87.9259507429193,0.413845666194757,3.6997779235437));
#9295=CARTESIAN_POINT('Ctrl Pts',(87.929989923136,0.337347535583371,3.7077626584229));
#9296=CARTESIAN_POINT('Ctrl Pts',(87.9325359113087,0.288121415849994,3.71191241466898));
#9297=CARTESIAN_POINT('Ctrl Pts',(87.9383865952892,0.173168811171942,3.71930217894022));
#9298=CARTESIAN_POINT('Ctrl Pts',(87.94166166476,0.107409295024827,3.72178184391183));
#9299=CARTESIAN_POINT('Ctrl Pts',(87.9542963132215,-0.149666044005904,3.72465583143753));
#9300=CARTESIAN_POINT('Ctrl Pts',(87.9633404188895,-0.340834509650255,3.71204770811981));
#9301=CARTESIAN_POINT('Ctrl Pts',(87.9811734316564,-0.707499832718931,3.65928959122063));
#9302=CARTESIAN_POINT('Ctrl Pts',(87.9899197054762,-0.882722593028811,3.6210149663471));
#9303=CARTESIAN_POINT('Ctrl Pts',(88.0021233170764,-1.11247135391488,3.55315762055016));
#9304=CARTESIAN_POINT('Ctrl Pts',(88.0052422536444,-1.1700162574781,3.53462629232209));
#9305=CARTESIAN_POINT('Ctrl Pts',(88.0107276247342,-1.26897764421147,3.50007606229411));
#9306=CARTESIAN_POINT('Ctrl Pts',(88.0130731675355,-1.31060659683479,3.48470182783606));
#9307=CARTESIAN_POINT('Ctrl Pts',(88.0180275870966,-1.39704225674514,3.45101184348976));
#9308=CARTESIAN_POINT('Ctrl Pts',(88.0206405852091,-1.44178630984336,3.43255906743687));
#9309=CARTESIAN_POINT('Ctrl Pts',(88.027844680944,-1.56280222561935,3.3798676052861));
#9310=CARTESIAN_POINT('Ctrl Pts',(88.032490539931,-1.638297560711,3.34392515592509));
#9311=CARTESIAN_POINT('Ctrl Pts',(88.0521474877394,-1.94731673693956,3.18382705588358));
#9312=CARTESIAN_POINT('Ctrl Pts',(88.0678516829027,-2.16846840066719,3.03751754194363));
#9313=CARTESIAN_POINT('Ctrl Pts',(88.0900120865799,-2.45854736152291,2.79767011230306));
#9314=CARTESIAN_POINT('Ctrl Pts',(88.0965584132985,-2.541596160395,2.72244330185412));
#9315=CARTESIAN_POINT('Ctrl Pts',(88.1029424533549,-2.62112001609809,2.64359554843587));
#9316=CARTESIAN_POINT('Origin',(80.1322559480305,0.,0.));
#9317=CARTESIAN_POINT('',(89.5984125828093,-2.62112000687686,2.6435955575787));
#9318=CARTESIAN_POINT('',(89.3487674494621,-2.62112000711956,2.64359555733806));
#9319=CARTESIAN_POINT('',(80.1322559480305,-2.62112000711956,2.64359555733806));
#9320=CARTESIAN_POINT('Ctrl Pts',(89.5984125828093,-2.62112000663417,2.64359555781933));
#9321=CARTESIAN_POINT('Ctrl Pts',(89.5943271447616,-2.5618080717952,2.70240322927981));
#9322=CARTESIAN_POINT('Ctrl Pts',(89.5901926787951,-2.50053473596257,2.75919725800358));
#9323=CARTESIAN_POINT('Ctrl Pts',(89.5822945568946,-2.38202439419345,2.86185173325579));
#9324=CARTESIAN_POINT('Ctrl Pts',(89.5785496786393,-2.32524350402295,2.90817422540554));
#9325=CARTESIAN_POINT('Ctrl Pts',(89.5723142085096,-2.23011948428828,2.98120990868023));
#9326=CARTESIAN_POINT('Ctrl Pts',(89.5698624397723,-2.1925739153427,3.0089308407746));
#9327=CARTESIAN_POINT('Ctrl Pts',(89.5649901827266,-2.11776324134503,3.06202183484714));
#9328=CARTESIAN_POINT('Ctrl Pts',(89.562571907531,-2.08053876462607,3.0874353553927));
#9329=CARTESIAN_POINT('Ctrl Pts',(89.5565104335751,-1.98706422803676,3.14879316191372));
#9330=CARTESIAN_POINT('Ctrl Pts',(89.5528385141918,-1.93029301021984,3.18391123407403));
#9331=CARTESIAN_POINT('Ctrl Pts',(89.5343776809933,-1.64427933930165,3.35037437243731));
#9332=CARTESIAN_POINT('Ctrl Pts',(89.5188149771131,-1.40247738177234,3.45856688682408));
#9333=CARTESIAN_POINT('Ctrl Pts',(89.4933721941459,-0.993160166882023,3.59167855485942));
#9334=CARTESIAN_POINT('Ctrl Pts',(89.4835709032494,-0.83173765598187,3.6324566666028));
#9335=CARTESIAN_POINT('Ctrl Pts',(89.4715019718314,-0.621798218042232,3.6707562904483));
#9336=CARTESIAN_POINT('Ctrl Pts',(89.4688723455797,-0.575317235283083,3.67832777848009));
#9337=CARTESIAN_POINT('Ctrl Pts',(89.464798557957,-0.501903698917201,3.68886069567858));
#9338=CARTESIAN_POINT('Ctrl Pts',(89.4633257551182,-0.475062309323462,3.69241336352804));
#9339=CARTESIAN_POINT('Ctrl Pts',(89.4604433012178,-0.421872711140325,3.69886380255716));
#9340=CARTESIAN_POINT('Ctrl Pts',(89.4590331920707,-0.395527805133241,3.70177360594109));
#9341=CARTESIAN_POINT('Ctrl Pts',(89.4552986738902,-0.324976102185999,3.70880427079457));
#9342=CARTESIAN_POINT('Ctrl Pts',(89.4529998739697,-0.280721626942598,3.71241623237597));
#9343=CARTESIAN_POINT('Ctrl Pts',(89.4377034636118,0.0182346209747569,3.73143969417713));
#9344=CARTESIAN_POINT('Ctrl Pts',(89.4257234248191,0.273896898122981,3.72142194754956));
#9345=CARTESIAN_POINT('Ctrl Pts',(89.4049751944012,0.701512062560916,3.66032612678257));
#9346=CARTESIAN_POINT('Ctrl Pts',(89.3963859606162,0.874467693343638,3.62290020498499));
#9347=CARTESIAN_POINT('Ctrl Pts',(89.3840783653783,1.10779716648023,3.55472314485318));
#9348=CARTESIAN_POINT('Ctrl Pts',(89.380672045639,1.17098193445921,3.53441251582577));
#9349=CARTESIAN_POINT('Ctrl Pts',(89.3748522765092,1.27629864743267,3.49742455879786));
#9350=CARTESIAN_POINT('Ctrl Pts',(89.3724678820671,1.31873094876546,3.48164691358501));
#9351=CARTESIAN_POINT('Ctrl Pts',(89.3678751547635,1.39903377573888,3.45010923326288));
#9352=CARTESIAN_POINT('Ctrl Pts',(89.3656716891562,1.43695233626936,3.43448934043742));
#9353=CARTESIAN_POINT('Ctrl Pts',(89.3597588301606,1.53705241603428,3.39130697012417));
#9354=CARTESIAN_POINT('Ctrl Pts',(89.3560142559021,1.59874770073665,3.36266234819664));
#9355=CARTESIAN_POINT('Ctrl Pts',(89.3424350497237,1.81641827523252,3.25425499992135));
#9356=CARTESIAN_POINT('Ctrl Pts',(89.3323054185756,1.96749236243847,3.1652035561517));
#9357=CARTESIAN_POINT('Ctrl Pts',(89.3113307670147,2.26141386177886,2.96275420499678));
#9358=CARTESIAN_POINT('Ctrl Pts',(89.300501553853,2.40335113914105,2.84882590155623));
#9359=CARTESIAN_POINT('Ctrl Pts',(89.2861985663028,2.5834569035375,2.68118461925042));
#9360=CARTESIAN_POINT('Ctrl Pts',(89.2824983910797,2.62937429390787,2.63616996086165));
#9361=CARTESIAN_POINT('Ctrl Pts',(89.2761074655527,2.70790401280267,2.55508974984062));
#9362=CARTESIAN_POINT('Ctrl Pts',(89.2733916289446,2.74101865568885,2.51953268185867));
#9363=CARTESIAN_POINT('Ctrl Pts',(89.2692181405706,2.7916720871035,2.46296212279386));
#9364=CARTESIAN_POINT('Ctrl Pts',(89.267729578352,2.80969045020819,2.44238717781868));
#9365=CARTESIAN_POINT('Ctrl Pts',(89.2648342479026,2.84468102692327,2.40153213123823));
#9366=CARTESIAN_POINT('Ctrl Pts',(89.2634266093837,2.86166698599168,2.38126622728695));
#9367=CARTESIAN_POINT('Ctrl Pts',(89.259737617861,2.90605210688444,2.3271495667082));
#9368=CARTESIAN_POINT('Ctrl Pts',(89.2574803451724,2.9330764566551,2.29299515105011));
#9369=CARTESIAN_POINT('Ctrl Pts',(89.2419237087941,3.11764829601166,2.05112205328567));
#9370=CARTESIAN_POINT('Ctrl Pts',(89.2296902411884,3.25360833024745,1.82781101317892));
#9371=CARTESIAN_POINT('Ctrl Pts',(89.2099146921086,3.42945410741587,1.4561379406622));
#9372=CARTESIAN_POINT('Ctrl Pts',(89.2026052257,3.48548030831931,1.31640269209036));
#9373=CARTESIAN_POINT('Ctrl Pts',(89.1911544044757,3.5574065486287,1.0998951742217));
#9374=CARTESIAN_POINT('Ctrl Pts',(89.187193005777,3.57959695857387,1.02537570048041));
#9375=CARTESIAN_POINT('Ctrl Pts',(89.1806917497927,3.61157702884788,0.904234949720744));
#9376=CARTESIAN_POINT('Ctrl Pts',(89.1781977102319,3.6228337593404,0.858023754605999));
#9377=CARTESIAN_POINT('Ctrl Pts',(89.1733053945656,3.64294860031054,0.767979035047733));
#9378=CARTESIAN_POINT('Ctrl Pts',(89.1709107515881,3.65190833694855,0.724176476745814));
#9379=CARTESIAN_POINT('Ctrl Pts',(89.1650281296726,3.67177254526394,0.617293325350234));
#9380=CARTESIAN_POINT('Ctrl Pts',(89.1615153958727,3.68184275931097,0.554073904307277));
#9381=CARTESIAN_POINT('Ctrl Pts',(89.1398253282955,3.73323708455912,0.167510083016139));
#9382=CARTESIAN_POINT('Ctrl Pts',(89.1203886395769,3.73356572176802,-0.159819337753641));
#9383=CARTESIAN_POINT('Ctrl Pts',(89.0962884968879,3.680240688744,-0.567410937842279));
#9384=CARTESIAN_POINT('Ctrl Pts',(89.0913339933252,3.66629067271162,-0.651491111261201));
#9385=CARTESIAN_POINT('Ctrl Pts',(89.0830910000021,3.63777258928263,-0.793086656427543));
#9386=CARTESIAN_POINT('Ctrl Pts',(89.0797563563629,3.62469329085107,-0.850867281344274));
#9387=CARTESIAN_POINT('Ctrl Pts',(89.0748566634192,3.60303802061444,-0.936939635855264));
#9388=CARTESIAN_POINT('Ctrl Pts',(89.07324333015,3.5954955463849,-0.965479542648749));
#9389=CARTESIAN_POINT('Ctrl Pts',(89.0702707695591,3.58080465612314,-1.01850679064977));
#9390=CARTESIAN_POINT('Ctrl Pts',(89.0689074038154,3.57374283771589,-1.04301496428459));
#9391=CARTESIAN_POINT('Ctrl Pts',(89.0655409037207,3.55550500125024,-1.10394896451903));
#9392=CARTESIAN_POINT('Ctrl Pts',(89.0635541446008,3.54402040381528,-1.14028010784235));
#9393=CARTESIAN_POINT('Ctrl Pts',(89.0550405017232,3.49177317004527,-1.29714127939003));
#9394=CARTESIAN_POINT('Ctrl Pts',(89.0487689976239,3.44540155202557,-1.41572189261893));
#9395=CARTESIAN_POINT('Ctrl Pts',(89.031957226059,3.30277196959761,-1.73167653153313));
#9396=CARTESIAN_POINT('Ctrl Pts',(89.0216261014067,3.19499827980722,-1.92327693488621));
#9397=CARTESIAN_POINT('Ctrl Pts',(89.0066481876398,3.02183548524199,-2.17599087775461));
#9398=CARTESIAN_POINT('Ctrl Pts',(89.0023440689527,2.9701981383992,-2.24596257615318));
#9399=CARTESIAN_POINT('Ctrl Pts',(88.9943565522433,2.87174779334856,-2.37002894411395));
#9400=CARTESIAN_POINT('Ctrl Pts',(88.9907010319644,2.82573477310012,-2.42470508581248));
#9401=CARTESIAN_POINT('Ctrl Pts',(88.9845744622068,2.74734510282089,-2.51258992862816));
#9402=CARTESIAN_POINT('Ctrl Pts',(88.9821395595911,2.71586984457589,-2.54657888168349));
#9403=CARTESIAN_POINT('Ctrl Pts',(88.977242835758,2.65200519511514,-2.61301296685249));
#9404=CARTESIAN_POINT('Ctrl Pts',(88.9747819940956,2.61963443281089,-2.64546470534321));
#9405=CARTESIAN_POINT('Ctrl Pts',(88.968568792321,2.53727299727478,-2.72503793078099));
#9406=CARTESIAN_POINT('Ctrl Pts',(88.9647854578592,2.48656315467354,-2.77138752751406));
#9407=CARTESIAN_POINT('Ctrl Pts',(88.9502894328436,2.29025887611617,-2.9410860159636));
#9408=CARTESIAN_POINT('Ctrl Pts',(88.9392182292009,2.13655142010712,-3.05457143130824));
#9409=CARTESIAN_POINT('Ctrl Pts',(88.9180357866656,1.83159890814682,-3.24540697237114));
#9410=CARTESIAN_POINT('Ctrl Pts',(88.9079886350751,1.682418945424,-3.32519006561237));
#9411=CARTESIAN_POINT('Ctrl Pts',(88.8945741242445,1.47166198478017,-3.42007913692788));
#9412=CARTESIAN_POINT('Ctrl Pts',(88.8910027424847,1.41435753318342,-3.44417242865778));
#9413=CARTESIAN_POINT('Ctrl Pts',(88.8848047264691,1.31228714745151,-3.48410984953826));
#9414=CARTESIAN_POINT('Ctrl Pts',(88.8821550692265,1.26777128804404,-3.50055358015823));
#9415=CARTESIAN_POINT('Ctrl Pts',(88.8780552145461,1.19726655602733,-3.52507586705999));
#9416=CARTESIAN_POINT('Ctrl Pts',(88.8765760119042,1.17148390065933,-3.53372786667786));
#9417=CARTESIAN_POINT('Ctrl Pts',(88.8738542315812,1.12334177068792,-3.54929830729211));
#9418=CARTESIAN_POINT('Ctrl Pts',(88.8726075840097,1.10100773709355,-3.55628980999406));
#9419=CARTESIAN_POINT('Ctrl Pts',(88.8692014278906,1.03926167410361,-3.57498151166268));
#9420=CARTESIAN_POINT('Ctrl Pts',(88.8670651445378,0.999718354159187,-3.58624052655691));
#9421=CARTESIAN_POINT('Ctrl Pts',(88.8525579979586,0.726393416625571,-3.6591907873291));
#9422=CARTESIAN_POINT('Ctrl Pts',(88.8411322079086,0.48724908128512,-3.6986398726336));
#9423=CARTESIAN_POINT('Ctrl Pts',(88.8210452842138,0.0693639414856265,-3.72630851783919));
#9424=CARTESIAN_POINT('Ctrl Pts',(88.8124948751221,-0.107821275637139,-3.72539330121516));
#9425=CARTESIAN_POINT('Ctrl Pts',(88.7997846512026,-0.360040015419946,-3.70607812564811));
#9426=CARTESIAN_POINT('Ctrl Pts',(88.7959081711549,-0.435621180879112,-3.69795579998194));
#9427=CARTESIAN_POINT('Ctrl Pts',(88.7895152448493,-0.557590371981448,-3.68105726400317));
#9428=CARTESIAN_POINT('Ctrl Pts',(88.7870420336098,-0.604154334058376,-3.67370206767575));
#9429=CARTESIAN_POINT('Ctrl Pts',(88.7821702937406,-0.694576886866073,-3.65765342765294));
#9430=CARTESIAN_POINT('Ctrl Pts',(88.7797749241903,-0.738443381164276,-3.64905012144772));
#9431=CARTESIAN_POINT('Ctrl Pts',(88.7738538417917,-0.845372690050457,-3.62607159105905));
#9432=CARTESIAN_POINT('Ctrl Pts',(88.7703022616376,-0.908234575301005,-3.61083915777708));
#9433=CARTESIAN_POINT('Ctrl Pts',(88.751330180831,-1.23726325887303,-3.52197474243307));
#9434=CARTESIAN_POINT('Ctrl Pts',(88.7350463333981,-1.49499003332496,-3.42053958137388));
#9435=CARTESIAN_POINT('Ctrl Pts',(88.7095086293281,-1.87759794522472,-3.21838979981905));
#9436=CARTESIAN_POINT('Ctrl Pts',(88.7003075897857,-2.01135697332097,-3.13653573443043));
#9437=CARTESIAN_POINT('Ctrl Pts',(88.6888614998624,-2.17723465715658,-3.02003897546785));
#9438=CARTESIAN_POINT('Ctrl Pts',(88.6862943852759,-2.21440950985724,-2.9928877462384));
#9439=CARTESIAN_POINT('Ctrl Pts',(88.6822914701913,-2.27250748609849,-2.94877967154556));
#9440=CARTESIAN_POINT('Ctrl Pts',(88.6808287769051,-2.29376573649089,-2.93227397452747));
#9441=CARTESIAN_POINT('Ctrl Pts',(88.678113254031,-2.33333012967654,-2.90086112130445));
#9442=CARTESIAN_POINT('Ctrl Pts',(88.6768567906216,-2.35167696416519,-2.88600766708209));
#9443=CARTESIAN_POINT('Ctrl Pts',(88.6733829152909,-2.40246044310033,-2.84408789508451));
#9444=CARTESIAN_POINT('Ctrl Pts',(88.6711903289283,-2.43458033666695,-2.81664179577578));
#9445=CARTESIAN_POINT('Ctrl Pts',(88.6571449461076,-2.64003297376343,-2.63494376472635));
#9446=CARTESIAN_POINT('Ctrl Pts',(88.6461490978435,-2.79910533774633,-2.46530592000982));
#9447=CARTESIAN_POINT('Ctrl Pts',(88.6261107240962,-3.05530512538202,-2.13507240425678));
#9448=CARTESIAN_POINT('Ctrl Pts',(88.6171449357426,-3.15808570742325,-1.97987671932963));
#9449=CARTESIAN_POINT('Ctrl Pts',(88.6040144848518,-3.28559775587395,-1.75196526466524));
#9450=CARTESIAN_POINT('Ctrl Pts',(88.6001727315239,-3.3203516838051,-1.68517021365381));
#9451=CARTESIAN_POINT('Ctrl Pts',(88.5938204014959,-3.37349001454877,-1.5750063318007));
#9452=CARTESIAN_POINT('Ctrl Pts',(88.5913518523316,-3.39311916184391,-1.53226039442805));
#9453=CARTESIAN_POINT('Ctrl Pts',(88.5864775280323,-3.42986385083162,-1.44807145336529));
#9454=CARTESIAN_POINT('Ctrl Pts',(88.5840746532376,-3.44705101305148,-1.40666842158982));
#9455=CARTESIAN_POINT('Ctrl Pts',(88.5781118952671,-3.48742168811705,-1.30423126708377));
#9456=CARTESIAN_POINT('Ctrl Pts',(88.5745253651667,-3.50975468530323,-1.24287994488893));
#9457=CARTESIAN_POINT('Ctrl Pts',(88.5557650332944,-3.61661158733736,-0.923437066245195));
#9458=CARTESIAN_POINT('Ctrl Pts',(88.5397636267566,-3.67431166599015,-0.657275453897727));
#9459=CARTESIAN_POINT('Ctrl Pts',(88.5143435170982,-3.71911506418414,-0.228907073054607));
#9460=CARTESIAN_POINT('Ctrl Pts',(88.5049862263008,-3.72550271886407,-0.0696511161675265));
#9461=CARTESIAN_POINT('Ctrl Pts',(88.4933758970248,-3.72055898139491,0.135848430779211));
#9462=CARTESIAN_POINT('Ctrl Pts',(88.490791469862,-3.71858022525425,0.182141203561677));
#9463=CARTESIAN_POINT('Ctrl Pts',(88.4867673161267,-3.71408205582662,0.255324102884424));
#9464=CARTESIAN_POINT('Ctrl Pts',(88.485300298954,-3.71213344617649,0.282243301695779));
#9465=CARTESIAN_POINT('Ctrl Pts',(88.4824047992743,-3.70766088553837,0.33591714617746));
#9466=CARTESIAN_POINT('Ctrl Pts',(88.4809762930765,-3.70513965397643,0.362670369165699));
#9467=CARTESIAN_POINT('Ctrl Pts',(88.4771527425558,-3.69754054804012,0.434921969598884));
#9468=CARTESIAN_POINT('Ctrl Pts',(88.4747851438938,-3.6919126222383,0.480358999039255));
#9469=CARTESIAN_POINT('Ctrl Pts',(88.4598586819442,-3.65057995528813,0.770133492151917));
#9470=CARTESIAN_POINT('Ctrl Pts',(88.4482318779265,-3.59147432453225,1.01053211722554));
#9471=CARTESIAN_POINT('Ctrl Pts',(88.4276787042224,-3.44856265581029,1.41386695122147));
#9472=CARTESIAN_POINT('Ctrl Pts',(88.4188946236114,-3.37578581070706,1.57976808592928));
#9473=CARTESIAN_POINT('Ctrl Pts',(88.4063408879922,-3.25989249180027,1.79901880998709));
#9474=CARTESIAN_POINT('Ctrl Pts',(88.4028979724788,-3.22694718624467,1.85746571989442));
#9475=CARTESIAN_POINT('Ctrl Pts',(88.3970255296454,-3.16900466839523,1.95406062123651));
#9476=CARTESIAN_POINT('Ctrl Pts',(88.3946257685157,-3.14485266737148,1.9926979101459));
#9477=CARTESIAN_POINT('Ctrl Pts',(88.3900088785258,-3.09753828120153,2.06538596757483));
#9478=CARTESIAN_POINT('Ctrl Pts',(88.3877967640531,-3.07450805298463,2.09951486029721));
#9479=CARTESIAN_POINT('Ctrl Pts',(88.3818718100216,-3.01190688096473,2.18904521985672));
#9480=CARTESIAN_POINT('Ctrl Pts',(88.3781240189798,-2.97137548824645,2.24375331244069));
#9481=CARTESIAN_POINT('Ctrl Pts',(88.3656851753564,-2.8338933990256,2.41906028999436));
#9482=CARTESIAN_POINT('Ctrl Pts',(88.3567794841335,-2.73094174453057,2.53470751268217));
#9483=CARTESIAN_POINT('Ctrl Pts',(88.3477258692703,-2.62111999772913,2.64359556664866));
#9484=CARTESIAN_POINT('Ctrl Pts',(88.1029424533549,-2.62112001609809,2.64359554843587));
#9485=CARTESIAN_POINT('Ctrl Pts',(88.104827393899,-2.6446000911777,2.6203150981389));
#9486=CARTESIAN_POINT('Ctrl Pts',(88.1066980440785,-2.66777287808874,2.59671897917028));
#9487=CARTESIAN_POINT('Ctrl Pts',(88.110721425517,-2.71740373500025,2.54481533952543));
#9488=CARTESIAN_POINT('Ctrl Pts',(88.1128670494712,-2.74373799950446,2.51640024549215));
#9489=CARTESIAN_POINT('Ctrl Pts',(88.1163603226718,-2.78648353173111,2.46880813712911));
#9490=CARTESIAN_POINT('Ctrl Pts',(88.1177251218543,-2.80315154355,2.44986645501762));
#9491=CARTESIAN_POINT('Ctrl Pts',(88.1206139875581,-2.83838882781883,2.40899192472459));
#9492=CARTESIAN_POINT('Ctrl Pts',(88.1221341987369,-2.85689885897995,2.38701115277737));
#9493=CARTESIAN_POINT('Ctrl Pts',(88.1265554238813,-2.91054475537499,2.32178829339098));
#9494=CARTESIAN_POINT('Ctrl Pts',(88.1294123149259,-2.9449677254837,2.27796781038236));
#9495=CARTESIAN_POINT('Ctrl Pts',(88.1361650371508,-3.02522191071424,2.17094269986712));
#9496=CARTESIAN_POINT('Ctrl Pts',(88.1400167486146,-3.07007478313663,2.10703623624153));
#9497=CARTESIAN_POINT('Ctrl Pts',(88.1585229962119,-3.27831360160684,1.78955399165135));
#9498=CARTESIAN_POINT('Ctrl Pts',(88.172552382389,-3.41247338270368,1.51818168747295));
#9499=CARTESIAN_POINT('Ctrl Pts',(88.1917895691776,-3.53999809288119,1.1550781273012));
#9500=CARTESIAN_POINT('Ctrl Pts',(88.1960153612915,-3.564930464326,1.07566794129381));
#9501=CARTESIAN_POINT('Ctrl Pts',(88.202825832497,-3.60010339943074,0.948924974560949));
#9502=CARTESIAN_POINT('Ctrl Pts',(88.2053550649856,-3.6121180859515,0.902111825947858));
#9503=CARTESIAN_POINT('Ctrl Pts',(88.2102628935753,-3.63341547107911,0.811868670640676));
#9504=CARTESIAN_POINT('Ctrl Pts',(88.2126366141887,-3.64283907630651,0.768480293008751));
#9505=CARTESIAN_POINT('Ctrl Pts',(88.2183085894543,-3.66328839184387,0.665477462950102));
#9506=CARTESIAN_POINT('Ctrl Pts',(88.2216269655774,-3.67363809505849,0.605743066487205));
#9507=CARTESIAN_POINT('Ctrl Pts',(88.2354444802331,-3.71016812870533,0.359267300349725));
#9508=CARTESIAN_POINT('Ctrl Pts',(88.2463149520546,-3.72359845602328,0.170940362312663));
#9509=CARTESIAN_POINT('Ctrl Pts',(88.2724685176875,-3.72149562287613,-0.274500399021354));
#9510=CARTESIAN_POINT('Ctrl Pts',(88.2878736676169,-3.69368862339893,-0.530614676385393));
#9511=CARTESIAN_POINT('Ctrl Pts',(88.3048402312432,-3.6304675943449,-0.824934232501567));
#9512=CARTESIAN_POINT('Ctrl Pts',(88.3072951516026,-3.62044276122353,-0.867874407031743));
#9513=CARTESIAN_POINT('Ctrl Pts',(88.3111622734454,-3.60318582772701,-0.936279511793043));
#9514=CARTESIAN_POINT('Ctrl Pts',(88.3125986549176,-3.59644111070314,-0.961862193918668));
#9515=CARTESIAN_POINT('Ctrl Pts',(88.3154780346354,-3.58222108132513,-1.01355671691687));
#9516=CARTESIAN_POINT('Ctrl Pts',(88.3169202351315,-3.57473165532099,-1.03966281797688));
#9517=CARTESIAN_POINT('Ctrl Pts',(88.3208491473606,-3.55333701081578,-1.11127286053428));
#9518=CARTESIAN_POINT('Ctrl Pts',(88.3233055682666,-3.53884373647796,-1.15659702753469));
#9519=CARTESIAN_POINT('Ctrl Pts',(88.3289052048355,-3.50332677435404,-1.26074155644079));
#9520=CARTESIAN_POINT('Ctrl Pts',(88.3320222971041,-3.48168356566194,-1.31933617425825));
#9521=CARTESIAN_POINT('Ctrl Pts',(88.3435284448993,-3.3952900659898,-1.53627167913842));
#9522=CARTESIAN_POINT('Ctrl Pts',(88.3516544954185,-3.32112522513915,-1.69063810611603));
#9523=CARTESIAN_POINT('Ctrl Pts',(88.3688759871969,-3.14379534632403,-2.00267392944265));
#9524=CARTESIAN_POINT('Ctrl Pts',(88.3779696420024,-3.03876311178762,-2.15871799761719));
#9525=CARTESIAN_POINT('Ctrl Pts',(88.3909255993634,-2.88000925268686,-2.35989395274745));
#9526=CARTESIAN_POINT('Ctrl Pts',(88.3944347378501,-2.83613487198033,-2.41244502930289));
#9527=CARTESIAN_POINT('Ctrl Pts',(88.4003782403782,-2.76062702422136,-2.49797715936819));
#9528=CARTESIAN_POINT('Ctrl Pts',(88.4027807349994,-2.7297896093326,-2.53163976589444));
#9529=CARTESIAN_POINT('Ctrl Pts',(88.4076610982472,-2.66658071186967,-2.59814169273959));
#9530=CARTESIAN_POINT('Ctrl Pts',(88.4101390483007,-2.63420261666848,-2.63096356249864));
#9531=CARTESIAN_POINT('Ctrl Pts',(88.4164992171179,-2.55043293084138,-2.71278460780704));
#9532=CARTESIAN_POINT('Ctrl Pts',(88.4204159121678,-2.49823529902089,-2.76092881701725));
#9533=CARTESIAN_POINT('Ctrl Pts',(88.4292178137408,-2.37963729120204,-2.86419895946408));
#9534=CARTESIAN_POINT('Ctrl Pts',(88.4341277285961,-2.3126333094049,-2.91856729225456));
#9535=CARTESIAN_POINT('Ctrl Pts',(88.4515421286468,-2.07168127601554,-3.1005699659503));
#9536=CARTESIAN_POINT('Ctrl Pts',(88.464381802101,-1.88858947384899,-3.21537204128734));
#9537=CARTESIAN_POINT('Ctrl Pts',(88.4848148390558,-1.57904793569892,-3.37385799323009));
#9538=CARTESIAN_POINT('Ctrl Pts',(88.4924900246113,-1.4583614010496,-3.42775397885702));
#9539=CARTESIAN_POINT('Ctrl Pts',(88.502028059765,-1.29934536946942,-3.48884404558364));
#9540=CARTESIAN_POINT('Ctrl Pts',(88.5041459437752,-1.2634222934525,-3.50201306370316));
#9541=CARTESIAN_POINT('Ctrl Pts',(88.507607592847,-1.20355148370574,-3.52291984300524));
#9542=CARTESIAN_POINT('Ctrl Pts',(88.5089678672653,-1.17971740632928,-3.53097258094205));
#9543=CARTESIAN_POINT('Ctrl Pts',(88.5118627255322,-1.12829208302488,-3.54776860265111));
#9544=CARTESIAN_POINT('Ctrl Pts',(88.5133931338831,-1.10067756557123,-3.55643277509863));
#9545=CARTESIAN_POINT('Ctrl Pts',(88.5178810736388,-1.01855029465883,-3.5811523211024));
#9546=CARTESIAN_POINT('Ctrl Pts',(88.5207924273677,-0.963766057324589,-3.59628311808079));
#9547=CARTESIAN_POINT('Ctrl Pts',(88.5277085434199,-0.83076624075273,-3.62975837824628));
#9548=CARTESIAN_POINT('Ctrl Pts',(88.531666235363,-0.752260578365273,-3.64683747696754));
#9549=CARTESIAN_POINT('Ctrl Pts',(88.5430050657308,-0.523168863031586,-3.68896343098206));
#9550=CARTESIAN_POINT('Ctrl Pts',(88.5502556606628,-0.371519167082576,-3.70730796494108));
#9551=CARTESIAN_POINT('Ctrl Pts',(88.5659530603562,-0.0454642368930008,
-3.72653711703448));
#9552=CARTESIAN_POINT('Ctrl Pts',(88.5744104019956,0.128734914225388,-3.72458946953677));
#9553=CARTESIAN_POINT('Ctrl Pts',(88.5866464004245,0.369859855226244,-3.70495430767562));
#9554=CARTESIAN_POINT('Ctrl Pts',(88.5901305000481,0.437404254416894,-3.69758834042493));
#9555=CARTESIAN_POINT('Ctrl Pts',(88.595807138833,0.545341042563475,-3.68281858956291));
#9556=CARTESIAN_POINT('Ctrl Pts',(88.5979639292996,0.58587945749871,-3.67658737196949));
#9557=CARTESIAN_POINT('Ctrl Pts',(88.6025473616529,0.670976838102068,-3.66206380159366));
#9558=CARTESIAN_POINT('Ctrl Pts',(88.6049781783315,0.71550369373251,-3.65362497063357));
#9559=CARTESIAN_POINT('Ctrl Pts',(88.6110401221843,0.824998844997339,-3.63079487650112));
#9560=CARTESIAN_POINT('Ctrl Pts',(88.6146993266615,0.8897546904354,-3.61547097324373));
#9561=CARTESIAN_POINT('Ctrl Pts',(88.6283312126836,1.12605139098444,-3.5528207615217));
#9562=CARTESIAN_POINT('Ctrl Pts',(88.6386127284437,1.29453201990194,-3.49495381727692));
#9563=CARTESIAN_POINT('Ctrl Pts',(88.6639048739681,1.69070422161208,-3.32629440356851));
#9564=CARTESIAN_POINT('Ctrl Pts',(88.6790450116868,1.91251703535783,-3.20390408657019));
#9565=CARTESIAN_POINT('Ctrl Pts',(88.695824017371,2.15704541231188,-3.03447347045936));
#9566=CARTESIAN_POINT('Ctrl Pts',(88.6983197998562,2.19340366967098,-3.00829766516535));
#9567=CARTESIAN_POINT('Ctrl Pts',(88.702234949962,2.25058087167595,-2.96554557472101));
#9568=CARTESIAN_POINT('Ctrl Pts',(88.7036794952817,2.27170912181008,-2.94939190035971));
#9569=CARTESIAN_POINT('Ctrl Pts',(88.7065584232541,2.31392704295263,-2.91639119902499));
#9570=CARTESIAN_POINT('Ctrl Pts',(88.7079923220953,2.33501015366738,-2.89953852457337));
#9571=CARTESIAN_POINT('Ctrl Pts',(88.7118710237571,2.39211144376187,-2.85286813091862));
#9572=CARTESIAN_POINT('Ctrl Pts',(88.7142868069874,2.42775504930457,-2.82259801015629));
#9573=CARTESIAN_POINT('Ctrl Pts',(88.7250197460445,2.58577077741671,-2.68319567663285));
#9574=CARTESIAN_POINT('Ctrl Pts',(88.7329455114334,2.70143125993398,-2.56671523059201));
#9575=CARTESIAN_POINT('Ctrl Pts',(88.7534943810955,2.98233960389416,-2.24371496556524));
#9576=CARTESIAN_POINT('Ctrl Pts',(88.7660224629439,3.13393049565725,-2.02659235269491));
#9577=CARTESIAN_POINT('Ctrl Pts',(88.7827492310719,3.29315333297383,-1.737348313372));
#9578=CARTESIAN_POINT('Ctrl Pts',(88.7861443597917,3.3234843947264,-1.67859728600798));
#9579=CARTESIAN_POINT('Ctrl Pts',(88.7919284603268,3.37171604778075,-1.57873526970265));
#9580=CARTESIAN_POINT('Ctrl Pts',(88.7942884032278,3.3904677721366,-1.538051435188));
#9581=CARTESIAN_POINT('Ctrl Pts',(88.7991484089269,3.42717893766358,-1.45446698600369));
#9582=CARTESIAN_POINT('Ctrl Pts',(88.8016499525833,3.4450776820633,-1.41154850651784));
#9583=CARTESIAN_POINT('Ctrl Pts',(88.8081582148311,3.48907669736529,-1.30021974661874));
#9584=CARTESIAN_POINT('Ctrl Pts',(88.8122027366835,3.51397028608591,-1.23135673575019));
#9585=CARTESIAN_POINT('Ctrl Pts',(88.8213576283,3.56492768265269,-1.07623040719316));
#9586=CARTESIAN_POINT('Ctrl Pts',(88.8264961627339,3.58992217747943,-0.989665804135875));
#9587=CARTESIAN_POINT('Ctrl Pts',(88.8456145267138,3.67008303277628,-0.668790051456514));
#9588=CARTESIAN_POINT('Ctrl Pts',(88.860010743048,3.70563260448271,-0.430192759626316));
#9589=CARTESIAN_POINT('Ctrl Pts',(88.8800892350963,3.72318174986647,-0.0865362361471175));
#9590=CARTESIAN_POINT('Ctrl Pts',(88.8860444892711,3.72414901642061,0.0169684931800194));
#9591=CARTESIAN_POINT('Ctrl Pts',(88.8938416980841,3.71963348413003,0.156531915750616));
#9592=CARTESIAN_POINT('Ctrl Pts',(88.8958389585287,3.71793726594362,0.19266078435085));
#9593=CARTESIAN_POINT('Ctrl Pts',(88.8991786177201,3.71417079082982,0.253838948103428));
#9594=CARTESIAN_POINT('Ctrl Pts',(88.9005344810712,3.71237294848949,0.278901573804043));
#9595=CARTESIAN_POINT('Ctrl Pts',(88.903486058419,3.70786063795343,0.333984122159623));
#9596=CARTESIAN_POINT('Ctrl Pts',(88.9050761127884,3.70503518314193,0.363992187110998));
#9597=CARTESIAN_POINT('Ctrl Pts',(88.9099654414399,3.69512104083905,0.457149589248394));
#9598=CARTESIAN_POINT('Ctrl Pts',(88.9132053030085,3.68677953800527,0.520156453243628));
#9599=CARTESIAN_POINT('Ctrl Pts',(88.9211449827596,3.66198656661282,0.676540165080279));
#9600=CARTESIAN_POINT('Ctrl Pts',(88.9257770346585,3.64357360172728,0.769561717512575));
#9601=CARTESIAN_POINT('Ctrl Pts',(88.9453734479564,3.54975451915886,1.16383504216627));
#9602=CARTESIAN_POINT('Ctrl Pts',(88.9599042681047,3.44038240512592,1.45569059069758));
#9603=CARTESIAN_POINT('Ctrl Pts',(88.9789150292079,3.26628351775866,1.78727715231472));
#9604=CARTESIAN_POINT('Ctrl Pts',(88.9822089432988,3.23506071765283,1.84318994704575));
#9605=CARTESIAN_POINT('Ctrl Pts',(88.9878745966884,3.17973525009053,1.93652502756773));
#9606=CARTESIAN_POINT('Ctrl Pts',(88.9902202111532,3.15637478229152,1.97437166047396));
#9607=CARTESIAN_POINT('Ctrl Pts',(88.99509832939,3.10690779466692,2.05139141585444));
#9608=CARTESIAN_POINT('Ctrl Pts',(88.9976333096695,3.08072515318665,2.09050593012863));
#9609=CARTESIAN_POINT('Ctrl Pts',(89.0043458539657,3.01020054116036,2.19166013839208));
#9610=CARTESIAN_POINT('Ctrl Pts',(89.0085659127104,2.96468332354661,2.25284999896869));
#9611=CARTESIAN_POINT('Ctrl Pts',(89.0235158806796,2.79941859606333,2.46133011291959));
#9612=CARTESIAN_POINT('Ctrl Pts',(89.034576293122,2.67032539840791,2.60081519371446));
#9613=CARTESIAN_POINT('Ctrl Pts',(89.0590032766803,2.36650822081009,2.8825221331891));
#9614=CARTESIAN_POINT('Ctrl Pts',(89.0723763774385,2.1883564808912,3.02000017347433));
#9615=CARTESIAN_POINT('Ctrl Pts',(89.0874414131702,1.96260541531723,3.16368421629125));
#9616=CARTESIAN_POINT('Ctrl Pts',(89.0898341150602,1.92591810365992,3.18615090749703));
#9617=CARTESIAN_POINT('Ctrl Pts',(89.0936282618884,1.8662304856135,3.22129480869734));
#9618=CARTESIAN_POINT('Ctrl Pts',(89.0950523829701,1.84347166086447,3.23437301885312));
#9619=CARTESIAN_POINT('Ctrl Pts',(89.0979325178397,1.79666417301898,3.2606160276992));
#9620=CARTESIAN_POINT('Ctrl Pts',(89.0993872465129,1.77260487817393,3.27375794271531));
#9621=CARTESIAN_POINT('Ctrl Pts',(89.1033959931179,1.70522978174943,3.30959971015756));
#9622=CARTESIAN_POINT('Ctrl Pts',(89.1059175916601,1.66160741121389,3.33171428596256));
#9623=CARTESIAN_POINT('Ctrl Pts',(89.1116999232661,1.55912040002446,3.38115678139712));
#9624=CARTESIAN_POINT('Ctrl Pts',(89.1149319801386,1.49995111951618,3.407818207222));
#9625=CARTESIAN_POINT('Ctrl Pts',(89.1272487532407,1.26898963496278,3.50470673823234));
#9626=CARTESIAN_POINT('Ctrl Pts',(89.136032872342,1.09273259043286,3.5635999609455));
#9627=CARTESIAN_POINT('Ctrl Pts',(89.1539140185139,0.732213255348467,3.65478236498869));
#9628=CARTESIAN_POINT('Ctrl Pts',(89.1629903293211,0.548451413037632,3.68683645613083));
#9629=CARTESIAN_POINT('Ctrl Pts',(89.1755625381924,0.30278680742791,3.71091057225073));
#9630=CARTESIAN_POINT('Ctrl Pts',(89.1786876059433,0.242365807597258,3.7153459350924));
#9631=CARTESIAN_POINT('Ctrl Pts',(89.1841789574466,0.137544976599814,3.72047281307354));
#9632=CARTESIAN_POINT('Ctrl Pts',(89.1865241510833,0.093190541973855,3.72184791111675));
#9633=CARTESIAN_POINT('Ctrl Pts',(89.1914729873382,0.000523619055112301,
3.72306332900135));
#9634=CARTESIAN_POINT('Ctrl Pts',(89.1940806467488,-0.0477822142588712,
3.72275669244417));
#9635=CARTESIAN_POINT('Ctrl Pts',(89.2012555985288,-0.179211715953318,3.71936397562102));
#9636=CARTESIAN_POINT('Ctrl Pts',(89.20587696523,-0.262256342258192,3.71443203923228));
#9637=CARTESIAN_POINT('Ctrl Pts',(89.2166851209834,-0.452840211623173,3.6966904263104));
#9638=CARTESIAN_POINT('Ctrl Pts',(89.2229194763831,-0.560122945145468,3.68196198506632));
#9639=CARTESIAN_POINT('Ctrl Pts',(89.2385841869463,-0.824299585553218,3.63388068176301));
#9640=CARTESIAN_POINT('Ctrl Pts',(89.248098923262,-0.979972456563201,3.59502574567587));
#9641=CARTESIAN_POINT('Ctrl Pts',(89.2658772279148,-1.26773401371308,3.50311675968315));
#9642=CARTESIAN_POINT('Ctrl Pts',(89.2741419269388,-1.40025266201107,3.452285484909));
#9643=CARTESIAN_POINT('Ctrl Pts',(89.2842505168112,-1.56476492097124,3.3781459027993));
#9644=CARTESIAN_POINT('Ctrl Pts',(89.2863893941991,-1.59972614212561,3.36173102746785));
#9645=CARTESIAN_POINT('Ctrl Pts',(89.2898742818897,-1.65706668010135,3.33371152441502));
#9646=CARTESIAN_POINT('Ctrl Pts',(89.2912373073047,-1.67959440904065,3.32241858652376));
#9647=CARTESIAN_POINT('Ctrl Pts',(89.2941248181073,-1.72757054124143,3.29775586739967));
#9648=CARTESIAN_POINT('Ctrl Pts',(89.295645401778,-1.7529816170667,3.2843186947899));
#9649=CARTESIAN_POINT('Ctrl Pts',(89.3000726332398,-1.82728089756894,3.24392180068835));
#9650=CARTESIAN_POINT('Ctrl Pts',(89.3029349038935,-1.87572286928738,3.21615429447506));
#9651=CARTESIAN_POINT('Ctrl Pts',(89.3097037222228,-1.99054620475305,3.14685896049157));
#9652=CARTESIAN_POINT('Ctrl Pts',(89.3135658043411,-2.05627880024351,3.10430573145286));
#9653=CARTESIAN_POINT('Ctrl Pts',(89.3279815533104,-2.29942167297044,2.93578829575765));
#9654=CARTESIAN_POINT('Ctrl Pts',(89.3382058393382,-2.46687344235342,2.79653073526865));
#9655=CARTESIAN_POINT('Ctrl Pts',(89.3487674494621,-2.62112000711955,2.64359555733807));
#9656=CARTESIAN_POINT('Origin',(80.1322559480305,0.,0.));
#9657=CARTESIAN_POINT('',(89.5089317511108,-3.72371574749209,0.00232684839586724));
#9658=CARTESIAN_POINT('Ctrl Pts',(89.3487674494621,-2.62112000711955,2.64359555733807));
#9659=CARTESIAN_POINT('Ctrl Pts',(89.3529797741928,-2.68263871608259,2.58259987347577));
#9660=CARTESIAN_POINT('Ctrl Pts',(89.3572420136609,-2.74205702040921,2.51942838131009));
#9661=CARTESIAN_POINT('Ctrl Pts',(89.3656756632406,-2.853179327034,2.39268167386431));
#9662=CARTESIAN_POINT('Ctrl Pts',(89.369832700608,-2.90505703882765,2.32942058856126));
#9663=CARTESIAN_POINT('Ctrl Pts',(89.3765592883275,-2.98404385599776,2.22635576065072));
#9664=CARTESIAN_POINT('Ctrl Pts',(89.3790758305599,-3.01253811375682,2.18764520527887));
#9665=CARTESIAN_POINT('Ctrl Pts',(89.3839757636083,-3.06594189295966,2.11207151816034));
#9666=CARTESIAN_POINT('Ctrl Pts',(89.3863546743921,-3.09095586216386,2.07529212844363));
#9667=CARTESIAN_POINT('Ctrl Pts',(89.3920672311352,-3.14883459893498,1.98682142883577));
#9668=CARTESIAN_POINT('Ctrl Pts',(89.395421829218,-3.18109364008708,1.93475098583921));
#9669=CARTESIAN_POINT('Ctrl Pts',(89.4100519670901,-3.31437529037645,1.70726532986437));
#9670=CARTESIAN_POINT('Ctrl Pts',(89.4217623866582,-3.40227226634272,1.52458661664443));
#9671=CARTESIAN_POINT('Ctrl Pts',(89.4479525859899,-3.56198134792401,1.10909395211884));
#9672=CARTESIAN_POINT('Ctrl Pts',(89.4624645439403,-3.62671150748733,0.874513249080568));
#9673=CARTESIAN_POINT('Ctrl Pts',(89.4785770302165,-3.67553767807969,0.592594548908786));
#9674=CARTESIAN_POINT('Ctrl Pts',(89.4809882160038,-3.68218712340376,0.54976706659954));
#9675=CARTESIAN_POINT('Ctrl Pts',(89.4848047716062,-3.69167116223613,0.480754062023185));
#9676=CARTESIAN_POINT('Ctrl Pts',(89.4862332372311,-3.69497830122412,0.45463822564063));
#9677=CARTESIAN_POINT('Ctrl Pts',(89.4888859989603,-3.70066628243186,0.405548898349816));
#9678=CARTESIAN_POINT('Ctrl Pts',(89.4901139226997,-3.70311083491576,0.382584686000311));
#9679=CARTESIAN_POINT('Ctrl Pts',(89.4928019861062,-3.70803668507492,0.331828214641216));
#9680=CARTESIAN_POINT('Ctrl Pts',(89.4942571729711,-3.71041956024529,0.304027619698432));
#9681=CARTESIAN_POINT('Ctrl Pts',(89.5004197418618,-3.71926890458101,0.18508175469496));
#9682=CARTESIAN_POINT('Ctrl Pts',(89.5049934840879,-3.72269148191928,0.0937369082323972));
#9683=CARTESIAN_POINT('Ctrl Pts',(89.5094878198556,-3.72274925601168,0.00235358545693844));
#9684=CARTESIAN_POINT('',(90.4429666115571,0.0630273376275202,3.72323065059699));
#9685=CARTESIAN_POINT('Ctrl Pts',(89.5089317511109,-3.72371574749208,0.0023268483958672));
#9686=CARTESIAN_POINT('Ctrl Pts',(89.5144493688092,-3.72357263772784,-0.107412055256537));
#9687=CARTESIAN_POINT('Ctrl Pts',(89.5198863329416,-3.71852748988571,-0.217314149425214));
#9688=CARTESIAN_POINT('Ctrl Pts',(89.5253164743333,-3.70860419682644,-0.326901558437555));
#9689=CARTESIAN_POINT('Ctrl Pts',(89.530740622285,-3.69869185645852,-0.436368011930497));
#9690=CARTESIAN_POINT('Ctrl Pts',(89.5361583414371,-3.68391252706447,-0.545520371229198));
#9691=CARTESIAN_POINT('Ctrl Pts',(89.5416289472312,-3.66433387024312,-0.653894300217409));
#9692=CARTESIAN_POINT('Ctrl Pts',(89.547095047411,-3.64477133848699,-0.762178971975731));
#9693=CARTESIAN_POINT('Ctrl Pts',(89.5526141925419,-3.62041766047029,-0.869686450491287));
#9694=CARTESIAN_POINT('Ctrl Pts',(89.558226648156,-3.59137910554205,-0.975966541823195));
#9695=CARTESIAN_POINT('Ctrl Pts',(89.5638366528022,-3.56235323179511,-1.08220022047689));
#9696=CARTESIAN_POINT('Ctrl Pts',(89.5695400284607,-3.5286467523647,-1.18720755362765));
#9697=CARTESIAN_POINT('Ctrl Pts',(89.5753552132139,-3.4904011333468,-1.29055246128007));
#9698=CARTESIAN_POINT('Ctrl Pts',(89.5811693810291,-3.4521622025814,-1.393879296357));
#9699=CARTESIAN_POINT('Ctrl Pts',(89.5870953775833,-3.40938581625973,-1.49554425436715));
#9700=CARTESIAN_POINT('Ctrl Pts',(89.5931283660254,-3.3622466314541,-1.59512547099244));
#9701=CARTESIAN_POINT('Ctrl Pts',(89.5991618790538,-3.3151033477561,-1.6947153465008));
#9702=CARTESIAN_POINT('Ctrl Pts',(89.6053023841074,-3.26359652083738,-1.79222107456204));
#9703=CARTESIAN_POINT('Ctrl Pts',(89.6115214661064,-3.20793329375971,-1.88723523931771));
#9704=CARTESIAN_POINT('Ctrl Pts',(89.6177464373095,-3.15221735599179,-1.98233937841498));
#9705=CARTESIAN_POINT('Ctrl Pts',(89.6240500301323,-3.0923370587168,-2.07494716306154));
#9706=CARTESIAN_POINT('Ctrl Pts',(89.6303810247902,-3.02853314866813,-2.16466544028031));
#9707=CARTESIAN_POINT('Ctrl Pts',(89.6367151237953,-2.96469795293667,-2.25442771006255));
#9708=CARTESIAN_POINT('Ctrl Pts',(89.64307642923,-2.89693510650364,-2.34129751029344));
#9709=CARTESIAN_POINT('Ctrl Pts',(89.6493933299385,-2.82552077623839,-2.42489797482477));
#9710=CARTESIAN_POINT('Ctrl Pts',(89.6557200436836,-2.75399550684918,-2.50862830912122));
#9711=CARTESIAN_POINT('Ctrl Pts',(89.6620018381212,-2.67880709980692,-2.58907888684311));
#9712=CARTESIAN_POINT('Ctrl Pts',(89.6681508424376,-2.60027188408617,-2.66589079960463));
#9713=CARTESIAN_POINT('Ctrl Pts',(89.6728964356274,-2.53966106553649,-2.72517163131961));
#9714=CARTESIAN_POINT('Ctrl Pts',(89.6775625153991,-2.477057541777,-2.78228549830324));
#9715=CARTESIAN_POINT('Ctrl Pts',(89.6821048509549,-2.41262437404084,-2.83707738434133));
#9716=CARTESIAN_POINT('Ctrl Pts',(89.6821072920214,-2.41258974743762,-2.83710682968702));
#9717=CARTESIAN_POINT('Ctrl Pts',(89.6821097330548,-2.4125551202594,-2.83713627440416));
#9718=CARTESIAN_POINT('Ctrl Pts',(89.6821121740549,-2.41252049250622,-2.8371657184927));
#9719=CARTESIAN_POINT('Ctrl Pts',(89.6874488481156,-2.33681503472848,-2.90153830975086));
#9720=CARTESIAN_POINT('Ctrl Pts',(89.6926267789551,-2.25835696697216,-2.96290651400831));
#9721=CARTESIAN_POINT('Ctrl Pts',(89.6977083378158,-2.17743387421516,-3.0210494835982));
#9722=CARTESIAN_POINT('Ctrl Pts',(89.6982961279809,-2.16807340051844,-3.02777495242241));
#9723=CARTESIAN_POINT('Ctrl Pts',(89.6988826287051,-2.15868000253057,-3.03445726790254));
#9724=CARTESIAN_POINT('Ctrl Pts',(89.6994679365177,-2.1492541702095,-3.04109608898255));
#9725=CARTESIAN_POINT('Ctrl Pts',(89.7051084814648,-2.05841849414079,-3.10507365409939));
#9726=CARTESIAN_POINT('Ctrl Pts',(89.7106388626614,-1.96456457426539,-3.16501220907957));
#9727=CARTESIAN_POINT('Ctrl Pts',(89.7161398493902,-1.86811509933513,-3.22065648999706));
#9728=CARTESIAN_POINT('Ctrl Pts',(89.7216353495229,-1.7717618215652,-3.27624527220066));
#9729=CARTESIAN_POINT('Ctrl Pts',(89.7271019533148,-1.67281850372914,-3.32754867921573));
#9730=CARTESIAN_POINT('Ctrl Pts',(89.732606643235,-1.57172006659594,-3.37435762076696));
#9731=CARTESIAN_POINT('Ctrl Pts',(89.7381075151489,-1.47069175048162,-3.42113409603317));
#9732=CARTESIAN_POINT('Ctrl Pts',(89.7436467064045,-1.36751150125765,-3.4634226070263));
#9733=CARTESIAN_POINT('Ctrl Pts',(89.7492721239457,-1.26262286082101,-3.50105529733182));
#9734=CARTESIAN_POINT('Ctrl Pts',(89.7548954830333,-1.15777260124904,-3.53867421707851));
#9735=CARTESIAN_POINT('Ctrl Pts',(89.760605173825,-1.05121531499535,-3.5716409057542));
#9736=CARTESIAN_POINT('Ctrl Pts',(89.7664267450917,-0.943401282902844,-3.59982509011847));
#9737=CARTESIAN_POINT('Ctrl Pts',(89.7722476261605,-0.835600033102613,-3.62800593300228));
#9738=CARTESIAN_POINT('Ctrl Pts',(89.7781804392221,-0.726542398257346,-3.65140550588009));
#9739=CARTESIAN_POINT('Ctrl Pts',(89.7842265888405,-0.616684413474052,-3.66992886131566));
#9740=CARTESIAN_POINT('Ctrl Pts',(89.7902735172042,-0.506812278960044,-3.68845460256317));
#9741=CARTESIAN_POINT('Ctrl Pts',(89.7964338106735,-0.396139610282474,-3.70210288836393));
#9742=CARTESIAN_POINT('Ctrl Pts',(89.8026841522676,-0.285127903742074,-3.71081313279568));
#9743=CARTESIAN_POINT('Ctrl Pts',(89.8089408354159,-0.174003565477832,-3.71953221458231));
#9744=CARTESIAN_POINT('Ctrl Pts',(89.8152876659514,-0.0625394855586726,
-3.72330314762807));
#9745=CARTESIAN_POINT('Ctrl Pts',(89.8216770954455,0.0487961803852812,-3.72210009108173));
#9746=CARTESIAN_POINT('Ctrl Pts',(89.8280697237272,0.160187585132733,-3.72089643224024));
#9747=CARTESIAN_POINT('Ctrl Pts',(89.8345047957465,0.271450483496589,-3.7147135964053));
#9748=CARTESIAN_POINT('Ctrl Pts',(89.8409126010786,0.38211034631084,-3.70356277017798));
#9749=CARTESIAN_POINT('Ctrl Pts',(89.8473309919939,0.492953017297544,-3.69239352297929));
#9750=CARTESIAN_POINT('Ctrl Pts',(89.8537216764366,0.603190667762472,-3.67623947787963));
#9751=CARTESIAN_POINT('Ctrl Pts',(89.8599964980888,0.712340311951511,-3.65515343115013));
#9752=CARTESIAN_POINT('Ctrl Pts',(89.8657030852584,0.81160559686597,-3.63597689189637));
#9753=CARTESIAN_POINT('Ctrl Pts',(89.871313353658,0.909971355674651,-3.61272118873168));
#9754=CARTESIAN_POINT('Ctrl Pts',(89.8767525586254,1.00706894884951,-3.58546115444386));
#9755=CARTESIAN_POINT('Ctrl Pts',(89.8770619556114,1.01259212785528,-3.58391052847928));
#9756=CARTESIAN_POINT('Ctrl Pts',(89.8773707990964,1.01811121649432,-3.58234695125233));
#9757=CARTESIAN_POINT('Ctrl Pts',(89.8776790753233,1.02362615165207,-3.5807704383915));
#9758=CARTESIAN_POINT('Ctrl Pts',(89.8776815122706,1.02366974763763,-3.58075797593638));
#9759=CARTESIAN_POINT('Ctrl Pts',(89.8776839491846,1.02371334341927,-3.58074551265842));
#9760=CARTESIAN_POINT('Ctrl Pts',(89.8776863860656,1.02375693899699,-3.58073304855759));
#9761=CARTESIAN_POINT('Ctrl Pts',(89.8830296183515,1.11934687701787,-3.55340361085902));
#9762=CARTESIAN_POINT('Ctrl Pts',(89.8882135303408,1.21395884304279,-3.52211453451959));
#9763=CARTESIAN_POINT('Ctrl Pts',(89.8933001623114,1.3072499547986,-3.4869829616927));
#9764=CARTESIAN_POINT('Ctrl Pts',(89.8938972847919,1.31820144890839,-3.48285884734097));
#9765=CARTESIAN_POINT('Ctrl Pts',(89.8944930667014,1.32913470820646,-3.4786818304396));
#9766=CARTESIAN_POINT('Ctrl Pts',(89.8950876084025,1.34004915277909,-3.47445214012305));
#9767=CARTESIAN_POINT('Ctrl Pts',(89.900741891935,1.44384904451091,-3.43422641961143));
#9768=CARTESIAN_POINT('Ctrl Pts',(89.9062846299621,1.545950830139,-3.38923164780696));
#9769=CARTESIAN_POINT('Ctrl Pts',(89.9117967189255,1.64590618376087,-3.33967935958924));
#9770=CARTESIAN_POINT('Ctrl Pts',(89.9173032706963,1.74576112680444,-3.29017684933473));
#9771=CARTESIAN_POINT('Ctrl Pts',(89.9227796787904,1.84347404259024,-3.23612644845506));
#9772=CARTESIAN_POINT('Ctrl Pts',(89.9282931675701,1.93862843278367,-3.17777550341602));
#9773=CARTESIAN_POINT('Ctrl Pts',(89.9338027148404,2.03371479854958,-3.11946627258085));
#9774=CARTESIAN_POINT('Ctrl Pts',(89.9393495788318,2.12624641327672,-3.05686295954206));
#9775=CARTESIAN_POINT('Ctrl Pts',(89.9449819661159,2.21583646266807,-2.99024292319167));
#9776=CARTESIAN_POINT('Ctrl Pts',(89.9506122147042,2.30539249347191,-2.92364818339543));
#9777=CARTESIAN_POINT('Ctrl Pts',(89.9563280920228,2.39200928482382,-2.85303996676748));
#9778=CARTESIAN_POINT('Ctrl Pts',(89.9621554707194,2.47532764309845,-2.77872204621894));
#9779=CARTESIAN_POINT('Ctrl Pts',(89.9679820610267,2.55863472918569,-2.70441418018354));
#9780=CARTESIAN_POINT('Ctrl Pts',(89.9739202015018,2.63864432622805,-2.62639772042333));
#9781=CARTESIAN_POINT('Ctrl Pts',(89.9799716257893,2.71502347934517,-2.54500079096971));
#9782=CARTESIAN_POINT('Ctrl Pts',(89.9860237104523,2.79141096751009,-2.4635949788921));
#9783=CARTESIAN_POINT('Ctrl Pts',(89.9921891031505,2.86416722408592,-2.3788079853391));
#9784=CARTESIAN_POINT('Ctrl Pts',(89.9984448156139,2.93298485751985,-2.29099153144459));
#9785=CARTESIAN_POINT('Ctrl Pts',(90.0047065906403,3.00186918379431,-2.20308997249105));
#9786=CARTESIAN_POINT('Ctrl Pts',(90.0110587764147,3.06680718997094,-2.11215301755072));
#9787=CARTESIAN_POINT('Ctrl Pts',(90.0174541626742,3.12751670253634,-2.01855720431008));
#9788=CARTESIAN_POINT('Ctrl Pts',(90.0238526125877,3.18825529746403,-1.92491655481174));
#9789=CARTESIAN_POINT('Ctrl Pts',(90.030294105395,3.24476119420331,-1.82861435236295));
#9790=CARTESIAN_POINT('Ctrl Pts',(90.0367092909392,3.29677947739771,-1.7300530380692));
#9791=CARTESIAN_POINT('Ctrl Pts',(90.043134691733,3.34888059214043,-1.63133477922123));
#9792=CARTESIAN_POINT('Ctrl Pts',(90.0495333501238,3.39647947670092,-1.53034998886078));
#9793=CARTESIAN_POINT('Ctrl Pts',(90.0558175263701,3.43935117920548,-1.4275312671387));
#9794=CARTESIAN_POINT('Ctrl Pts',(90.0617137179113,3.47957598509268,-1.33106056779102));
#9795=CARTESIAN_POINT('Ctrl Pts',(90.0675085846285,3.51563920871451,-1.2329755145455));
#9796=CARTESIAN_POINT('Ctrl Pts',(90.0731205045349,3.54738485993372,-1.1336585668842));
#9797=CARTESIAN_POINT('Ctrl Pts',(90.0731228130997,3.54739791908159,-1.13361771106126));
#9798=CARTESIAN_POINT('Ctrl Pts',(90.0731251216355,3.5474109775156,-1.13357685498283));
#9799=CARTESIAN_POINT('Ctrl Pts',(90.0731274301423,3.5474240352357,-1.13353599864897));
#9800=CARTESIAN_POINT('Ctrl Pts',(90.0785089336928,3.57786369706669,-1.03829326282715));
#9801=CARTESIAN_POINT('Ctrl Pts',(90.0837330158939,3.60442229610753,-0.941658259288835));
#9802=CARTESIAN_POINT('Ctrl Pts',(90.0888624878585,3.62700700971911,-0.843986516594742));
#9803=CARTESIAN_POINT('Ctrl Pts',(90.0894422182873,3.62955952307635,-0.832947703699474));
#9804=CARTESIAN_POINT('Ctrl Pts',(90.0900207402207,3.63206129679853,-0.82189569892181));
#9805=CARTESIAN_POINT('Ctrl Pts',(90.0905981443356,3.63451221327311,-0.810831053933906));
#9806=CARTESIAN_POINT('Ctrl Pts',(90.0962795442613,3.65862814233822,-0.701959863738108));
#9807=CARTESIAN_POINT('Ctrl Pts',(90.1018533394814,3.67781824642278,-0.591859185322982));
#9808=CARTESIAN_POINT('Ctrl Pts',(90.107399858104,3.69201071129179,-0.481020504528848));
#9809=CARTESIAN_POINT('Ctrl Pts',(90.112940950973,3.7061892927104,-0.370290249109893));
#9810=CARTESIAN_POINT('Ctrl Pts',(90.1184552562561,3.71538045084791,-0.258823609572112));
#9811=CARTESIAN_POINT('Ctrl Pts',(90.1240089386278,3.71955946056852,-0.147105405430518));
#9812=CARTESIAN_POINT('Ctrl Pts',(90.1295588275376,3.72373561580207,-0.0354635107954085));
#9813=CARTESIAN_POINT('Ctrl Pts',(90.1351483217634,3.72290679006134,0.0764295340686877));
#9814=CARTESIAN_POINT('Ctrl Pts',(90.140824191506,3.71708940717279,0.188096888452428));
#9815=CARTESIAN_POINT('Ctrl Pts',(90.1464980116806,3.71127412495294,0.299723919529344));
#9816=CARTESIAN_POINT('Ctrl Pts',(90.1522583096122,3.70047409704029,0.411125395761373));
#9817=CARTESIAN_POINT('Ctrl Pts',(90.1581292358594,3.68474284199021,0.521832672354837));
#9818=CARTESIAN_POINT('Ctrl Pts',(90.1639994626508,3.66901346114476,0.632526759403664));
#9819=CARTESIAN_POINT('Ctrl Pts',(90.1699803652306,3.64835413879587,0.742526800876524));
#9820=CARTESIAN_POINT('Ctrl Pts',(90.1760717472594,3.62285309736902,0.851372273936879));
#9821=CARTESIAN_POINT('Ctrl Pts',(90.1821638774131,3.59734892398235,0.960231115064904));
#9822=CARTESIAN_POINT('Ctrl Pts',(90.1883665079535,3.56700185768382,1.06793509862119));
#9823=CARTESIAN_POINT('Ctrl Pts',(90.1946545894918,3.53193393770647,1.17403160929122));
#9824=CARTESIAN_POINT('Ctrl Pts',(90.2009488270132,3.49683168650664,1.28023198762478));
#9825=CARTESIAN_POINT('Ctrl Pts',(90.2073285908265,3.45699923761497,1.38482173281706));
#9826=CARTESIAN_POINT('Ctrl Pts',(90.2137445723081,3.41259342922832,1.48735510350216));
#9827=CARTESIAN_POINT('Ctrl Pts',(90.2201636768321,3.36816600587628,1.58993838331716));
#9828=CARTESIAN_POINT('Ctrl Pts',(90.2266188231901,3.31916054605349,1.69046324136125));
#9829=CARTESIAN_POINT('Ctrl Pts',(90.233038676517,3.26577094640859,1.78849187087495));
#9830=CARTESIAN_POINT('Ctrl Pts',(90.239468716635,3.2122966300783,1.88667604867183));
#9831=CARTESIAN_POINT('Ctrl Pts',(90.2458629821864,3.15442387293282,1.98235592320623));
#9832=CARTESIAN_POINT('Ctrl Pts',(90.2521320849717,3.09238895186967,2.07510156630849));
#9833=CARTESIAN_POINT('Ctrl Pts',(90.2579064984125,3.03524915144765,2.16052873291163));
#9834=CARTESIAN_POINT('Ctrl Pts',(90.263574174664,2.97457828973752,2.24346635863138));
#9835=CARTESIAN_POINT('Ctrl Pts',(90.2690571354595,2.91059682083417,2.32358854504316));
#9836=CARTESIAN_POINT('Ctrl Pts',(90.2690597464048,2.91056635333286,2.32362669863453));
#9837=CARTESIAN_POINT('Ctrl Pts',(90.2690623573112,2.91053588503632,2.32366485164704));
#9838=CARTESIAN_POINT('Ctrl Pts',(90.2690649681786,2.91050541594457,2.32370300408063));
#9839=CARTESIAN_POINT('Ctrl Pts',(90.2742912628997,2.84951401777874,2.40007450498025));
#9840=CARTESIAN_POINT('Ctrl Pts',(90.279361515835,2.78533191663936,2.47412713275621));
#9841=CARTESIAN_POINT('Ctrl Pts',(90.2843364642347,2.71818833114402,2.54559156128984));
#9842=CARTESIAN_POINT('Ctrl Pts',(90.2848916878766,2.71069484516782,2.55356727019879));
#9843=CARTESIAN_POINT('Ctrl Pts',(90.2854457244594,2.70316452526199,2.56151073285841));
#9844=CARTESIAN_POINT('Ctrl Pts',(90.2859986584125,2.69559772974738,2.56942156881173));
#9845=CARTESIAN_POINT('Ctrl Pts',(90.2915013907409,2.62029388909111,2.648149258616));
#9846=CARTESIAN_POINT('Ctrl Pts',(90.2968955092956,2.54137164504299,2.7236468238917));
#9847=CARTESIAN_POINT('Ctrl Pts',(90.3022592981764,2.45917985900135,2.79558902582741));
#9848=CARTESIAN_POINT('Ctrl Pts',(90.3076891130458,2.37597632658979,2.86841680605698));
#9849=CARTESIAN_POINT('Ctrl Pts',(90.313088318592,2.2894226369102,2.93760128305359));
#9850=CARTESIAN_POINT('Ctrl Pts',(90.3185249978489,2.19990511535511,3.00284842676939));
#9851=CARTESIAN_POINT('Ctrl Pts',(90.3238866980851,2.11162215919905,3.06719572579984));
#9852=CARTESIAN_POINT('Ctrl Pts',(90.3292850898537,2.02045687391114,3.12771381930532));
#9853=CARTESIAN_POINT('Ctrl Pts',(90.3347675827141,1.92679819254861,3.1841592531776));
#9854=CARTESIAN_POINT('Ctrl Pts',(90.3402483626254,1.83316877388635,3.24058705124945));
#9855=CARTESIAN_POINT('Ctrl Pts',(90.3458133571018,1.73704769886038,3.2929448632473));
#9856=CARTESIAN_POINT('Ctrl Pts',(90.3514888410463,1.63883842014456,3.34102540163832));
#9857=CARTESIAN_POINT('Ctrl Pts',(90.3571640816788,1.54063335172977,3.38910387878275));
#9858=CARTESIAN_POINT('Ctrl Pts',(90.3629498814715,1.44034038203927,3.43290551935315));
#9859=CARTESIAN_POINT('Ctrl Pts',(90.3688495987068,1.33837552613422,3.47225751229601));
#9860=CARTESIAN_POINT('Ctrl Pts',(90.3748968291848,1.23386119777986,3.51259344054621));
#9861=CARTESIAN_POINT('Ctrl Pts',(90.3810638525647,1.12759036442714,3.54825428961313));
#9862=CARTESIAN_POINT('Ctrl Pts',(90.3873286302831,1.02002315918263,3.57909084133929));
#9863=CARTESIAN_POINT('Ctrl Pts',(90.3934482336772,0.914948619605076,3.60921281455055));
#9864=CARTESIAN_POINT('Ctrl Pts',(90.3996609409719,0.808637163127249,3.63473156593701));
#9865=CARTESIAN_POINT('Ctrl Pts',(90.4059228398357,0.701528198865719,3.65554273541497));
#9866=CARTESIAN_POINT('Ctrl Pts',(90.412407563663,0.590607842630952,3.67709445471385));
#9867=CARTESIAN_POINT('Ctrl Pts',(90.4189449773761,0.478832125313426,3.69359719226042));
#9868=CARTESIAN_POINT('Ctrl Pts',(90.4254623811125,0.366700747059007,3.70497562314993));
#9869=CARTESIAN_POINT('Ctrl Pts',(90.4313363109118,0.265640283290959,3.71523064293606));
#9870=CARTESIAN_POINT('Ctrl Pts',(90.4371936819014,0.16429017486761,3.72132334342145));
#9871=CARTESIAN_POINT('Ctrl Pts',(90.4429666115571,0.06302733762752,3.72323065059699));
#9872=CARTESIAN_POINT('',(90.4430005297901,3.5302572329849,1.18158852036477));
#9873=CARTESIAN_POINT('Origin',(90.4430005297901,0.,0.));
#9874=CARTESIAN_POINT('',(89.755930604391,-3.72148643608346,0.000620124237849482));
#9875=CARTESIAN_POINT('Ctrl Pts',(89.755930604391,-3.72148643608346,0.000620124237849362));
#9876=CARTESIAN_POINT('Ctrl Pts',(89.7621758663193,-3.72148320024645,-0.11604520301192));
#9877=CARTESIAN_POINT('Ctrl Pts',(89.7682938357506,-3.71606355130549,-0.232631117773188));
#9878=CARTESIAN_POINT('Ctrl Pts',(89.7742966682074,-3.70526701499799,-0.348632458025145));
#9879=CARTESIAN_POINT('Ctrl Pts',(89.7803063561815,-3.69445814853769,-0.464766277269504));
#9880=CARTESIAN_POINT('Ctrl Pts',(89.7862007878316,-3.67825993465173,-0.580314274054517));
#9881=CARTESIAN_POINT('Ctrl Pts',(89.7920199315015,-3.65674536414029,-0.694770939840757));
#9882=CARTESIAN_POINT('Ctrl Pts',(89.7978513367025,-3.63518546022771,-0.809468777531487));
#9883=CARTESIAN_POINT('Ctrl Pts',(89.8036073909849,-3.60828645199377,-0.923070712205742));
#9884=CARTESIAN_POINT('Ctrl Pts',(89.809353237266,-3.57615892948402,-1.03506848814753));
#9885=CARTESIAN_POINT('Ctrl Pts',(89.8151055960043,-3.54399499299757,-1.14719320460903));
#9886=CARTESIAN_POINT('Ctrl Pts',(89.8208481430059,-3.50659021610027,-1.25771004248434));
#9887=CARTESIAN_POINT('Ctrl Pts',(89.8266661761538,-3.46409864915259,-1.36610976445866));
#9888=CARTESIAN_POINT('Ctrl Pts',(89.831946043114,-3.42553753842782,-1.46448254715063));
#9889=CARTESIAN_POINT('Ctrl Pts',(89.8372885959291,-3.38278668155183,-1.56111247008492));
#9890=CARTESIAN_POINT('Ctrl Pts',(89.8427666109971,-3.33599933114379,-1.65561882580734));
#9891=CARTESIAN_POINT('Ctrl Pts',(89.8433373580716,-3.33112461958535,-1.66546531680476));
#9892=CARTESIAN_POINT('Ctrl Pts',(89.8439095756265,-3.326206091597,-1.67528880256419));
#9893=CARTESIAN_POINT('Ctrl Pts',(89.8444833459717,-3.32124392029627,-1.6850888851092));
#9894=CARTESIAN_POINT('Ctrl Pts',(89.8474441542933,-3.29563779024094,-1.73565993011997));
#9895=CARTESIAN_POINT('Ctrl Pts',(89.8504464360192,-3.26887033107731,-1.78560634631337));
#9896=CARTESIAN_POINT('Ctrl Pts',(89.8535017500722,-3.24097044142362,-1.83487015331027));
#9897=CARTESIAN_POINT('Ctrl Pts',(89.8535044174161,-3.24094608432016,-1.83491316149629));
#9898=CARTESIAN_POINT('Ctrl Pts',(89.8535070848004,-3.24092172635365,-1.83495616916238));
#9899=CARTESIAN_POINT('Ctrl Pts',(89.8535097522252,-3.24089736752414,-1.83499917630854));
#9900=CARTESIAN_POINT('Ctrl Pts',(89.8589137387239,-3.19154835179572,-1.92212817122396));
#9901=CARTESIAN_POINT('Ctrl Pts',(89.8644938487987,-3.13852061015129,-2.00734601212772));
#9902=CARTESIAN_POINT('Ctrl Pts',(89.8701750604681,-3.08201730534746,-2.09034505631457));
#9903=CARTESIAN_POINT('Ctrl Pts',(89.8707320000666,-3.07647818275871,-2.09848160482437));
#9904=CARTESIAN_POINT('Ctrl Pts',(89.8712899112757,-3.07090569774484,-2.10659681532305));
#9905=CARTESIAN_POINT('Ctrl Pts',(89.8718487234165,-3.06530006698725,-2.11469038882675));
#9906=CARTESIAN_POINT('Ctrl Pts',(89.8780998110759,-3.00259332407221,-2.20522821675504));
#9907=CARTESIAN_POINT('Ctrl Pts',(89.8844631004165,-2.93573350537016,-2.29306097761275));
#9908=CARTESIAN_POINT('Ctrl Pts',(89.8908510398042,-2.86502180238879,-2.37781936750945));
#9909=CARTESIAN_POINT('Ctrl Pts',(89.8972325996347,-2.79438071832383,-2.46249311023463));
#9910=CARTESIAN_POINT('Ctrl Pts',(89.9036384191999,-2.71989569341618,-2.54409887403038));
#9911=CARTESIAN_POINT('Ctrl Pts',(89.909999111458,-2.64189179399096,-2.6223018081862));
#9912=CARTESIAN_POINT('Ctrl Pts',(89.9164074630992,-2.56330342709214,-2.70109070114267));
#9913=CARTESIAN_POINT('Ctrl Pts',(89.9227697801519,-2.48114335343996,-2.7764256997981));
#9914=CARTESIAN_POINT('Ctrl Pts',(89.9290375863566,-2.39576662525555,-2.84799545090647));
#9915=CARTESIAN_POINT('Ctrl Pts',(89.9352525739387,-2.31110936430494,-2.91896208577991));
#9916=CARTESIAN_POINT('Ctrl Pts',(89.9413745830721,-2.22328951831127,-2.98622675999417));
#9917=CARTESIAN_POINT('Ctrl Pts',(89.9473803537221,-2.13267399349501,-3.04951465433723));
#9918=CARTESIAN_POINT('Ctrl Pts',(89.9533856409564,-2.04206576249122,-3.11279745451974));
#9919=CARTESIAN_POINT('Ctrl Pts',(89.9592747054459,-1.94866232073446,-3.1721040811871));
#9920=CARTESIAN_POINT('Ctrl Pts',(89.9650488471482,-1.85285062128836,-3.22718824679365));
#9921=CARTESIAN_POINT('Ctrl Pts',(89.9708240154301,-1.75702188756238,-3.28228220576677));
#9922=CARTESIAN_POINT('Ctrl Pts',(89.9764842926361,-1.65878403119107,-3.33315208754173));
#9923=CARTESIAN_POINT('Ctrl Pts',(89.9820550254397,-1.55854429019367,-3.3795810664276));
#9924=CARTESIAN_POINT('Ctrl Pts',(89.9877080358082,-1.4568240470652,-3.42669578334012));
#9925=CARTESIAN_POINT('Ctrl Pts',(89.9932689499082,-1.3530422664884,-3.46923715542868));
#9926=CARTESIAN_POINT('Ctrl Pts',(89.998787728209,-1.24764593410952,-3.50701223733093));
#9927=CARTESIAN_POINT('Ctrl Pts',(90.0042355328496,-1.14360504002895,-3.54430151681884));
#9928=CARTESIAN_POINT('Ctrl Pts',(90.0096426030432,-1.03799086801436,-3.57694607131596));
#9929=CARTESIAN_POINT('Ctrl Pts',(90.015076291169,-0.93125450523574,-3.60479654993437));
#9930=CARTESIAN_POINT('Ctrl Pts',(90.0206161639213,-0.822432310411888,-3.63319128000809));
#9931=CARTESIAN_POINT('Ctrl Pts',(90.0261841147079,-0.712443581167876,-3.65660210740134));
#9932=CARTESIAN_POINT('Ctrl Pts',(90.0318663644519,-0.601789039154095,-3.67491544567526));
#9933=CARTESIAN_POINT('Ctrl Pts',(90.03687762912,-0.504201072810251,-3.6910662643095));
#9934=CARTESIAN_POINT('Ctrl Pts',(90.0419783102061,-0.406094477094452,-3.70325271084103));
#9935=CARTESIAN_POINT('Ctrl Pts',(90.047232028394,-0.307830069065341,-3.71143138244006));
#9936=CARTESIAN_POINT('Ctrl Pts',(90.0479331053229,-0.294717277907041,-3.71252277671782));
#9937=CARTESIAN_POINT('Ctrl Pts',(90.0486369074277,-0.281601620847862,-3.71354285516211));
#9938=CARTESIAN_POINT('Ctrl Pts',(90.0493435858886,-0.268483902733631,-3.71449156145726));
#9939=CARTESIAN_POINT('Ctrl Pts',(90.0493459763846,-0.268439529153975,-3.71449477066591));
#9940=CARTESIAN_POINT('Ctrl Pts',(90.0493483669136,-0.268395155550725,-3.71449797905786));
#9941=CARTESIAN_POINT('Ctrl Pts',(90.0493507574754,-0.268350781923909,-3.71450118663316));
#9942=CARTESIAN_POINT('Ctrl Pts',(90.0547735338317,-0.167693167150674,-3.72177728510962));
#9943=CARTESIAN_POINT('Ctrl Pts',(90.0603779902922,-0.0666090155227414,
-3.72486349689355));
#9944=CARTESIAN_POINT('Ctrl Pts',(90.0660918238188,0.0345328598509972,-3.72376215121569));
#9945=CARTESIAN_POINT('Ctrl Pts',(90.0667434557154,0.0460675452353268,-3.72363654868116));
#9946=CARTESIAN_POINT('Ctrl Pts',(90.0673965101889,0.0576029372165674,-3.72345651607179));
#9947=CARTESIAN_POINT('Ctrl Pts',(90.0680508799934,0.0691384552651014,-3.72322208374306));
#9948=CARTESIAN_POINT('Ctrl Pts',(90.0744342902308,0.181668011938435,-3.72093518462754));
#9949=CARTESIAN_POINT('Ctrl Pts',(90.0809422787749,0.294214737682507,-3.71346809242457));
#9950=CARTESIAN_POINT('Ctrl Pts',(90.0874852453869,0.406283979113922,-3.70087372346122));
#9951=CARTESIAN_POINT('Ctrl Pts',(90.0940208175582,0.518226567084839,-3.68829358784496));
#9952=CARTESIAN_POINT('Ctrl Pts',(90.1005909100288,0.62969285326157,-3.67059815377306));
#9953=CARTESIAN_POINT('Ctrl Pts',(90.1071233811401,0.740205377944357,-3.64787972663019));
#9954=CARTESIAN_POINT('Ctrl Pts',(90.1136494875706,0.850610228680375,-3.62518343437855));
#9955=CARTESIAN_POINT('Ctrl Pts',(90.1201378312342,0.960063280525032,-3.59747414462497));
#9956=CARTESIAN_POINT('Ctrl Pts',(90.1265380103702,1.0681023280649,-3.56487890111766));
#9957=CARTESIAN_POINT('Ctrl Pts',(90.1329346811574,1.17608215247311,-3.53230152515401));
#9958=CARTESIAN_POINT('Ctrl Pts',(90.1392431880217,1.28264957901568,-3.49484362828946));
#9959=CARTESIAN_POINT('Ctrl Pts',(90.1454370227585,1.38735577890121,-3.45266490700772));
#9960=CARTESIAN_POINT('Ctrl Pts',(90.1516288453074,1.49202796293576,-3.41049988830616));
#9961=CARTESIAN_POINT('Ctrl Pts',(90.1577060655008,1.59484012483382,-3.36361709399763));
#9962=CARTESIAN_POINT('Ctrl Pts',(90.1636667415201,1.69535609174828,-3.3122084954954));
#9963=CARTESIAN_POINT('Ctrl Pts',(90.1696268118186,1.79586184428049,-3.26080512110922));
#9964=CARTESIAN_POINT('Ctrl Pts',(90.1754704396039,1.89407179941306,-3.20487676734605));
#9965=CARTESIAN_POINT('Ctrl Pts',(90.1812196762402,1.98956268415211,-3.14464863508211));
#9966=CARTESIAN_POINT('Ctrl Pts',(90.1869720891323,2.08510632432536,-3.08438722884361));
#9967=CARTESIAN_POINT('Ctrl Pts',(90.1926301759772,2.17792774267623,-3.01982112287708));
#9968=CARTESIAN_POINT('Ctrl Pts',(90.1982382110071,2.26761734407342,-2.95121120649005));
#9969=CARTESIAN_POINT('Ctrl Pts',(90.2038477200996,2.35733052023075,-2.88258325610245));
#9970=CARTESIAN_POINT('Ctrl Pts',(90.2094074409087,2.44390998109456,-2.80990913967479));
#9971=CARTESIAN_POINT('Ctrl Pts',(90.2149804568369,2.52696313645904,-2.73348827855506));
#9972=CARTESIAN_POINT('Ctrl Pts',(90.2205596467886,2.610108301635,-2.65698275516099));
#9973=CARTESIAN_POINT('Ctrl Pts',(90.2261526023147,2.68971893078859,-2.57672191582007));
#9974=CARTESIAN_POINT('Ctrl Pts',(90.2318359798101,2.76542342787462,-2.49304835781216));
#9975=CARTESIAN_POINT('Ctrl Pts',(90.2364352263609,2.82668693665691,-2.42533592389905));
#9976=CARTESIAN_POINT('Ctrl Pts',(90.24109409516,2.88539266671139,-2.35538933141771));
#9977=CARTESIAN_POINT('Ctrl Pts',(90.2458560731707,2.94135779478508,-2.28341200968227));
#9978=CARTESIAN_POINT('Ctrl Pts',(90.2458574776968,2.94137430147326,-2.28339078026233));
#9979=CARTESIAN_POINT('Ctrl Pts',(90.2458588822319,2.94139080792326,-2.28336955066568));
#9980=CARTESIAN_POINT('Ctrl Pts',(90.245860286776,2.94140731413508,-2.28334832089232));
#9981=CARTESIAN_POINT('Ctrl Pts',(90.2517448434871,3.01056266485227,-2.19440287183321));
#9982=CARTESIAN_POINT('Ctrl Pts',(90.2577943942158,3.07566668485485,-2.10217505882779));
#9983=CARTESIAN_POINT('Ctrl Pts',(90.2639263439004,3.13644516681204,-2.00709297216542));
#9984=CARTESIAN_POINT('Ctrl Pts',(90.2700534151133,3.19717529447501,-1.91208653114349));
#9985=CARTESIAN_POINT('Ctrl Pts',(90.2762623875696,3.25358714427209,-1.81423050772147));
#9986=CARTESIAN_POINT('Ctrl Pts',(90.2824903460121,3.30544864642787,-1.71396457622133));
#9987=CARTESIAN_POINT('Ctrl Pts',(90.2887148681921,3.3572815341123,-1.61375396623144));
#9988=CARTESIAN_POINT('Ctrl Pts',(90.2949581587654,3.40456932356956,-1.51113613082438));
#9989=CARTESIAN_POINT('Ctrl Pts',(90.3011810498467,3.44711720445529,-1.40656138592201));
#9990=CARTESIAN_POINT('Ctrl Pts',(90.3074019107302,3.48965120423418,-1.30202075818778));
#9991=CARTESIAN_POINT('Ctrl Pts',(90.3136023159836,3.52744847020503,-1.19552446407259));
#9992=CARTESIAN_POINT('Ctrl Pts',(90.3197687339331,3.56034892071842,-1.08753386357061));
#9993=CARTESIAN_POINT('Ctrl Pts',(90.3259354487432,3.5932509551087,-0.979538064239594));
#9994=CARTESIAN_POINT('Ctrl Pts',(90.3320682076598,3.62125565042711,-0.870047759469028));
#9995=CARTESIAN_POINT('Ctrl Pts',(90.3381793344755,3.64423723377603,-0.759536554368533));
#9996=CARTESIAN_POINT('Ctrl Pts',(90.3406749151909,3.65362214722101,-0.714407457786194));
#9997=CARTESIAN_POINT('Ctrl Pts',(90.3431671843077,3.66216979237232,-0.669108258246237));
#9998=CARTESIAN_POINT('Ctrl Pts',(90.345658177608,3.66987330948582,-0.62367182598591));
#9999=CARTESIAN_POINT('Ctrl Pts',(90.3456586167391,3.66987466751999,-0.623663816108521));
#10000=CARTESIAN_POINT('Ctrl Pts',(90.3456590558701,3.66987602552788,-0.623655806227113));
#10001=CARTESIAN_POINT('Ctrl Pts',(90.3456594950011,3.66987738350949,-0.623647796341697));
#10002=CARTESIAN_POINT('Ctrl Pts',(90.3524840062436,3.69098170271146,-0.499166597645409));
#10003=CARTESIAN_POINT('Ctrl Pts',(90.3592950968009,3.70573899079509,-0.373714783119458));
#10004=CARTESIAN_POINT('Ctrl Pts',(90.3660689121749,3.71411672006159,-0.247903770232333));
#10005=CARTESIAN_POINT('Ctrl Pts',(90.3728585237779,3.7225139858113,-0.12179937179144));
#10006=CARTESIAN_POINT('Ctrl Pts',(90.3796106154978,3.72450199002899,0.00466615234247741));
#10007=CARTESIAN_POINT('Ctrl Pts',(90.3863244864897,3.72008560322385,0.130880164094778));
#10008=CARTESIAN_POINT('Ctrl Pts',(90.393041252459,3.71566731210153,0.257148598505923));
#10009=CARTESIAN_POINT('Ctrl Pts',(90.3997198692073,3.70483896923014,0.383165532035909));
#10010=CARTESIAN_POINT('Ctrl Pts',(90.4063826830949,3.68764344224471,0.5083169351252));
#10011=CARTESIAN_POINT('Ctrl Pts',(90.4130415494875,3.67045810303578,0.633394190180367));
#10012=CARTESIAN_POINT('Ctrl Pts',(90.419684914363,3.64691277564379,0.757607069371454));
#10013=CARTESIAN_POINT('Ctrl Pts',(90.4263552072003,3.61709182197542,0.880339277295861));
#10014=CARTESIAN_POINT('Ctrl Pts',(90.4318741295373,3.59241831343142,0.981886471745885));
#10015=CARTESIAN_POINT('Ctrl Pts',(90.4374119961341,3.56344927633743,1.082419944246));
#10016=CARTESIAN_POINT('Ctrl Pts',(90.4430005297901,3.53025723298489,1.18158852036477));
#10017=CARTESIAN_POINT('Ctrl Pts',(89.7566589985681,-3.72274994162807,0.00065924818494276));
#10018=CARTESIAN_POINT('Ctrl Pts',(89.754692356951,-3.72274344729714,0.0373324930346883));
#10019=CARTESIAN_POINT('Ctrl Pts',(89.7527097850186,-3.72219504574113,0.0740027969240078));
#10020=CARTESIAN_POINT('Ctrl Pts',(89.7481085869829,-3.71968528510386,0.158398523147372));
#10021=CARTESIAN_POINT('Ctrl Pts',(89.7454793224464,-3.71734703073846,0.206105536755127));
#10022=CARTESIAN_POINT('Ctrl Pts',(89.7275651638507,-3.69537905180333,0.527642985931046));
#10023=CARTESIAN_POINT('Ctrl Pts',(89.7114316014278,-3.64642915685228,0.798592725572422));
#10024=CARTESIAN_POINT('Ctrl Pts',(89.6889378155214,-3.53714918903783,1.16587590463302));
#10025=CARTESIAN_POINT('Ctrl Pts',(89.6825811181009,-3.50158739501498,1.26869164843413));
#10026=CARTESIAN_POINT('Ctrl Pts',(89.6723642039251,-3.43597870109353,1.43448835134085));
#10027=CARTESIAN_POINT('Ctrl Pts',(89.6684320771745,-3.40857351286186,1.49844390509589));
#10028=CARTESIAN_POINT('Ctrl Pts',(89.6628287522555,-3.36608403513711,1.59039370623631));
#10029=CARTESIAN_POINT('Ctrl Pts',(89.6610915574921,-3.35240934010757,1.6190199570756));
#10030=CARTESIAN_POINT('Ctrl Pts',(89.6579877322658,-3.32702422154747,1.67045942330549));
#10031=CARTESIAN_POINT('Ctrl Pts',(89.6566145446623,-3.31544171565319,1.69333137616355));
#10032=CARTESIAN_POINT('Ctrl Pts',(89.6533322295204,-3.28690625779162,1.74826481963309));
#10033=CARTESIAN_POINT('Ctrl Pts',(89.6514364501536,-3.26971971795486,1.78020105101389));
#10034=CARTESIAN_POINT('Ctrl Pts',(89.6443192861104,-3.20264969025658,1.90058213208958));
#10035=CARTESIAN_POINT('Ctrl Pts',(89.6392559566166,-3.14961899067667,1.9872293465319));
#10036=CARTESIAN_POINT('Ctrl Pts',(89.6224653878367,-2.95888814319197,2.27200911067671));
#10037=CARTESIAN_POINT('Ctrl Pts',(89.6111551859286,-2.80550814796508,2.45889715906491));
#10038=CARTESIAN_POINT('Ctrl Pts',(89.5990569744384,-2.63046736566053,2.63430302642997));
#10039=CARTESIAN_POINT('Ctrl Pts',(89.5987349289147,-2.62579979151321,2.63895555994337));
#10040=CARTESIAN_POINT('Ctrl Pts',(89.5984125828093,-2.62112000663417,2.64359555781933));
#10041=CARTESIAN_POINT('Origin',(81.4430005297901,0.,0.));
#10042=CARTESIAN_POINT('',(82.8483099710866,-4.43364346784955,0.00310368774765633));
#10043=CARTESIAN_POINT('',(82.4452259247167,1.97302819977468,3.97206321802814));
#10044=CARTESIAN_POINT('Ctrl Pts',(82.8483099710627,-4.43364346785048,0.00310368833033136));
#10045=CARTESIAN_POINT('Ctrl Pts',(82.8431982004951,-4.4338383207308,0.127632029051098));
#10046=CARTESIAN_POINT('Ctrl Pts',(82.8380437813906,-4.42875792909011,0.252000944091934));
#10047=CARTESIAN_POINT('Ctrl Pts',(82.8327597771156,-4.4184097134055,0.375824375914131));
#10048=CARTESIAN_POINT('Ctrl Pts',(82.8297019360816,-4.41242122495965,0.447480709082303));
#10049=CARTESIAN_POINT('Ctrl Pts',(82.8266006981391,-4.40466844329161,0.518955322921443));
#10050=CARTESIAN_POINT('Ctrl Pts',(82.8234392149119,-4.39515054133119,0.590181060107312));
#10051=CARTESIAN_POINT('Ctrl Pts',(82.8216860236884,-4.38987241679758,0.629679083141025));
#10052=CARTESIAN_POINT('Ctrl Pts',(82.8199141716151,-4.38405193541917,0.669099352470447));
#10053=CARTESIAN_POINT('Ctrl Pts',(82.8181206431555,-4.3776895649354,0.70842910067796));
#10054=CARTESIAN_POINT('Ctrl Pts',(82.8181187212864,-4.3776827472888,0.708471244769515));
#10055=CARTESIAN_POINT('Ctrl Pts',(82.8181167993924,-4.37767592901998,0.708513388757189));
#10056=CARTESIAN_POINT('Ctrl Pts',(82.8181148774735,-4.37766911012896,0.708555532640965));
#10057=CARTESIAN_POINT('Ctrl Pts',(82.8129148389423,-4.3592195821887,0.822582103675738));
#10058=CARTESIAN_POINT('Ctrl Pts',(82.8075272992602,-4.33618224457112,0.93601237641731));
#10059=CARTESIAN_POINT('Ctrl Pts',(82.8020295457792,-4.30864871846121,1.04846335123121));
#10060=CARTESIAN_POINT('Ctrl Pts',(82.8014868661422,-4.3059309021735,1.05956331313577));
#10061=CARTESIAN_POINT('Ctrl Pts',(82.8009431126332,-4.30316930831883,1.07065370525351));
#10062=CARTESIAN_POINT('Ctrl Pts',(82.8003983595855,-4.30036404582785,1.08173414129563));
#10063=CARTESIAN_POINT('Ctrl Pts',(82.7943421099015,-4.26917675803463,1.20492002811735));
#10064=CARTESIAN_POINT('Ctrl Pts',(82.7881628508326,-4.23258800048932,1.32687961667018));
#10065=CARTESIAN_POINT('Ctrl Pts',(82.7819515177903,-4.19076317124117,1.44713010522075));
#10066=CARTESIAN_POINT('Ctrl Pts',(82.775746103116,-4.14897819410393,1.5672660150416));
#10067=CARTESIAN_POINT('Ctrl Pts',(82.7695090211858,-4.10196745579517,1.68569623676777));
#10068=CARTESIAN_POINT('Ctrl Pts',(82.763313229815,-4.04993106810721,1.80196281954222));
#10069=CARTESIAN_POINT('Ctrl Pts',(82.7581865020976,-4.00687338990092,1.898167981539));
#10070=CARTESIAN_POINT('Ctrl Pts',(82.7530883257333,-3.96037342239628,1.99289395940686));
#10071=CARTESIAN_POINT('Ctrl Pts',(82.7481264079222,-3.91044593450664,2.0858223196227));
#10072=CARTESIAN_POINT('Ctrl Pts',(82.7467858018045,-3.89695657449428,2.11092961340606));
#10073=CARTESIAN_POINT('Ctrl Pts',(82.7454551421122,-3.88321715603325,2.13590542803796));
#10074=CARTESIAN_POINT('Ctrl Pts',(82.7441365530662,-3.86922830218736,2.16074292003209));
#10075=CARTESIAN_POINT('Ctrl Pts',(82.7393269478812,-3.81820340994339,2.25133864478362));
#10076=CARTESIAN_POINT('Ctrl Pts',(82.7346478456743,-3.76390741767749,2.34011631238078));
#10077=CARTESIAN_POINT('Ctrl Pts',(82.7299933208539,-3.70666292796658,2.42695743283104));
#10078=CARTESIAN_POINT('Ctrl Pts',(82.7289460935899,-3.69378341982112,2.44649592332766));
#10079=CARTESIAN_POINT('Ctrl Pts',(82.7279001104591,-3.68075453556109,2.46593655474058));
#10080=CARTESIAN_POINT('Ctrl Pts',(82.7268541650439,-3.66757973118956,2.4852782682022));
#10081=CARTESIAN_POINT('Ctrl Pts',(82.7211602299211,-3.595858511079,2.59057101102986));
#10082=CARTESIAN_POINT('Ctrl Pts',(82.7154673659965,-3.51981327232184,2.69293423205903));
#10083=CARTESIAN_POINT('Ctrl Pts',(82.7097732753536,-3.43970668251573,2.79202036852321));
#10084=CARTESIAN_POINT('Ctrl Pts',(82.7045389955647,-3.3660688832119,2.88310507264559));
#10085=CARTESIAN_POINT('Ctrl Pts',(82.6993036398664,-3.28899541526,2.9714242342106));
#10086=CARTESIAN_POINT('Ctrl Pts',(82.6941566462714,-3.20857965293882,3.05657768639395));
#10087=CARTESIAN_POINT('Ctrl Pts',(82.6937040853997,-3.20150891799011,3.06406499327231));
#10088=CARTESIAN_POINT('Ctrl Pts',(82.6932522076729,-3.1944123615882,3.07152779766707));
#10089=CARTESIAN_POINT('Ctrl Pts',(82.6928010738893,-3.18729005828529,3.07896581173227));
#10090=CARTESIAN_POINT('Ctrl Pts',(82.6885158565976,-3.11963691772868,3.14961781707563));
#10091=CARTESIAN_POINT('Ctrl Pts',(82.6844125514995,-3.04952028554853,3.2178922091441));
#10092=CARTESIAN_POINT('Ctrl Pts',(82.6803745937489,-2.9772327649036,3.28372831794796));
#10093=CARTESIAN_POINT('Ctrl Pts',(82.6791511744965,-2.95533111314611,3.30367532284211));
#10094=CARTESIAN_POINT('Ctrl Pts',(82.6779337539151,-2.9332299348907,3.3233987677457));
#10095=CARTESIAN_POINT('Ctrl Pts',(82.6767190900405,-2.9109367004746,3.34289763278784));
#10096=CARTESIAN_POINT('Ctrl Pts',(82.6714898824389,-2.8149628649872,3.42684152494881));
#10097=CARTESIAN_POINT('Ctrl Pts',(82.6663115200674,-2.71543044857947,3.50662209046862));
#10098=CARTESIAN_POINT('Ctrl Pts',(82.6611172833366,-2.61272339386486,3.58191009741878));
#10099=CARTESIAN_POINT('Ctrl Pts',(82.6559198850698,-2.50995382523878,3.65724392933993));
#10100=CARTESIAN_POINT('Ctrl Pts',(82.6507062078556,-2.40400557751432,3.72807934776612));
#10101=CARTESIAN_POINT('Ctrl Pts',(82.6453940202299,-2.29529843068837,3.7941160661364));
#10102=CARTESIAN_POINT('Ctrl Pts',(82.6405334395281,-2.19583284376807,3.85453878113515));
#10103=CARTESIAN_POINT('Ctrl Pts',(82.6355899255016,-2.09405699856372,3.91094430538531));
#10104=CARTESIAN_POINT('Ctrl Pts',(82.6304940642063,-1.99032227923783,3.96312847935643));
#10105=CARTESIAN_POINT('Ctrl Pts',(82.6300128876823,-1.98052713200542,3.96805596815257));
#10106=CARTESIAN_POINT('Ctrl Pts',(82.6295303528188,-1.97071450152822,3.97294585314192));
#10107=CARTESIAN_POINT('Ctrl Pts',(82.6290464011762,-1.9608846720785,3.97779798356357));
#10108=CARTESIAN_POINT('Ctrl Pts',(82.6270433239479,-1.92019897996788,3.99788096520893));
#10109=CARTESIAN_POINT('Ctrl Pts',(82.625015938978,-1.87921937340591,4.01731684720352));
#10110=CARTESIAN_POINT('Ctrl Pts',(82.6229600729164,-1.83796794857875,4.03609494548256));
#10111=CARTESIAN_POINT('Ctrl Pts',(82.6229578270958,-1.83792288567218,4.03611545860888));
#10112=CARTESIAN_POINT('Ctrl Pts',(82.6229555812412,-1.83787782244118,4.03613597095037));
#10113=CARTESIAN_POINT('Ctrl Pts',(82.6229533353526,-1.8378327588858,4.03615648250706));
#10114=CARTESIAN_POINT('Ctrl Pts',(82.6178327674325,-1.73508901790095,4.08292230135918));
#10115=CARTESIAN_POINT('Ctrl Pts',(82.6125243072668,-1.63034728655921,4.12573969567118));
#10116=CARTESIAN_POINT('Ctrl Pts',(82.6071032863895,-1.5239600949963,4.16447005790881));
#10117=CARTESIAN_POINT('Ctrl Pts',(82.6065744137859,-1.51358100362888,4.16824857637942));
#10118=CARTESIAN_POINT('Ctrl Pts',(82.6060444698436,-1.50318629019696,4.17198820670683));
#10119=CARTESIAN_POINT('Ctrl Pts',(82.6055135245124,-1.4927763072773,4.17568882823057));
#10120=CARTESIAN_POINT('Ctrl Pts',(82.5995477274928,-1.37580787112226,4.21726967574725));
#10121=CARTESIAN_POINT('Ctrl Pts',(82.5934560145702,-1.25690592807626,4.25392421717051));
#10122=CARTESIAN_POINT('Ctrl Pts',(82.5873277913627,-1.1365420839014,4.28551969062002));
#10123=CARTESIAN_POINT('Ctrl Pts',(82.5812054988219,-1.0162947233816,4.31708458714458));
#10124=CARTESIAN_POINT('Ctrl Pts',(82.5750471072853,-0.89458839386563,4.34360053668037));
#10125=CARTESIAN_POINT('Ctrl Pts',(82.5689255999665,-0.77189485234871,4.36497801511059));
#10126=CARTESIAN_POINT('Ctrl Pts',(82.5644289908867,-0.681769191447175,
4.38068103703099));
#10127=CARTESIAN_POINT('Ctrl Pts',(82.5599523947277,-0.591107837079897,
4.39361192698146));
#10128=CARTESIAN_POINT('Ctrl Pts',(82.5556188258972,-0.500087401159369,
4.40357392969721));
#10129=CARTESIAN_POINT('Ctrl Pts',(82.5540567867667,-0.467278995859554,
4.40716474333583));
#10130=CARTESIAN_POINT('Ctrl Pts',(82.5525133304488,-0.434424426428198,
4.41036978328745));
#10131=CARTESIAN_POINT('Ctrl Pts',(82.5509942179002,-0.401533624456914,
4.41317976781749));
#10132=CARTESIAN_POINT('Ctrl Pts',(82.5460952165885,-0.295463746915021,
4.42224171514418));
#10133=CARTESIAN_POINT('Ctrl Pts',(82.5413174954551,-0.189042120070781,
4.42742225121933));
#10134=CARTESIAN_POINT('Ctrl Pts',(82.536558687016,-0.0825715696876148,
4.42892500778567));
#10135=CARTESIAN_POINT('Ctrl Pts',(82.5357498825313,-0.0644758930611303,
4.4291804154714));
#10136=CARTESIAN_POINT('Ctrl Pts',(82.5349416243627,-0.0463786813114588,
4.42932958564746));
#10137=CARTESIAN_POINT('Ctrl Pts',(82.5341334099387,-0.0282812715984249,
4.42937351348461));
#10138=CARTESIAN_POINT('Ctrl Pts',(82.5262973875791,0.14718170324818,4.42979941471063));
#10139=CARTESIAN_POINT('Ctrl Pts',(82.5184653978724,0.322665269126018,4.42033670888078));
#10140=CARTESIAN_POINT('Ctrl Pts',(82.5106321803695,0.497009262517875,4.40107786738388));
#10141=CARTESIAN_POINT('Ctrl Pts',(82.5073424783614,0.570228190110464,4.39298976699313));
#10142=CARTESIAN_POINT('Ctrl Pts',(82.5040525680356,0.643245945700422,4.38317325741542));
#10143=CARTESIAN_POINT('Ctrl Pts',(82.5007620893839,0.715975650346953,4.37163257845778));
#10144=CARTESIAN_POINT('Ctrl Pts',(82.4967352603142,0.80498096534671,4.35750930144286));
#10145=CARTESIAN_POINT('Ctrl Pts',(82.4927075574528,0.893559613112715,4.34080280069945));
#10146=CARTESIAN_POINT('Ctrl Pts',(82.4888009173514,0.981485590988129,4.32131589256869));
#10147=CARTESIAN_POINT('Ctrl Pts',(82.4873052817133,1.01514756716311,4.31385543715981));
#10148=CARTESIAN_POINT('Ctrl Pts',(82.4858273902324,1.04871334781174,4.30598756179976));
#10149=CARTESIAN_POINT('Ctrl Pts',(82.4843740851927,1.08216828460725,4.29770167811292));
#10150=CARTESIAN_POINT('Ctrl Pts',(82.480001238261,1.18283078402603,4.2727702975245));
#10151=CARTESIAN_POINT('Ctrl Pts',(82.4757657178508,1.28252133410666,4.24419825053364));
#10152=CARTESIAN_POINT('Ctrl Pts',(82.4715597827366,1.38098904233782,4.21219023683576));
#10153=CARTESIAN_POINT('Ctrl Pts',(82.47071405811,1.40078881658986,4.20575410201695));
#10154=CARTESIAN_POINT('Ctrl Pts',(82.4698695296969,1.42053931409565,4.1991790123273));
#10155=CARTESIAN_POINT('Ctrl Pts',(82.4690253215438,1.44023874403481,4.19246657992103));
#10156=CARTESIAN_POINT('Ctrl Pts',(82.4639755178385,1.5580749126782,4.15231479281467));
#10157=CARTESIAN_POINT('Ctrl Pts',(82.4589368589213,1.67408104493834,4.10724876386509));
#10158=CARTESIAN_POINT('Ctrl Pts',(82.4538338262441,1.7878010490968,4.05744660917939));
#10159=CARTESIAN_POINT('Ctrl Pts',(82.4510432927973,1.84998749689243,4.03021288618236));
#10160=CARTESIAN_POINT('Ctrl Pts',(82.4482332511581,1.91149046456204,4.00156368429464));
#10161=CARTESIAN_POINT('Ctrl Pts',(82.4453899175418,1.97223673451587,3.97153404972695));
#10162=CARTESIAN_POINT('',(82.4430005297901,-1.97158113240048,3.97043534620102));
#10163=CARTESIAN_POINT('Origin',(82.4430005297901,0.,0.));
#10164=CARTESIAN_POINT('',(82.6635449442269,-4.43315179037873,0.0011479234960335));
#10165=CARTESIAN_POINT('Ctrl Pts',(82.4430005297901,-1.97158113240048,3.97043534620102));
#10166=CARTESIAN_POINT('Ctrl Pts',(82.4459140470573,-2.02972790039701,3.94156166845641));
#10167=CARTESIAN_POINT('Ctrl Pts',(82.4488510668016,-2.08723260366219,3.91141452221414));
#10168=CARTESIAN_POINT('Ctrl Pts',(82.4577025121475,-2.2575544382045,3.8172965693948));
#10169=CARTESIAN_POINT('Ctrl Pts',(82.4636592841556,-2.36824732103486,3.74962785239478));
#10170=CARTESIAN_POINT('Ctrl Pts',(82.4782616257372,-2.63154904369224,3.57235033341775));
#10171=CARTESIAN_POINT('Ctrl Pts',(82.4868979764478,-2.78046866885149,3.45770631344884));
#10172=CARTESIAN_POINT('Ctrl Pts',(82.5030578932604,-3.0472355141486,3.22392913955234));
#10173=CARTESIAN_POINT('Ctrl Pts',(82.5105870370778,-3.16648552289963,3.10688511384025));
#10174=CARTESIAN_POINT('Ctrl Pts',(82.5301318685963,-3.46110369168554,2.78308949972469));
#10175=CARTESIAN_POINT('Ctrl Pts',(82.5420223880646,-3.62462358748545,2.56650253995901));
#10176=CARTESIAN_POINT('Ctrl Pts',(82.5650048709782,-3.90251929498455,2.11839683055745));
#10177=CARTESIAN_POINT('Ctrl Pts',(82.5759565558287,-4.01851747108689,1.88912280783753));
#10178=CARTESIAN_POINT('Ctrl Pts',(82.5973131753662,-4.20610848430369,1.42170340030805));
#10179=CARTESIAN_POINT('Ctrl Pts',(82.6076937618501,-4.2788215920027,1.18501630825411));
#10180=CARTESIAN_POINT('Ctrl Pts',(82.6208977765467,-4.34285070554643,0.891076505103667));
#10181=CARTESIAN_POINT('Ctrl Pts',(82.623275823123,-4.35332048581509,0.838433112605661));
#10182=CARTESIAN_POINT('Ctrl Pts',(82.6275113760015,-4.37004809604923,0.745537923488229));
#10183=CARTESIAN_POINT('Ctrl Pts',(82.6293558561636,-4.37671187288937,0.705365293883261));
#10184=CARTESIAN_POINT('Ctrl Pts',(82.6328942474834,-4.3883004437183,0.629000742213165));
#10185=CARTESIAN_POINT('Ctrl Pts',(82.6345839545017,-4.39333327460925,0.592828279565368));
#10186=CARTESIAN_POINT('Ctrl Pts',(82.6392248750366,-4.40578396093067,0.494450154625385));
#10187=CARTESIAN_POINT('Ctrl Pts',(82.6422126649266,-4.41233088898492,0.432144434949856));
#10188=CARTESIAN_POINT('Ctrl Pts',(82.6511917295901,-4.42781583262629,0.247126109229468));
#10189=CARTESIAN_POINT('Ctrl Pts',(82.6572970613572,-4.43296811398252,0.124159609381366));
#10190=CARTESIAN_POINT('Ctrl Pts',(82.6634574424051,-4.43299985245739,0.00114372756053367));
#10191=CARTESIAN_POINT('',(83.915600810406,-4.42944218562652,-0.000347422039578779));
#10192=CARTESIAN_POINT('Ctrl Pts',(82.6635449442269,-4.43315179037873,0.00114792349603368));
#10193=CARTESIAN_POINT('Ctrl Pts',(82.6697535422384,-4.43290168749669,-0.126097675849478));
#10194=CARTESIAN_POINT('Ctrl Pts',(82.6760083411183,-4.42714199085535,-0.253438677504856));
#10195=CARTESIAN_POINT('Ctrl Pts',(82.6822350885931,-4.4159129991645,-0.380374531670116));
#10196=CARTESIAN_POINT('Ctrl Pts',(82.6862669568839,-4.40864213813809,-0.462566502268552));
#10197=CARTESIAN_POINT('Ctrl Pts',(82.6900873253285,-4.39873439968036,-0.544553531573465));
#10198=CARTESIAN_POINT('Ctrl Pts',(82.6938299895795,-4.38647203791183,-0.626197505433351));
#10199=CARTESIAN_POINT('Ctrl Pts',(82.6958632937083,-4.37981017643023,-0.670552814380214));
#10200=CARTESIAN_POINT('Ctrl Pts',(82.697873663436,-4.37245333657578,-0.71480777713799));
#10201=CARTESIAN_POINT('Ctrl Pts',(82.699882552671,-4.36444623982428,-0.758946675668096));
#10202=CARTESIAN_POINT('Ctrl Pts',(82.7072473607457,-4.3350913456947,-0.920764714535287));
#10203=CARTESIAN_POINT('Ctrl Pts',(82.7146085283909,-4.29702613331697,-1.08103278384968));
#10204=CARTESIAN_POINT('Ctrl Pts',(82.7219689832407,-4.25060656947618,-1.2388514253652));
#10205=CARTESIAN_POINT('Ctrl Pts',(82.7298622375662,-4.20082684382732,-1.40809404694312));
#10206=CARTESIAN_POINT('Ctrl Pts',(82.7377548970905,-4.14143940568037,-1.57452592045708));
#10207=CARTESIAN_POINT('Ctrl Pts',(82.7456521057249,-4.07283034190275,-1.7370584266606));
#10208=CARTESIAN_POINT('Ctrl Pts',(82.7475014553387,-4.0567636338451,-1.77511990401166));
#10209=CARTESIAN_POINT('Ctrl Pts',(82.7493510529934,-4.04019102741035,-1.81296741700496));
#10210=CARTESIAN_POINT('Ctrl Pts',(82.7512009627978,-4.0231171363229,-1.85058674534914));
#10211=CARTESIAN_POINT('Ctrl Pts',(82.7569077384329,-3.97044599234479,-1.96663838521422));
#10212=CARTESIAN_POINT('Ctrl Pts',(82.7626175306464,-3.91300409043966,-2.08052044276572));
#10213=CARTESIAN_POINT('Ctrl Pts',(82.7683204612542,-3.85091206751601,-2.19178529820373));
#10214=CARTESIAN_POINT('Ctrl Pts',(82.7719807173375,-3.81106015272649,-2.26319733036503));
#10215=CARTESIAN_POINT('Ctrl Pts',(82.7754195184539,-3.76896543646566,-2.33334009894391));
#10216=CARTESIAN_POINT('Ctrl Pts',(82.7787739803614,-3.72489414217142,-2.40217518693356));
#10217=CARTESIAN_POINT('Ctrl Pts',(82.7806520316568,-3.70022009499944,-2.4407136559153));
#10218=CARTESIAN_POINT('Ctrl Pts',(82.7825036467726,-3.67492610882491,-2.47884309045198));
#10219=CARTESIAN_POINT('Ctrl Pts',(82.7843528882297,-3.64905554361889,-2.51656304323995));
#10220=CARTESIAN_POINT('Ctrl Pts',(82.7895081501627,-3.57693432900977,-2.62171763837164));
#10221=CARTESIAN_POINT('Ctrl Pts',(82.7946452802066,-3.50033122955016,-2.7236900114497));
#10222=CARTESIAN_POINT('Ctrl Pts',(82.7998383961552,-3.41954196534363,-2.82206378685053));
#10223=CARTESIAN_POINT('Ctrl Pts',(82.804746494571,-3.34318671666422,-2.91503844329819));
#10224=CARTESIAN_POINT('Ctrl Pts',(82.8097050153416,-3.2630918453971,-3.00479882243312));
#10225=CARTESIAN_POINT('Ctrl Pts',(82.8147857671755,-3.17954463462073,-3.09101035441384));
#10226=CARTESIAN_POINT('Ctrl Pts',(82.8150898768471,-3.17454389542689,-3.09617056721964));
#10227=CARTESIAN_POINT('Ctrl Pts',(82.8153944244299,-3.16953078459027,-3.10131808095286));
#10228=CARTESIAN_POINT('Ctrl Pts',(82.8156994253226,-3.16450536241097,-3.10645282965993));
#10229=CARTESIAN_POINT('Ctrl Pts',(82.8207194321271,-3.08179198636384,-3.19096560999218));
#10230=CARTESIAN_POINT('Ctrl Pts',(82.825862755279,-2.99574477245991,-3.27201555267624));
#10231=CARTESIAN_POINT('Ctrl Pts',(82.8312003612335,-2.90667527770515,-3.34930710644914));
#10232=CARTESIAN_POINT('Ctrl Pts',(82.8312023843414,-2.90664151777541,-3.3493364021966));
#10233=CARTESIAN_POINT('Ctrl Pts',(82.8312044074773,-2.90660775741141,-3.34936569740487));
#10234=CARTESIAN_POINT('Ctrl Pts',(82.831206430641,-2.90657399661315,-3.34939499207396));
#10235=CARTESIAN_POINT('Ctrl Pts',(82.8363572762157,-2.82062116310868,-3.42397734631702));
#10236=CARTESIAN_POINT('Ctrl Pts',(82.841700361716,-2.73158702110858,-3.49528321595245));
#10237=CARTESIAN_POINT('Ctrl Pts',(82.8471575515268,-2.63977466411272,-3.56307841028072));
#10238=CARTESIAN_POINT('Ctrl Pts',(82.8477049420542,-2.63056530613615,-3.56987869549384));
#10239=CARTESIAN_POINT('Ctrl Pts',(82.8482534806254,-2.62132803877145,-3.57664365679372));
#10240=CARTESIAN_POINT('Ctrl Pts',(82.8488030883847,-2.61206319676825,-3.58337305721038));
#10241=CARTESIAN_POINT('Ctrl Pts',(82.8548238049242,-2.51057083873772,-3.65709074351118));
#10242=CARTESIAN_POINT('Ctrl Pts',(82.8609723051984,-2.40576350692455,-3.72654164247399));
#10243=CARTESIAN_POINT('Ctrl Pts',(82.8671559578527,-2.29806345963243,-3.79146048281249));
#10244=CARTESIAN_POINT('Ctrl Pts',(82.8733328329235,-2.19048145681947,-3.85630816895108));
#10245=CARTESIAN_POINT('Ctrl Pts',(82.879544443025,-2.08001323879596,-3.91663404207498));
#10246=CARTESIAN_POINT('Ctrl Pts',(82.8857158943829,-1.96709267257739,-3.972213696294));
#10247=CARTESIAN_POINT('Ctrl Pts',(82.8900077147347,-1.88856417804148,-4.01086552668066));
#10248=CARTESIAN_POINT('Ctrl Pts',(82.8942800162594,-1.80884676597104,-4.04722325500299));
#10249=CARTESIAN_POINT('Ctrl Pts',(82.8984045010245,-1.72802482212208,-4.08104405161748));
#10250=CARTESIAN_POINT('Ctrl Pts',(82.9002058966658,-1.69272531062903,-4.09581550528394));
#10251=CARTESIAN_POINT('Ctrl Pts',(82.9019790953342,-1.65721572201682,-4.11010276553236));
#10252=CARTESIAN_POINT('Ctrl Pts',(82.9037134080104,-1.62150602886537,-4.12388455513962));
#10253=CARTESIAN_POINT('Ctrl Pts',(82.9094157471257,-1.50409422483852,-4.1691984359855));
#10254=CARTESIAN_POINT('Ctrl Pts',(82.9150416488362,-1.38474146504016,-4.20960104440071));
#10255=CARTESIAN_POINT('Ctrl Pts',(82.9206660839083,-1.26393293989382,-4.24512429519591));
#10256=CARTESIAN_POINT('Ctrl Pts',(82.9281829542762,-1.10247636492875,-4.29259993814471));
#10257=CARTESIAN_POINT('Ctrl Pts',(82.9356972835923,-0.938412063536249,
-4.33136558777071));
#10258=CARTESIAN_POINT('Ctrl Pts',(82.9432144689425,-0.772724773604452,
-4.36119264732472));
#10259=CARTESIAN_POINT('Ctrl Pts',(82.9469438926373,-0.690524046043502,
-4.37599043898003));
#10260=CARTESIAN_POINT('Ctrl Pts',(82.9506740056613,-0.607923936337747,
-4.38858727479971));
#10261=CARTESIAN_POINT('Ctrl Pts',(82.9544054051174,-0.525045504401398,
-4.39895043695672));
#10262=CARTESIAN_POINT('Ctrl Pts',(82.9581359118733,-0.442186900304788,
-4.40931111983035));
#10263=CARTESIAN_POINT('Ctrl Pts',(82.9618677244815,-0.359045347278706,
-4.41743945724858));
#10264=CARTESIAN_POINT('Ctrl Pts',(82.965469567743,-0.27574647201453,-4.42307138832066));
#10265=CARTESIAN_POINT('Ctrl Pts',(82.9673012120467,-0.233386519262133,
-4.42593539258676));
#10266=CARTESIAN_POINT('Ctrl Pts',(82.9690992459571,-0.19098671178188,-4.42815373228215));
#10267=CARTESIAN_POINT('Ctrl Pts',(82.9708464058618,-0.14856873889832,-4.4296914588579));
#10268=CARTESIAN_POINT('Ctrl Pts',(82.9760346635733,-0.0226069569703721,
-4.4342577963425));
#10269=CARTESIAN_POINT('Ctrl Pts',(82.9811221551682,0.103488754728788,-4.43342346283101));
#10270=CARTESIAN_POINT('Ctrl Pts',(82.9862060321369,0.229218662760157,-4.42723651800783));
#10271=CARTESIAN_POINT('Ctrl Pts',(82.9912928436474,0.355021145260182,-4.42104600192432));
#10272=CARTESIAN_POINT('Ctrl Pts',(82.9963763800366,0.480458980621974,-4.4094964009439));
#10273=CARTESIAN_POINT('Ctrl Pts',(83.0015360391351,0.605031145700445,-4.39262062142151));
#10274=CARTESIAN_POINT('Ctrl Pts',(83.0063406759549,0.721031834823586,-4.37690601894306));
#10275=CARTESIAN_POINT('Ctrl Pts',(83.0112117514418,0.836282318339334,-4.35657281110158));
#10276=CARTESIAN_POINT('Ctrl Pts',(83.0162215122836,0.950372167218369,-4.33168733254973));
#10277=CARTESIAN_POINT('Ctrl Pts',(83.0165996648668,0.958984029627877,-4.32980889797041));
#10278=CARTESIAN_POINT('Ctrl Pts',(83.0169786076386,0.967589302089159,-4.32790453468976));
#10279=CARTESIAN_POINT('Ctrl Pts',(83.017358371671,0.976187819452551,-4.3259742753369));
#10280=CARTESIAN_POINT('Ctrl Pts',(83.020341280886,1.04372606555874,-4.31081278577855));
#10281=CARTESIAN_POINT('Ctrl Pts',(83.0233749977415,1.11084583174612,-4.29405393857436));
#10282=CARTESIAN_POINT('Ctrl Pts',(83.0264749356101,1.17746184370479,-4.27571908021852));
#10283=CARTESIAN_POINT('Ctrl Pts',(83.0264771251977,1.1775088967755,-4.27570612970766));
#10284=CARTESIAN_POINT('Ctrl Pts',(83.0264793148184,1.17755594959518,-4.27569317841065));
#10285=CARTESIAN_POINT('Ctrl Pts',(83.0264815044721,1.17760300216381,-4.27568022632754));
#10286=CARTESIAN_POINT('Ctrl Pts',(83.031631555246,1.28827032652172,-4.24521701412813));
#10287=CARTESIAN_POINT('Ctrl Pts',(83.0369750667503,1.39786167467843,-4.21030931034651));
#10288=CARTESIAN_POINT('Ctrl Pts',(83.0424357424794,1.50601219890857,-4.17108757267222));
#10289=CARTESIAN_POINT('Ctrl Pts',(83.0430131410074,1.51744777146085,-4.16694036182888));
#10290=CARTESIAN_POINT('Ctrl Pts',(83.0435918494819,1.52886720783642,-4.16274495782363));
#10291=CARTESIAN_POINT('Ctrl Pts',(83.0441717777059,1.54027005805773,-4.15850154327633));
#10292=CARTESIAN_POINT('Ctrl Pts',(83.0502290459922,1.65937121602083,-4.11417967843622));
#10293=CARTESIAN_POINT('Ctrl Pts',(83.0564188321494,1.77666664557797,-4.06461532858667));
#10294=CARTESIAN_POINT('Ctrl Pts',(83.0626487687321,1.89169347240627,-4.01002655004524));
#10295=CARTESIAN_POINT('Ctrl Pts',(83.068872772623,2.00661076060745,-3.9554897557237));
#10296=CARTESIAN_POINT('Ctrl Pts',(83.0751364884606,2.11926396248689,-3.89593843265172));
#10297=CARTESIAN_POINT('Ctrl Pts',(83.0813650127668,2.22921934865866,-3.83162264812522));
#10298=CARTESIAN_POINT('Ctrl Pts',(83.0873458487568,2.33480216387975,-3.76986449484245));
#10299=CARTESIAN_POINT('Ctrl Pts',(83.0932938490061,2.43789893180415,-3.70371211631604));
#10300=CARTESIAN_POINT('Ctrl Pts',(83.0991143652774,2.5380963922071,-3.63334847875165));
#10301=CARTESIAN_POINT('Ctrl Pts',(83.0996646519468,2.54756931938391,-3.6266961183838));
#10302=CARTESIAN_POINT('Ctrl Pts',(83.1002137991261,2.55701630012658,-3.62000613859655));
#10303=CARTESIAN_POINT('Ctrl Pts',(83.1007617268327,2.56643696581559,-3.61327870839512));
#10304=CARTESIAN_POINT('Ctrl Pts',(83.1050766073558,2.64062384559076,-3.56030081150069));
#10305=CARTESIAN_POINT('Ctrl Pts',(83.1092212503589,2.7130810149356,-3.50486908319631));
#10306=CARTESIAN_POINT('Ctrl Pts',(83.1133169435521,2.78379252150318,-3.4472891530527));
#10307=CARTESIAN_POINT('Ctrl Pts',(83.1149440208849,2.81188375882832,-3.42441463713097));
#10308=CARTESIAN_POINT('Ctrl Pts',(83.1165633729672,2.83969995819367,-3.40120074459727));
#10309=CARTESIAN_POINT('Ctrl Pts',(83.1181826040973,2.86724187719823,-3.37766518050719));
#10310=CARTESIAN_POINT('Ctrl Pts',(83.1238769429428,2.96409835207831,-3.29489782607189));
#10311=CARTESIAN_POINT('Ctrl Pts',(83.1295698325491,3.05756544207097,-3.20815179462532));
#10312=CARTESIAN_POINT('Ctrl Pts',(83.1352635643397,3.14733049837667,-3.11773076315744));
#10313=CARTESIAN_POINT('Ctrl Pts',(83.1409577238474,3.23710229789627,-3.02730293919834));
#10314=CARTESIAN_POINT('Ctrl Pts',(83.1466527721168,3.32317236319105,-2.93319848395593));
#10315=CARTESIAN_POINT('Ctrl Pts',(83.15234916326,3.40520966066485,-2.83571279856705));
#10316=CARTESIAN_POINT('Ctrl Pts',(83.156465764087,3.46449540810214,-2.76526299219011));
#10317=CARTESIAN_POINT('Ctrl Pts',(83.1603823538859,3.52140497973347,-2.69282752856406));
#10318=CARTESIAN_POINT('Ctrl Pts',(83.1642220955801,3.57594577686112,-2.61868992215394));
#10319=CARTESIAN_POINT('Ctrl Pts',(83.1656972154139,3.59689880391248,-2.59020835689558));
#10320=CARTESIAN_POINT('Ctrl Pts',(83.1671609934016,3.61750259350637,-2.56147516766554));
#10321=CARTESIAN_POINT('Ctrl Pts',(83.1686204127657,3.63775885406154,-2.53250484177084));
#10322=CARTESIAN_POINT('Ctrl Pts',(83.1738842292335,3.71081889458932,-2.42801501364069));
#10323=CARTESIAN_POINT('Ctrl Pts',(83.1790915795336,3.77935744318782,-2.32044082006187));
#10324=CARTESIAN_POINT('Ctrl Pts',(83.1843073977264,3.84309018161013,-2.21019936344676));
#10325=CARTESIAN_POINT('Ctrl Pts',(83.1895263928587,3.90686173945572,-2.09989075908509));
#10326=CARTESIAN_POINT('Ctrl Pts',(83.1947542364531,3.96582124515078,-1.98691151111031));
#10327=CARTESIAN_POINT('Ctrl Pts',(83.2000719246885,4.01971677939873,-1.87171061619713));
#10328=CARTESIAN_POINT('Ctrl Pts',(83.2049704710994,4.06936425103758,-1.76558989130256));
#10329=CARTESIAN_POINT('Ctrl Pts',(83.209945708905,4.11471474761423,-1.65758342461459));
#10330=CARTESIAN_POINT('Ctrl Pts',(83.2150681294169,4.15560070766259,-1.54806904063664));
#10331=CARTESIAN_POINT('Ctrl Pts',(83.2155141276777,4.15916056125742,-1.53853385611296));
#10332=CARTESIAN_POINT('Ctrl Pts',(83.2159612417034,4.16268659683867,-1.52898722160007));
#10333=CARTESIAN_POINT('Ctrl Pts',(83.2164095180213,4.16617871895642,-1.51942937543462));
#10334=CARTESIAN_POINT('Ctrl Pts',(83.2184084439692,4.18175057327004,-1.4768096207348));
#10335=CARTESIAN_POINT('Ctrl Pts',(83.2204305259555,4.19664788204346,-1.43396768820987));
#10336=CARTESIAN_POINT('Ctrl Pts',(83.2224799502902,4.2108624193871,-1.39092663162212));
#10337=CARTESIAN_POINT('Ctrl Pts',(83.2224818919627,4.21087588657161,-1.39088585352034));
#10338=CARTESIAN_POINT('Ctrl Pts',(83.2224838336597,4.21088935314335,-1.39084507523976));
#10339=CARTESIAN_POINT('Ctrl Pts',(83.2224857753812,4.21090281910232,-1.39080429678043));
#10340=CARTESIAN_POINT('Ctrl Pts',(83.2276958762136,4.24703519050223,-1.28138598944583));
#10341=CARTESIAN_POINT('Ctrl Pts',(83.2330927463868,4.27884346901629,-1.17038633843429));
#10342=CARTESIAN_POINT('Ctrl Pts',(83.238599482485,4.30623236297333,-1.05818515621962));
#10343=CARTESIAN_POINT('Ctrl Pts',(83.2391478689658,4.30895987685862,-1.04701163884735));
#10344=CARTESIAN_POINT('Ctrl Pts',(83.2396973449987,4.31164357857737,-1.03582624554528));
#10345=CARTESIAN_POINT('Ctrl Pts',(83.2402478346343,4.31428338468635,-1.02462937754755));
#10346=CARTESIAN_POINT('Ctrl Pts',(83.2463188982337,4.34339643194308,-0.90114494964345));
#10347=CARTESIAN_POINT('Ctrl Pts',(83.2525127122266,4.367168791287,-0.776259208809224));
#10348=CARTESIAN_POINT('Ctrl Pts',(83.2587383288107,4.38552444664463,-0.650475198184107));
#10349=CARTESIAN_POINT('Ctrl Pts',(83.2649580273905,4.40386265331336,-0.524810756488961));
#10350=CARTESIAN_POINT('Ctrl Pts',(83.2712091204897,4.41679482015103,-0.398249774132754));
#10351=CARTESIAN_POINT('Ctrl Pts',(83.2774183828953,4.4242873067542,-0.271289330281206));
#10352=CARTESIAN_POINT('Ctrl Pts',(83.2818665938466,4.42965479789635,-0.180337007791962));
#10353=CARTESIAN_POINT('Ctrl Pts',(83.2862932319342,4.43223067893641,-0.0891765403184688));
#10354=CARTESIAN_POINT('Ctrl Pts',(83.2905748263073,4.43183580562401,0.00200120831765594));
#10355=CARTESIAN_POINT('Ctrl Pts',(83.2922657104634,4.43167986254079,0.0380090589267377));
#10356=CARTESIAN_POINT('Ctrl Pts',(83.2939339734225,4.43106060173415,0.0740190327286194));
#10357=CARTESIAN_POINT('Ctrl Pts',(83.2955720103559,4.42996711655931,0.110017136420428));
#10358=CARTESIAN_POINT('Ctrl Pts',(83.3013557983644,4.42610610078323,0.237123794527655));
#10359=CARTESIAN_POINT('Ctrl Pts',(83.3070431808581,4.41681895720635,0.364089474368331));
#10360=CARTESIAN_POINT('Ctrl Pts',(83.3127292137339,4.40235937168851,0.490468223047512));
#10361=CARTESIAN_POINT('Ctrl Pts',(83.3202757972191,4.38316840468998,0.658199890889831));
#10362=CARTESIAN_POINT('Ctrl Pts',(83.3278200867937,4.3548679440162,0.824908498874133));
#10363=CARTESIAN_POINT('Ctrl Pts',(83.3353674090675,4.31762806162275,0.989594993068796));
#10364=CARTESIAN_POINT('Ctrl Pts',(83.3391920019019,4.29875681402142,1.07304959627369));
#10365=CARTESIAN_POINT('Ctrl Pts',(83.3430173561456,4.27758922004229,1.15598442351761));
#10366=CARTESIAN_POINT('Ctrl Pts',(83.3468440873736,4.25414314863876,1.23826639036087));
#10367=CARTESIAN_POINT('Ctrl Pts',(83.3517492151144,4.22408982939495,1.34373592404053));
#10368=CARTESIAN_POINT('Ctrl Pts',(83.3565356218405,4.19008965765042,1.44807887305938));
#10369=CARTESIAN_POINT('Ctrl Pts',(83.3611065242648,4.15204113187027,1.55088410347697));
#10370=CARTESIAN_POINT('Ctrl Pts',(83.3618388982381,4.14594479740122,1.567356096989));
#10371=CARTESIAN_POINT('Ctrl Pts',(83.362565739757,4.13974457730305,1.58378851468944));
#10372=CARTESIAN_POINT('Ctrl Pts',(83.3632866507204,4.13344010795501,1.60017955307763));
#10373=CARTESIAN_POINT('Ctrl Pts',(83.3685125371654,4.08773898454253,1.71899825563343));
#10374=CARTESIAN_POINT('Ctrl Pts',(83.3736802157154,4.03696913488963,1.8357987771688));
#10375=CARTESIAN_POINT('Ctrl Pts',(83.3788545764085,3.98131696754136,1.95011384795414));
#10376=CARTESIAN_POINT('Ctrl Pts',(83.3840321159857,3.92563061011647,2.06449914854751));
#10377=CARTESIAN_POINT('Ctrl Pts',(83.3892167134998,3.86505561520871,2.17639569603508));
#10378=CARTESIAN_POINT('Ctrl Pts',(83.3944892480764,3.79982286445714,2.28534536985133));
#10379=CARTESIAN_POINT('Ctrl Pts',(83.3993493524282,3.73969277499033,2.38577274043547));
#10380=CARTESIAN_POINT('Ctrl Pts',(83.4042846234623,3.67560478451595,2.48369665225706));
#10381=CARTESIAN_POINT('Ctrl Pts',(83.4093655796607,3.60777834532099,2.57876776006166));
#10382=CARTESIAN_POINT('Ctrl Pts',(83.4098046666016,3.60191690851023,2.58698363129919));
#10383=CARTESIAN_POINT('Ctrl Pts',(83.4102448415338,3.5960275520837,2.59517822973848));
#10384=CARTESIAN_POINT('Ctrl Pts',(83.4106861499687,3.59011041702327,2.60335134822733));
#10385=CARTESIAN_POINT('Ctrl Pts',(83.4130537171506,3.55836569230572,2.64719915529321));
#10386=CARTESIAN_POINT('Ctrl Pts',(83.4154539753355,3.52582211620615,2.69042785635404));
#10387=CARTESIAN_POINT('Ctrl Pts',(83.4178940510447,3.49250453772734,2.73300404509958));
#10388=CARTESIAN_POINT('Ctrl Pts',(83.4178960990468,3.49247657364914,2.73303978010571));
#10389=CARTESIAN_POINT('Ctrl Pts',(83.4178981470768,3.49244860902571,2.73307551465235));
#10390=CARTESIAN_POINT('Ctrl Pts',(83.4179001951349,3.49242064385706,2.73311124873948));
#10391=CARTESIAN_POINT('Ctrl Pts',(83.4230804538993,3.42168690417833,2.82349531361935));
#10392=CARTESIAN_POINT('Ctrl Pts',(83.4284505832191,3.34726193598441,2.91118426735303));
#10393=CARTESIAN_POINT('Ctrl Pts',(83.4339335812588,3.26940588398292,2.9958897134484));
#10394=CARTESIAN_POINT('Ctrl Pts',(83.4344900909845,3.26150370166652,3.00448709105785));
#10395=CARTESIAN_POINT('Ctrl Pts',(83.4350477634512,3.25356621653918,3.01305372383549));
#10396=CARTESIAN_POINT('Ctrl Pts',(83.4356065181459,3.24559372995324,3.02158930431373));
#10397=CARTESIAN_POINT('Ctrl Pts',(83.4416628908757,3.15917951132197,3.1141069284753));
#10398=CARTESIAN_POINT('Ctrl Pts',(83.4478458747289,3.06864739174935,3.20297803546822));
#10399=CARTESIAN_POINT('Ctrl Pts',(83.4540637428815,2.97437175577744,3.28786046013636));
#10400=CARTESIAN_POINT('Ctrl Pts',(83.4602754787236,2.88018909821294,3.37265917035822));
#10401=CARTESIAN_POINT('Ctrl Pts',(83.4665216800954,2.78227053048892,3.45347735854507));
#10402=CARTESIAN_POINT('Ctrl Pts',(83.472728267662,2.68100906535056,3.53001146314587));
#10403=CARTESIAN_POINT('Ctrl Pts',(83.4774236798418,2.60440266744516,3.58791110011411));
#10404=CARTESIAN_POINT('Ctrl Pts',(83.4820963018083,2.52588060915895,3.64336056465543));
#10405=CARTESIAN_POINT('Ctrl Pts',(83.4866286167864,2.44553776480205,3.69610140141218));
#10406=CARTESIAN_POINT('Ctrl Pts',(83.4880828915604,2.41975831823126,3.71302424742482));
#10407=CARTESIAN_POINT('Ctrl Pts',(83.4895227208511,2.39379174784691,3.72966800614239));
#10408=CARTESIAN_POINT('Ctrl Pts',(83.4909442224484,2.36764216970578,3.74602356322536));
#10409=CARTESIAN_POINT('Ctrl Pts',(83.4958650556628,2.27711978626616,3.80264183835173));
#10410=CARTESIAN_POINT('Ctrl Pts',(83.500662889532,2.18449736086475,3.85594589781447));
#10411=CARTESIAN_POINT('Ctrl Pts',(83.505440332829,2.09013217084792,3.90597666055246));
#10412=CARTESIAN_POINT('Ctrl Pts',(83.5063418383544,2.07232542047616,3.9154174861665));
#10413=CARTESIAN_POINT('Ctrl Pts',(83.5072426178155,2.05445647939991,3.92474182120197));
#10414=CARTESIAN_POINT('Ctrl Pts',(83.5081433606626,2.03652755806437,3.93395002496193));
#10415=CARTESIAN_POINT('Ctrl Pts',(83.5156887938591,1.88633876816063,4.01108623154202));
#10416=CARTESIAN_POINT('Ctrl Pts',(83.5232317390843,1.73194090282254,4.08007809689432));
#10417=CARTESIAN_POINT('Ctrl Pts',(83.5307775529328,1.57426266678588,4.1405149697427));
#10418=CARTESIAN_POINT('Ctrl Pts',(83.5345789459057,1.49482830085911,4.17096156017889));
#10419=CARTESIAN_POINT('Ctrl Pts',(83.538381051415,1.41456137295648,4.19923609301629));
#10420=CARTESIAN_POINT('Ctrl Pts',(83.5421844836819,1.33358065191831,4.22528092553794));
#10421=CARTESIAN_POINT('Ctrl Pts',(83.5471073281589,1.22876598260772,4.25899117747211));
#10422=CARTESIAN_POINT('Ctrl Pts',(83.5519120286095,1.12268776988625,4.28876818841022));
#10423=CARTESIAN_POINT('Ctrl Pts',(83.556502202349,1.01563498595979,4.31429907462853));
#10424=CARTESIAN_POINT('Ctrl Pts',(83.5572066933098,0.999204732359207,4.31821750551682));
#10425=CARTESIAN_POINT('Ctrl Pts',(83.5579061309835,0.982751620683477,4.32203589941005));
#10426=CARTESIAN_POINT('Ctrl Pts',(83.5586001669221,0.966276803372248,4.32575310922017));
#10427=CARTESIAN_POINT('Ctrl Pts',(83.5638217887403,0.842327508043682,4.35371976450071));
#10428=CARTESIAN_POINT('Ctrl Pts',(83.5689828774853,0.717244017525123,4.37637234041289));
#10429=CARTESIAN_POINT('Ctrl Pts',(83.574147593184,0.591516394640054,4.39360678407597));
#10430=CARTESIAN_POINT('Ctrl Pts',(83.5793154218535,0.465712990929349,4.41085161559448));
#10431=CARTESIAN_POINT('Ctrl Pts',(83.5844872421536,0.339264707288376,4.42267138590536));
#10432=CARTESIAN_POINT('Ctrl Pts',(83.5897434241407,0.212678499269937,4.429003912549));
#10433=CARTESIAN_POINT('Ctrl Pts',(83.5946043131319,0.0956122510871442,
4.4348601993222));
#10434=CARTESIAN_POINT('Ctrl Pts',(83.5995377961836,-0.0215724676693285,
4.43602349133232));
#10435=CARTESIAN_POINT('Ctrl Pts',(83.6046149580464,-0.138461181276436,
4.43248217517797));
#10436=CARTESIAN_POINT('Ctrl Pts',(83.6050357345095,-0.148148487063251,
4.43218868394672));
#10437=CARTESIAN_POINT('Ctrl Pts',(83.6054574978282,-0.157833784798538,
4.43186289506993));
#10438=CARTESIAN_POINT('Ctrl Pts',(83.6058802884664,-0.1675168523186,4.43150481028875));
#10439=CARTESIAN_POINT('Ctrl Pts',(83.6083705427704,-0.224550519560011,
4.42939567615212));
#10440=CARTESIAN_POINT('Ctrl Pts',(83.6108965182637,-0.281505603001958,
4.42616618672832));
#10441=CARTESIAN_POINT('Ctrl Pts',(83.6134666278495,-0.338333304651339,
4.42181886367226));
#10442=CARTESIAN_POINT('Ctrl Pts',(83.6134686787691,-0.338378652541717,
4.42181539455555));
#10443=CARTESIAN_POINT('Ctrl Pts',(83.6134707297169,-0.338424000351126,
4.42181192472713));
#10444=CARTESIAN_POINT('Ctrl Pts',(83.6134727806927,-0.338469348079556,
4.42180845418703));
#10445=CARTESIAN_POINT('Ctrl Pts',(83.618654874038,-0.453047081791832,4.41303962202268));
#10446=CARTESIAN_POINT('Ctrl Pts',(83.6240267635337,-0.567422948792048,
4.39969405719048));
#10447=CARTESIAN_POINT('Ctrl Pts',(83.6295116449866,-0.681212096767725,
4.38182930509884));
#10448=CARTESIAN_POINT('Ctrl Pts',(83.6300706981457,-0.692810192950719,
4.3800084186898));
#10449=CARTESIAN_POINT('Ctrl Pts',(83.6306309251727,-0.704402161603934,
4.37814061365625));
#10450=CARTESIAN_POINT('Ctrl Pts',(83.6311922447393,-0.715987573789082,
4.37622597240999));
#10451=CARTESIAN_POINT('Ctrl Pts',(83.6372533034713,-0.841085410874153,
4.35555191482162));
#10452=CARTESIAN_POINT('Ctrl Pts',(83.6434412084401,-0.96542337207803,4.32941315273088));
#10453=CARTESIAN_POINT('Ctrl Pts',(83.649664316664,-1.08850789870529,4.29793296106795));
#10454=CARTESIAN_POINT('Ctrl Pts',(83.6558814031489,-1.21147332361096,4.26648323095146));
#10455=CARTESIAN_POINT('Ctrl Pts',(83.6621332726753,-1.33318786235633,4.22970275874476));
#10456=CARTESIAN_POINT('Ctrl Pts',(83.6683459091601,-1.45317992705797,4.18775171601595));
#10457=CARTESIAN_POINT('Ctrl Pts',(83.6731578198372,-1.54611810213333,4.15525912274806));
#10458=CARTESIAN_POINT('Ctrl Pts',(83.6779460695833,-1.63802567327674,4.11966361603014));
#10459=CARTESIAN_POINT('Ctrl Pts',(83.6825958502752,-1.72862303737288,4.08091454301838));
#10460=CARTESIAN_POINT('Ctrl Pts',(83.6839450610236,-1.75491136052506,4.06967085879707));
#10461=CARTESIAN_POINT('Ctrl Pts',(83.685282613146,-1.78108906197937,4.05816178987407));
#10462=CARTESIAN_POINT('Ctrl Pts',(83.6866057017605,-1.80714857123362,4.04638645852495));
#10463=CARTESIAN_POINT('Ctrl Pts',(83.6914041439244,-1.90165852817018,4.0036808938168));
#10464=CARTESIAN_POINT('Ctrl Pts',(83.6960718155216,-1.99465230072675,3.95756905734555));
#10465=CARTESIAN_POINT('Ctrl Pts',(83.7007146286701,-2.08598548365827,3.90836441317301));
#10466=CARTESIAN_POINT('Ctrl Pts',(83.7017617439562,-2.10658428204085,3.89726706046652));
#10467=CARTESIAN_POINT('Ctrl Pts',(83.7028075947953,-2.1270987954403,3.8860122855028));
#10468=CARTESIAN_POINT('Ctrl Pts',(83.7038533962134,-2.1475276796128,3.87460349311657));
#10469=CARTESIAN_POINT('Ctrl Pts',(83.7114039453886,-2.29502154591708,3.79223350733086));
#10470=CARTESIAN_POINT('Ctrl Pts',(83.7189520000807,-2.43805615563127,3.70183762496549));
#10471=CARTESIAN_POINT('Ctrl Pts',(83.7265029116128,-2.57577454065322,3.603962383649));
#10472=CARTESIAN_POINT('Ctrl Pts',(83.7303166368923,-2.64533171718342,3.55452871190574));
#10473=CARTESIAN_POINT('Ctrl Pts',(83.7341310752323,-2.71353203111865,3.50318657492858));
#10474=CARTESIAN_POINT('Ctrl Pts',(83.7379468442458,-2.78026072840528,3.45000355426256));
#10475=CARTESIAN_POINT('Ctrl Pts',(83.7436340194881,-2.87971585627676,3.37073744633586));
#10476=CARTESIAN_POINT('Ctrl Pts',(83.7491229268731,-2.97568597598866,3.28710709185555));
#10477=CARTESIAN_POINT('Ctrl Pts',(83.7543517004372,-3.06761895138763,3.19933279850464));
#10478=CARTESIAN_POINT('Ctrl Pts',(83.7595860249966,-3.15964952510658,3.11146532179344));
#10479=CARTESIAN_POINT('Ctrl Pts',(83.7647608101047,-3.24787155568025,3.01970019803276));
#10480=CARTESIAN_POINT('Ctrl Pts',(83.7699403890791,-3.33192600747476,2.92438887205071));
#10481=CARTESIAN_POINT('Ctrl Pts',(83.7751231036246,-3.41603134346466,2.829019847279));
#10482=CARTESIAN_POINT('Ctrl Pts',(83.7803109808668,-3.49596370603902,2.73010012777394));
#10483=CARTESIAN_POINT('Ctrl Pts',(83.7855845286649,-3.57138955912243,2.62801851725546));
#10484=CARTESIAN_POINT('Ctrl Pts',(83.7904563696584,-3.64106992935743,2.533712863102));
#10485=CARTESIAN_POINT('Ctrl Pts',(83.7954017729062,-3.70690444270405,2.43670821705469));
#10486=CARTESIAN_POINT('Ctrl Pts',(83.8004916423735,-3.76865384235248,2.33734320296745));
#10487=CARTESIAN_POINT('Ctrl Pts',(83.8009191948214,-3.77384083332494,2.32899647516146));
#10488=CARTESIAN_POINT('Ctrl Pts',(83.8013477666393,-3.77899902712594,2.3206330799814));
#10489=CARTESIAN_POINT('Ctrl Pts',(83.8017773998531,-3.78412829715226,2.31225321102945));
#10490=CARTESIAN_POINT('Ctrl Pts',(83.8041810383647,-3.81282466087439,2.26537095173032));
#10491=CARTESIAN_POINT('Ctrl Pts',(83.8066179712436,-3.8406151563232,2.21797404828616));
#10492=CARTESIAN_POINT('Ctrl Pts',(83.8090956800703,-3.86747750675075,2.17009996787264));
#10493=CARTESIAN_POINT('Ctrl Pts',(83.8090977039212,-3.86749944855063,2.17006086319733));
#10494=CARTESIAN_POINT('Ctrl Pts',(83.8090997277993,-3.86752138973141,2.17002175820357));
#10495=CARTESIAN_POINT('Ctrl Pts',(83.8091017517046,-3.8675433302931,2.16998265289143));
#10496=CARTESIAN_POINT('Ctrl Pts',(83.8144007795553,-3.92498853209468,2.06759637036372));
#10497=CARTESIAN_POINT('Ctrl Pts',(83.8198957562386,-3.97832517195201,1.96276873835478));
#10498=CARTESIAN_POINT('Ctrl Pts',(83.825505383901,-4.02739117448023,1.85586145227348));
#10499=CARTESIAN_POINT('Ctrl Pts',(83.8261913020303,-4.03339072787186,1.84278934658422));
#10500=CARTESIAN_POINT('Ctrl Pts',(83.8268789343311,-4.03932643526781,1.82968621130896));
#10501=CARTESIAN_POINT('Ctrl Pts',(83.8275681321777,-4.04519800591419,1.81655276077925));
#10502=CARTESIAN_POINT('Ctrl Pts',(83.8338838104617,-4.09900396512889,1.69620031232743));
#10503=CARTESIAN_POINT('Ctrl Pts',(83.8403303453004,-4.14742402367748,1.57329554968749));
#10504=CARTESIAN_POINT('Ctrl Pts',(83.8468067626538,-4.19027938554954,1.44835441049137));
#10505=CARTESIAN_POINT('Ctrl Pts',(83.8532704385826,-4.23305043562794,1.3236590751127));
#10506=CARTESIAN_POINT('Ctrl Pts',(83.8597634953365,-4.2702791213177,1.19693534424601));
#10507=CARTESIAN_POINT('Ctrl Pts',(83.8662062977059,-4.30182808985253,1.06869775645993));
#10508=CARTESIAN_POINT('Ctrl Pts',(83.8706801815884,-4.32373570299136,0.979649537340729));
#10509=CARTESIAN_POINT('Ctrl Pts',(83.8751297259372,-4.34290503282981,0.889868301763519));
#10510=CARTESIAN_POINT('Ctrl Pts',(83.8794335881289,-4.35912518117283,0.799504371769359));
#10511=CARTESIAN_POINT('Ctrl Pts',(83.8813204430654,-4.3662362515575,0.759887948242621));
#10512=CARTESIAN_POINT('Ctrl Pts',(83.8831792974447,-4.37278033297821,0.720160187088544));
#10513=CARTESIAN_POINT('Ctrl Pts',(83.8849999264898,-4.37873913709929,0.680336875005218));
#10514=CARTESIAN_POINT('Ctrl Pts',(83.8909649371895,-4.39826224118045,0.549861925525245));
#10515=CARTESIAN_POINT('Ctrl Pts',(83.8968658543233,-4.4120960442704,0.418457158923947));
#10516=CARTESIAN_POINT('Ctrl Pts',(83.9027691917311,-4.4203396281389,0.286618145884316));
#10517=CARTESIAN_POINT('Ctrl Pts',(83.907044634625,-4.42630997501838,0.191134840000573));
#10518=CARTESIAN_POINT('Ctrl Pts',(83.9113213748735,-4.42934795132635,0.0954213214250343));
#10519=CARTESIAN_POINT('Ctrl Pts',(83.915600810406,-4.42944218562652,-0.000347422039578667));
#10520=CARTESIAN_POINT('',(85.1613954767416,-4.43439065261444,-0.00220057529882202));
#10521=CARTESIAN_POINT('Ctrl Pts',(83.9156030730062,-4.42944223517521,-0.000398056376253822));
#10522=CARTESIAN_POINT('Ctrl Pts',(83.9200220896795,-4.42945985862297,-0.100320665778061));
#10523=CARTESIAN_POINT('Ctrl Pts',(83.9245029427185,-4.42639348513736,-0.200087969978499));
#10524=CARTESIAN_POINT('Ctrl Pts',(83.9289760356259,-4.42011577234908,-0.299621035218978));
#10525=CARTESIAN_POINT('Ctrl Pts',(83.9305230564219,-4.41794462311603,-0.334044581747511));
#10526=CARTESIAN_POINT('Ctrl Pts',(83.9320691490095,-4.41538902195064,-0.368439800463256));
#10527=CARTESIAN_POINT('Ctrl Pts',(83.9336114343194,-4.4124426794653,-0.402802392015783));
#10528=CARTESIAN_POINT('Ctrl Pts',(83.9399260209631,-4.40037945433718,-0.543493326605526));
#10529=CARTESIAN_POINT('Ctrl Pts',(83.9459499749625,-4.38139419249402,-0.683482294095519));
#10530=CARTESIAN_POINT('Ctrl Pts',(83.9517310700353,-4.35555705311141,-0.822055333667062));
#10531=CARTESIAN_POINT('Ctrl Pts',(83.9572489548599,-4.33089626523016,-0.954319214909025));
#10532=CARTESIAN_POINT('Ctrl Pts',(83.962705971755,-4.30026642860534,-1.08534392858136));
#10533=CARTESIAN_POINT('Ctrl Pts',(83.9681825322541,-4.26378442005296,-1.21458324295616));
#10534=CARTESIAN_POINT('Ctrl Pts',(83.973361322082,-4.22928600543357,-1.33679557800421));
#10535=CARTESIAN_POINT('Ctrl Pts',(83.9785580193129,-4.18955396851155,-1.45741185058128));
#10536=CARTESIAN_POINT('Ctrl Pts',(83.9838564405357,-4.14472505692022,-1.57596796994945));
#10537=CARTESIAN_POINT('Ctrl Pts',(83.9841690471093,-4.14208015349308,-1.58296277475942));
#10538=CARTESIAN_POINT('Ctrl Pts',(83.9844820077835,-4.13941750629901,-1.58995042318379));
#10539=CARTESIAN_POINT('Ctrl Pts',(83.9847953397724,-4.13673714269204,-1.59693082553478));
#10540=CARTESIAN_POINT('Ctrl Pts',(83.989745650979,-4.09439025673095,-1.70721373698422));
#10541=CARTESIAN_POINT('Ctrl Pts',(83.994789192224,-4.04762128275976,-1.81568482447509));
#10542=CARTESIAN_POINT('Ctrl Pts',(84.0000005781829,-3.99657730699651,-1.92196719207186));
#10543=CARTESIAN_POINT('Ctrl Pts',(84.0007224333611,-3.98950695018371,-1.93668889528134));
#10544=CARTESIAN_POINT('Ctrl Pts',(84.0014475088764,-3.98235457773494,-1.95136868637714));
#10545=CARTESIAN_POINT('Ctrl Pts',(84.0021760030253,-3.97512058473301,-1.96600564259331));
#10546=CARTESIAN_POINT('Ctrl Pts',(84.0029981870553,-3.96695624528217,-1.98252502256009));
#10547=CARTESIAN_POINT('Ctrl Pts',(84.003824730455,-3.95868802532439,-1.99898971458215));
#10548=CARTESIAN_POINT('Ctrl Pts',(84.0046559199584,-3.9503165789104,-2.01539830187999));
#10549=CARTESIAN_POINT('Ctrl Pts',(84.0046579578214,-3.95029605427527,-2.01543853151902));
#10550=CARTESIAN_POINT('Ctrl Pts',(84.0046599957124,-3.95027552901963,-2.01547876082083));
#10551=CARTESIAN_POINT('Ctrl Pts',(84.0046620336313,-3.95025500314353,-2.01551898978539));
#10552=CARTESIAN_POINT('Ctrl Pts',(84.0098464822127,-3.89803734672897,-2.11786113776804));
#10553=CARTESIAN_POINT('Ctrl Pts',(84.0152204254087,-3.84167465055871,-2.21825612911228));
#10554=CARTESIAN_POINT('Ctrl Pts',(84.020706973181,-3.78136802300308,-2.31637084667125));
#10555=CARTESIAN_POINT('Ctrl Pts',(84.021263903114,-3.77524640200608,-2.32633030120334));
#10556=CARTESIAN_POINT('Ctrl Pts',(84.0218219933164,-3.76908418364762,-2.33626624232669));
#10557=CARTESIAN_POINT('Ctrl Pts',(84.0223811633663,-3.76288160597131,-2.3461783102358));
#10558=CARTESIAN_POINT('Ctrl Pts',(84.0284415357854,-3.69565709942856,-2.45360685184891));
#10559=CARTESIAN_POINT('Ctrl Pts',(84.0346282174866,-3.62368643149239,-2.55823383882937));
#10560=CARTESIAN_POINT('Ctrl Pts',(84.0408496095882,-3.54727283849583,-2.65965152486281));
#10561=CARTESIAN_POINT('Ctrl Pts',(84.0470649488748,-3.4709335885614,-2.76097054126119));
#10562=CARTESIAN_POINT('Ctrl Pts',(84.0533145802337,-3.39016033354804,-2.8590867479529));
#10563=CARTESIAN_POINT('Ctrl Pts',(84.0595245500108,-3.30528192202576,-2.95362680933311));
#10564=CARTESIAN_POINT('Ctrl Pts',(84.0642453959957,-3.24075698508966,-3.02549657443695));
#10565=CARTESIAN_POINT('Ctrl Pts',(84.0689432014021,-3.17385757186749,-3.09530178468054));
#10566=CARTESIAN_POINT('Ctrl Pts',(84.0735010891228,-3.10463126550535,-3.16276943169823));
#10567=CARTESIAN_POINT('Ctrl Pts',(84.0749344687681,-3.08286074711311,-3.18398688106778));
#10568=CARTESIAN_POINT('Ctrl Pts',(84.0763540105883,-3.06086037940469,-3.20497287834147));
#10569=CARTESIAN_POINT('Ctrl Pts',(84.077756079434,-3.03863244229489,-3.22571822680655));
#10570=CARTESIAN_POINT('Ctrl Pts',(84.0826619466766,-2.96085644087079,-3.298306620583));
#10571=CARTESIAN_POINT('Ctrl Pts',(84.0874437688791,-2.88040415007025,-3.36805936072332));
#10572=CARTESIAN_POINT('Ctrl Pts',(84.0922045774475,-2.79763216707804,-3.43495049127518));
#10573=CARTESIAN_POINT('Ctrl Pts',(84.0931287399803,-2.7815645675626,-3.44793531848348));
#10574=CARTESIAN_POINT('Ctrl Pts',(84.0940521106749,-2.76540943083509,-3.46081240846906));
#10575=CARTESIAN_POINT('Ctrl Pts',(84.0949754431863,-2.74916917906846,-3.47358170203163));
#10576=CARTESIAN_POINT('Ctrl Pts',(84.1025236857171,-2.61640513405698,-3.57797066654195));
#10577=CARTESIAN_POINT('Ctrl Pts',(84.1100694581678,-2.47795358470528,-3.67516035798));
#10578=CARTESIAN_POINT('Ctrl Pts',(84.1176181112967,-2.33464800299958,-3.76457020605654));
#10579=CARTESIAN_POINT('Ctrl Pts',(84.1214282800525,-2.26231477472148,-3.80969966210601));
#10580=CARTESIAN_POINT('Ctrl Pts',(84.1252391669181,-2.18874467800358,-3.85284616832275));
#10581=CARTESIAN_POINT('Ctrl Pts',(84.1290513879722,-2.11404396154338,-3.89392997526874));
#10582=CARTESIAN_POINT('Ctrl Pts',(84.1343997316991,-2.00924282262703,-3.95156837504573));
#10583=CARTESIAN_POINT('Ctrl Pts',(84.1395900454753,-1.90207862838257,-4.00490400576711));
#10584=CARTESIAN_POINT('Ctrl Pts',(84.1445355063654,-1.79286940114767,-4.05352855524393));
#10585=CARTESIAN_POINT('Ctrl Pts',(84.1448461261242,-1.78601007204187,-4.05658261757847));
#10586=CARTESIAN_POINT('Ctrl Pts',(84.1451557799437,-1.77914269155742,-4.05961808944955));
#10587=CARTESIAN_POINT('Ctrl Pts',(84.1454644463109,-1.77226734507983,-4.06263486767839));
#10588=CARTESIAN_POINT('Ctrl Pts',(84.1506930242929,-1.6558041050483,-4.11373684023112));
#10589=CARTESIAN_POINT('Ctrl Pts',(84.1558618313948,-1.53721142653457,-4.15982835192703));
#10590=CARTESIAN_POINT('Ctrl Pts',(84.1610351961871,-1.41695144635677,-4.20071349901739));
#10591=CARTESIAN_POINT('Ctrl Pts',(84.1662116927519,-1.29661866503086,-4.24162339653298));
#10592=CARTESIAN_POINT('Ctrl Pts',(84.1713931150129,-1.17461651478789,-4.27732022802709));
#10593=CARTESIAN_POINT('Ctrl Pts',(84.1766599594209,-1.05143177192609,-4.30764600656593));
#10594=CARTESIAN_POINT('Ctrl Pts',(84.1815263579785,-0.937612944456394,
-4.33566607199942));
#10595=CARTESIAN_POINT('Ctrl Pts',(84.1864661287189,-0.82278399811288,-4.35910082126407));
#10596=CARTESIAN_POINT('Ctrl Pts',(84.1915502021094,-0.707349358148297,
-4.37785988037722));
#10597=CARTESIAN_POINT('Ctrl Pts',(84.1919764438846,-0.697671475456709,
-4.37943261429451));
#10598=CARTESIAN_POINT('Ctrl Pts',(84.1924036999512,-0.687989313361263,
-4.38097250404709));
#10599=CARTESIAN_POINT('Ctrl Pts',(84.1928320121081,-0.678303097849305,
-4.38247950761368));
#10600=CARTESIAN_POINT('Ctrl Pts',(84.1952646007355,-0.623290469050379,
-4.39103849824374));
#10601=CARTESIAN_POINT('Ctrl Pts',(84.1977313301607,-0.568148240667956,
-4.39853655272527));
#10602=CARTESIAN_POINT('Ctrl Pts',(84.2002399855675,-0.512921282444363,
-4.40496731133519));
#10603=CARTESIAN_POINT('Ctrl Pts',(84.2002420223226,-0.512876444166573,
-4.4049725324111));
#10604=CARTESIAN_POINT('Ctrl Pts',(84.2002440591053,-0.512831605832806,
-4.40497775278361));
#10605=CARTESIAN_POINT('Ctrl Pts',(84.2002460959157,-0.512786767443101,
-4.40498297245274));
#10606=CARTESIAN_POINT('Ctrl Pts',(84.2054311220285,-0.398643484480754,
-4.41827047396691));
#10607=CARTESIAN_POINT('Ctrl Pts',(84.2108055944895,-0.283822881198216,
-4.4270271922881));
#10608=CARTESIAN_POINT('Ctrl Pts',(84.2162926444345,-0.168713809015507,
-4.43123589822478));
#10609=CARTESIAN_POINT('Ctrl Pts',(84.2168497233916,-0.157027230155568,
-4.43166319185937));
#10610=CARTESIAN_POINT('Ctrl Pts',(84.2174079627475,-0.145337715089774,
-4.43204363065165));
#10611=CARTESIAN_POINT('Ctrl Pts',(84.2179672820597,-0.133645695587933,
-4.4323772133244));
#10612=CARTESIAN_POINT('Ctrl Pts',(84.2240283194387,-0.00694567704394078,
-4.43599206624319));
#10613=CARTESIAN_POINT('Ctrl Pts',(84.2302156387763,0.120053657973535,-4.4341017418951));
#10614=CARTESIAN_POINT('Ctrl Pts',(84.2364376599109,0.246844678988904,-4.42673266576923));
#10615=CARTESIAN_POINT('Ctrl Pts',(84.242653642254,0.373512642795672,-4.41937074171085));
#10616=CARTESIAN_POINT('Ctrl Pts',(84.2489039080635,0.499972749915472,-4.40654106651511));
#10617=CARTESIAN_POINT('Ctrl Pts',(84.2551145213253,0.62573182461737,-4.38831046061018));
#10618=CARTESIAN_POINT('Ctrl Pts',(84.2598428657655,0.721476350417396,-4.37443089985839));
#10619=CARTESIAN_POINT('Ctrl Pts',(84.2645481063376,0.816817457352416,-4.35742027862559));
#10620=CARTESIAN_POINT('Ctrl Pts',(84.2691135469234,0.911500643384384,-4.33716756098911));
#10621=CARTESIAN_POINT('Ctrl Pts',(84.2705404182196,0.941092687753812,-4.330837827654));
#10622=CARTESIAN_POINT('Ctrl Pts',(84.2719536338983,0.970620092880962,-4.32419149102998));
#10623=CARTESIAN_POINT('Ctrl Pts',(84.2733496313951,1.00007407902062,-4.3172254305111));
#10624=CARTESIAN_POINT('Ctrl Pts',(84.2782487153611,1.10343927240734,-4.29277888567797));
#10625=CARTESIAN_POINT('Ctrl Pts',(84.2830233214964,1.20593053517353,-4.26454360145908));
#10626=CARTESIAN_POINT('Ctrl Pts',(84.2877766640604,1.30732974394678,-4.23280178892722));
#10627=CARTESIAN_POINT('Ctrl Pts',(84.2887094415093,1.32722793012016,-4.2265728991471));
#10628=CARTESIAN_POINT('Ctrl Pts',(84.2896414001277,1.34708421448667,-4.22020892404134));
#10629=CARTESIAN_POINT('Ctrl Pts',(84.2905733198829,1.36689716823111,-4.21371191096212));
#10630=CARTESIAN_POINT('Ctrl Pts',(84.2981220981959,1.52738694721297,-4.16108451342339));
#10631=CARTESIAN_POINT('Ctrl Pts',(84.3056684083374,1.68503722575149,-4.09973129194983));
#10632=CARTESIAN_POINT('Ctrl Pts',(84.3132176001518,1.83890268277897,-4.03002407267672));
#10633=CARTESIAN_POINT('Ctrl Pts',(84.3170293094954,1.91659184668235,-3.9948277674892));
#10634=CARTESIAN_POINT('Ctrl Pts',(84.3208417376448,1.9933154911568,-3.95750103751852));
#10635=CARTESIAN_POINT('Ctrl Pts',(84.3246555010349,2.06894820376035,-3.9180881461032));
#10636=CARTESIAN_POINT('Ctrl Pts',(84.3303408196572,2.18169669532784,-3.85933388617491));
#10637=CARTESIAN_POINT('Ctrl Pts',(84.3358434779605,2.29187550637682,-3.79565548959621));
#10638=CARTESIAN_POINT('Ctrl Pts',(84.3410678358074,2.39887081547596,-3.72711308762104));
#10639=CARTESIAN_POINT('Ctrl Pts',(84.346297747787,2.50597987370265,-3.65849781667161));
#10640=CARTESIAN_POINT('Ctrl Pts',(84.3514680195384,2.6100981748788,-3.58533117720361));
#10641=CARTESIAN_POINT('Ctrl Pts',(84.3566430066945,2.71080634011115,-3.50788928878811));
#10642=CARTESIAN_POINT('Ctrl Pts',(84.3618211287584,2.81157551241485,-3.43040048756468));
#10643=CARTESIAN_POINT('Ctrl Pts',(84.3670043347982,2.90893011277071,-3.34863099623333));
#10644=CARTESIAN_POINT('Ctrl Pts',(84.372273141828,3.00246865738971,-3.26289847479069));
#10645=CARTESIAN_POINT('Ctrl Pts',(84.377140630556,3.08888249053952,-3.18369609000235));
#10646=CARTESIAN_POINT('Ctrl Pts',(84.3820816227187,3.1720397850012,-3.10111099545226));
#10647=CARTESIAN_POINT('Ctrl Pts',(84.3871670230929,3.25164114268718,-3.01542965871224));
#10648=CARTESIAN_POINT('Ctrl Pts',(84.3875941892897,3.25832754035971,-3.00823255168778));
#10649=CARTESIAN_POINT('Ctrl Pts',(84.3880223743954,3.26498887791591,-3.00101359155394));
#10650=CARTESIAN_POINT('Ctrl Pts',(84.3884516204334,3.27162499419796,-2.99377294403262));
#10651=CARTESIAN_POINT('Ctrl Pts',(84.3908738698233,3.30907281478261,-2.95291373395086));
#10652=CARTESIAN_POINT('Ctrl Pts',(84.3933299774408,3.34571674374655,-2.91136478436287));
#10653=CARTESIAN_POINT('Ctrl Pts',(84.3958276195801,3.38152702007041,-2.869159449948));
#10654=CARTESIAN_POINT('Ctrl Pts',(84.3958296535773,3.38155618277521,-2.86912507931938));
#10655=CARTESIAN_POINT('Ctrl Pts',(84.395831687602,3.38158534492731,-2.86909070825542));
#10656=CARTESIAN_POINT('Ctrl Pts',(84.3958337216543,3.38161450652671,-2.86905633675616));
#10657=CARTESIAN_POINT('Ctrl Pts',(84.4010193379607,3.4559591379798,-2.78142957766832));
#10658=CARTESIAN_POINT('Ctrl Pts',(84.4063943313847,3.52690871113519,-2.69072693480184));
#10659=CARTESIAN_POINT('Ctrl Pts',(84.4118818220266,3.59423325632701,-2.59726247276966));
#10660=CARTESIAN_POINT('Ctrl Pts',(84.4124385352232,3.60106342064289,-2.58778037925449));
#10661=CARTESIAN_POINT('Ctrl Pts',(84.412996406283,3.6078562742022,-2.57826990430067));
#10662=CARTESIAN_POINT('Ctrl Pts',(84.4135553549299,3.61461157703828,-2.56873140574106));
#10663=CARTESIAN_POINT('Ctrl Pts',(84.4196164272486,3.68786406499651,-2.46529877395051));
#10664=CARTESIAN_POINT('Ctrl Pts',(84.4258036729112,3.75670158311348,-2.35856499542504));
#10665=CARTESIAN_POINT('Ctrl Pts',(84.4320255247527,3.82086467332084,-2.24896710701901));
#10666=CARTESIAN_POINT('Ctrl Pts',(84.4382413353983,3.88496546345941,-2.13947563424797));
#10667=CARTESIAN_POINT('Ctrl Pts',(84.4444913342497,3.9444012366354,-2.02712577217479));
#10668=CARTESIAN_POINT('Ctrl Pts',(84.4507016014946,3.99895415777029,-1.91236493124856));
#10669=CARTESIAN_POINT('Ctrl Pts',(84.4554152926301,4.04036068837952,-1.8252596365421));
#10670=CARTESIAN_POINT('Ctrl Pts',(84.4601059748468,4.07895536305849,-1.73676263301112));
#10671=CARTESIAN_POINT('Ctrl Pts',(84.4646566137891,4.11450449761833,-1.64702193201489));
#10672=CARTESIAN_POINT('Ctrl Pts',(84.4660970909123,4.12575736028934,-1.61861505806947));
#10673=CARTESIAN_POINT('Ctrl Pts',(84.4675235356913,4.13670491876008,-1.59008393111965));
#10674=CARTESIAN_POINT('Ctrl Pts',(84.4689322360632,4.1473394108455,-1.56143427734726));
#10675=CARTESIAN_POINT('Ctrl Pts',(84.4738515811032,4.18447629029761,-1.46138636439162));
#10676=CARTESIAN_POINT('Ctrl Pts',(84.4786476553848,4.21794505108998,-1.35995378726379));
#10677=CARTESIAN_POINT('Ctrl Pts',(84.4834231452708,4.24785814235454,-1.25747763211181));
#10678=CARTESIAN_POINT('Ctrl Pts',(84.4843331475761,4.25355828677076,-1.237950098885));
#10679=CARTESIAN_POINT('Ctrl Pts',(84.4852424024226,4.25912935472623,-1.21838452374533));
#10680=CARTESIAN_POINT('Ctrl Pts',(84.486151620347,4.26457216996989,-1.19878305716253));
#10681=CARTESIAN_POINT('Ctrl Pts',(84.4937000912189,4.30975928213367,-1.03604858439437));
#10682=CARTESIAN_POINT('Ctrl Pts',(84.5012460990225,4.34611122439299,-0.870839143295207));
#10683=CARTESIAN_POINT('Ctrl Pts',(84.5087949932654,4.37341321007671,-0.704147472553858));
#10684=CARTESIAN_POINT('Ctrl Pts',(84.5126064128654,4.38719792079147,-0.61998522566277));
#10685=CARTESIAN_POINT('Ctrl Pts',(84.516418552402,4.39867471587451,-0.535445277101942));
#10686=CARTESIAN_POINT('Ctrl Pts',(84.5202320281092,4.40781088907457,-0.450656510645831));
#10687=CARTESIAN_POINT('Ctrl Pts',(84.5256130576088,4.42070254521122,-0.331014774716957));
#10688=CARTESIAN_POINT('Ctrl Pts',(84.5308328806464,4.42865113939397,-0.210843533130558));
#10689=CARTESIAN_POINT('Ctrl Pts',(84.5358053747255,4.43140167015233,-0.0906023001580588));
#10690=CARTESIAN_POINT('Ctrl Pts',(84.5360862929687,4.43155705983328,-0.0838093396460685));
#10691=CARTESIAN_POINT('Ctrl Pts',(84.5363664218315,4.43169586038957,-0.0770161695411033));
#10692=CARTESIAN_POINT('Ctrl Pts',(84.5366457457854,4.43181802635749,-0.0702228776517116));
#10693=CARTESIAN_POINT('Ctrl Pts',(84.5418748984192,4.43410506434365,0.0569526104701331));
#10694=CARTESIAN_POINT('Ctrl Pts',(84.5470443992794,4.4309466875094,0.184162749014156));
#10695=CARTESIAN_POINT('Ctrl Pts',(84.552218609817,4.42234015442795,0.310905475783738));
#10696=CARTESIAN_POINT('Ctrl Pts',(84.5573959553126,4.41372840680822,0.437724993613409));
#10697=CARTESIAN_POINT('Ctrl Pts',(84.5625783790404,4.39966151476501,0.564076424817015));
#10698=CARTESIAN_POINT('Ctrl Pts',(84.5678464009617,4.38018123020949,0.689449568885464));
#10699=CARTESIAN_POINT('Ctrl Pts',(84.572713127436,4.36218487066706,0.805272321432545));
#10700=CARTESIAN_POINT('Ctrl Pts',(84.5776533538143,4.33956828933044,0.92026065161261));
#10701=CARTESIAN_POINT('Ctrl Pts',(84.582737983543,4.31240388012754,1.03400661169041));
#10702=CARTESIAN_POINT('Ctrl Pts',(84.5831651303285,4.31012186733797,1.04356211991886));
#10703=CARTESIAN_POINT('Ctrl Pts',(84.5835932962048,4.30780777020741,1.05310888891236));
#10704=CARTESIAN_POINT('Ctrl Pts',(84.5840225232079,4.30546163731095,1.06264669262437));
#10705=CARTESIAN_POINT('Ctrl Pts',(84.5864476969319,4.29220576148621,1.11653619813248));
#10706=CARTESIAN_POINT('Ctrl Pts',(84.5889068199102,4.27792749735515,1.17013839040833));
#10707=CARTESIAN_POINT('Ctrl Pts',(84.5914075994229,4.2626381487069,1.22340983725583));
#10708=CARTESIAN_POINT('Ctrl Pts',(84.591409635184,4.26262570240342,1.22345320290926));
#10709=CARTESIAN_POINT('Ctrl Pts',(84.5914116709727,4.26261325542998,1.22349656834367));
#10710=CARTESIAN_POINT('Ctrl Pts',(84.591413706789,4.26260080778662,1.22353993355905));
#10711=CARTESIAN_POINT('Ctrl Pts',(84.5965988639289,4.23089706942438,1.33398971130982));
#10712=CARTESIAN_POINT('Ctrl Pts',(84.6019734473727,4.19475153083039,1.44331960372824));
#10713=CARTESIAN_POINT('Ctrl Pts',(84.607460578133,4.15429803545426,1.55116413066714));
#10714=CARTESIAN_POINT('Ctrl Pts',(84.6080174542468,4.15019250448003,1.56210902038882));
#10715=CARTESIAN_POINT('Ctrl Pts',(84.6085754895695,4.14604263913158,1.57303858616504));
#10716=CARTESIAN_POINT('Ctrl Pts',(84.6091346037398,4.14184860431232,1.58395242950338));
#10717=CARTESIAN_POINT('Ctrl Pts',(84.6151954975086,4.09638454552827,1.70226036839237));
#10718=CARTESIAN_POINT('Ctrl Pts',(84.6213826301699,4.04572545282814,1.81872446903964));
#10719=CARTESIAN_POINT('Ctrl Pts',(84.6276044230074,3.99009117374434,1.93288649496196));
#10720=CARTESIAN_POINT('Ctrl Pts',(84.6338201725864,3.93451093251407,2.04693763473753));
#10721=CARTESIAN_POINT('Ctrl Pts',(84.6400701641749,3.87396548678901,2.1586913614496));
#10722=CARTESIAN_POINT('Ctrl Pts',(84.6462804649277,3.80870639577885,2.26771832871206));
#10723=CARTESIAN_POINT('Ctrl Pts',(84.65100029518,3.75910946895452,2.35057885333004));
#10724=CARTESIAN_POINT('Ctrl Pts',(84.6556970803124,3.70678832164182,2.43186689386273));
#10725=CARTESIAN_POINT('Ctrl Pts',(84.660253925992,3.65173737784779,2.51130545350703));
#10726=CARTESIAN_POINT('Ctrl Pts',(84.6616885949146,3.63440523983481,2.53631574369312));
#10727=CARTESIAN_POINT('Ctrl Pts',(84.6631093926092,3.61680274000409,2.56114239081144));
#10728=CARTESIAN_POINT('Ctrl Pts',(84.6645126710695,3.59893035714528,2.58577590195689));
#10729=CARTESIAN_POINT('Ctrl Pts',(84.6694225893463,3.53639683886947,2.67196587066897));
#10730=CARTESIAN_POINT('Ctrl Pts',(84.674208683927,3.47068942515095,2.75587981751586));
#10731=CARTESIAN_POINT('Ctrl Pts',(84.6789738848567,3.4021535104872,2.83742357267385));
#10732=CARTESIAN_POINT('Ctrl Pts',(84.679894240563,3.38891641490988,2.85317301566378));
#10733=CARTESIAN_POINT('Ctrl Pts',(84.6808138168642,3.37557370148446,2.8688341578141));
#10734=CARTESIAN_POINT('Ctrl Pts',(84.6817333553531,3.362127703261,2.88440648181033));
#10735=CARTESIAN_POINT('Ctrl Pts',(84.6892818648234,3.25174924041889,3.01223999457874));
#10736=CARTESIAN_POINT('Ctrl Pts',(84.6968279079958,3.13441231669963,3.13409281579267));
#10737=CARTESIAN_POINT('Ctrl Pts',(84.7043768347802,3.01082409715453,3.24923579076595));
#10738=CARTESIAN_POINT('Ctrl Pts',(84.7081880418649,2.94842843332505,3.30736772587436));
#10739=CARTESIAN_POINT('Ctrl Pts',(84.7119999681048,2.88443900415451,3.36378856116201));
#10740=CARTESIAN_POINT('Ctrl Pts',(84.7158132297576,2.81894492700688,3.41839963964567));
#10741=CARTESIAN_POINT('Ctrl Pts',(84.7212084245133,2.72628060608488,3.49566614560924));
#10742=CARTESIAN_POINT('Ctrl Pts',(84.7264411225267,2.63041772563086,3.56909176912647));
#10743=CARTESIAN_POINT('Ctrl Pts',(84.7314255010948,2.53160030781325,3.63820716678816));
#10744=CARTESIAN_POINT('Ctrl Pts',(84.7316931778632,2.52629350242069,3.64191888050341));
#10745=CARTESIAN_POINT('Ctrl Pts',(84.7319601384716,2.5209781870118,3.64561815736127));
#10746=CARTESIAN_POINT('Ctrl Pts',(84.7322263696277,2.51565440316096,3.64930492268869));
#10747=CARTESIAN_POINT('Ctrl Pts',(84.7374556145453,2.41108598956213,3.7217194331949));
#10748=CARTESIAN_POINT('Ctrl Pts',(84.7426251826069,2.30346961961977,3.78962151737821));
#10749=CARTESIAN_POINT('Ctrl Pts',(84.7477994256095,2.19322158624946,3.85273053620533));
#10750=CARTESIAN_POINT('Ctrl Pts',(84.7529768027908,2.08290677266984,3.9158777818684));
#10751=CARTESIAN_POINT('Ctrl Pts',(84.7581592233412,1.96995698362092,3.97422577405039));
#10752=CARTESIAN_POINT('Ctrl Pts',(84.7634272006878,1.85481995124432,4.02752638811055));
#10753=CARTESIAN_POINT('Ctrl Pts',(84.7682940795581,1.74844933626545,4.07676874723082));
#10754=CARTESIAN_POINT('Ctrl Pts',(84.7732344287618,1.64021136687734,4.12170321913324));
#10755=CARTESIAN_POINT('Ctrl Pts',(84.7783191586336,1.53048571385177,4.16216385123994));
#10756=CARTESIAN_POINT('Ctrl Pts',(84.778746094102,1.52127268302028,4.16556109737866));
#10757=CARTESIAN_POINT('Ctrl Pts',(84.7791740474533,1.51204914634207,4.16892682775203));
#10758=CARTESIAN_POINT('Ctrl Pts',(84.7796030606624,1.50281531855477,4.17226095757485));
#10759=CARTESIAN_POINT('Ctrl Pts',(84.7820291275204,1.45059808353492,4.1911154396548));
#10760=CARTESIAN_POINT('Ctrl Pts',(84.7844891619393,1.39805284444655,4.20895901044887));
#10761=CARTESIAN_POINT('Ctrl Pts',(84.7869908804251,1.3452220621743,4.22577697960224));
#10762=CARTESIAN_POINT('Ctrl Pts',(84.7869929158898,1.34517907764301,4.22579066314979));
#10763=CARTESIAN_POINT('Ctrl Pts',(84.7869949513822,1.3451360929226,4.22580434601856));
#10764=CARTESIAN_POINT('Ctrl Pts',(84.7869969869022,1.34509310801311,4.22581802820855));
#10765=CARTESIAN_POINT('Ctrl Pts',(84.7921822518366,1.23559374319761,4.26067191370071));
#10766=CARTESIAN_POINT('Ctrl Pts',(84.7975569329699,1.12456366365035,4.29120810213901));
#10767=CARTESIAN_POINT('Ctrl Pts',(84.8030441534666,1.01238125775074,4.31733535217763));
#10768=CARTESIAN_POINT('Ctrl Pts',(84.8036010288402,1.00099632812464,4.31998689901002));
#10769=CARTESIAN_POINT('Ctrl Pts',(84.8041590632998,0.9895995713314,4.32259305297463));
#10770=CARTESIAN_POINT('Ctrl Pts',(84.8047181764906,0.978191410431902,4.32515373038107));
#10771=CARTESIAN_POINT('Ctrl Pts',(84.8107791588467,0.854522959968089,4.35291236823539));
#10772=CARTESIAN_POINT('Ctrl Pts',(84.81696637055,0.729508691004713,4.37532504084231));
#10773=CARTESIAN_POINT('Ctrl Pts',(84.8231882360403,0.603651872050102,4.39232065761651));
#10774=CARTESIAN_POINT('Ctrl Pts',(84.8294040599685,0.477917262707511,4.40929977129021));
#10775=CARTESIAN_POINT('Ctrl Pts',(84.8356541195363,0.351341757595756,4.42087271830061));
#10776=CARTESIAN_POINT('Ctrl Pts',(84.8418644850906,0.224422162691511,4.42701081737272));
#10777=CARTESIAN_POINT('Ctrl Pts',(84.846584481589,0.127960845190481,4.43167588996372));
#10778=CARTESIAN_POINT('Ctrl Pts',(84.8512814299853,0.0312977998886688,
4.43320167315009));
#10779=CARTESIAN_POINT('Ctrl Pts',(84.8558384408538,-0.065339516415513,
4.43142996286704));
#10780=CARTESIAN_POINT('Ctrl Pts',(84.8572730147889,-0.0957615143271973,
4.43087221800623));
#10781=CARTESIAN_POINT('Ctrl Pts',(84.858693720529,-0.126180574620701,4.42998769318179));
#10782=CARTESIAN_POINT('Ctrl Pts',(84.8600969113421,-0.15658853336999,4.42877152555789));
#10783=CARTESIAN_POINT('Ctrl Pts',(84.8650070541574,-0.262994175985198,
4.4245158272844));
#10784=CARTESIAN_POINT('Ctrl Pts',(84.8697933831841,-0.369265327470869,
4.41635646912889));
#10785=CARTESIAN_POINT('Ctrl Pts',(84.8745588233476,-0.475132086597381,
4.40452868377238));
#10786=CARTESIAN_POINT('Ctrl Pts',(84.8754790548376,-0.495575513048501,
4.40224467638413));
#10787=CARTESIAN_POINT('Ctrl Pts',(84.8763985073895,-0.516004014129667,
4.39982385132363));
#10788=CARTESIAN_POINT('Ctrl Pts',(84.8773179221476,-0.536415866514308,
4.39726786245597));
#10789=CARTESIAN_POINT('Ctrl Pts',(84.8848664844736,-0.704000885742749,
4.37628272913923));
#10790=CARTESIAN_POINT('Ctrl Pts',(84.8924125810314,-0.870466541977115,
4.34619055125258));
#10791=CARTESIAN_POINT('Ctrl Pts',(84.8999615615935,-1.03481393150272,4.30717557716655));
#10792=CARTESIAN_POINT('Ctrl Pts',(84.903772953535,-1.1177910051455,4.28747737333592));
#10793=CARTESIAN_POINT('Ctrl Pts',(84.9075850647847,-1.20022762712079,4.26550388113197));
#10794=CARTESIAN_POINT('Ctrl Pts',(84.9113985116357,-1.28199226514604,4.24127456962471));
#10795=CARTESIAN_POINT('Ctrl Pts',(84.9170835661561,-1.40388630043182,4.20515371563275));
#10796=CARTESIAN_POINT('Ctrl Pts',(84.9225878106938,-1.52420041891705,4.16371187006001));
#10797=CARTESIAN_POINT('Ctrl Pts',(84.9278116334488,-1.64231834212475,4.11688424728089));
#10798=CARTESIAN_POINT('Ctrl Pts',(84.9330410104032,-1.76056185353242,4.07000683530217));
#10799=CARTESIAN_POINT('Ctrl Pts',(84.9382107268945,-1.87673977245805,4.01809080361348));
#10800=CARTESIAN_POINT('Ctrl Pts',(84.9433851385672,-1.9903877189014,3.96132701634406));
#10801=CARTESIAN_POINT('Ctrl Pts',(84.9485626848299,-2.10410451176347,3.90452884232514));
#10802=CARTESIAN_POINT('Ctrl Pts',(84.9537452947748,-2.21528801804004,3.84287672460635));
#10803=CARTESIAN_POINT('Ctrl Pts',(84.9590134846708,-2.3234834856855,3.77660572067685));
#10804=CARTESIAN_POINT('Ctrl Pts',(84.9638804636316,-2.42343908240562,3.71538173517016));
#10805=CARTESIAN_POINT('Ctrl Pts',(84.968820929834,-2.52084483146928,3.65021526271105));
#10806=CARTESIAN_POINT('Ctrl Pts',(84.9739057901906,-2.61535212615944,3.58133026333488));
#10807=CARTESIAN_POINT('Ctrl Pts',(84.9743328450834,-2.62328937512469,3.57554491743315));
#10808=CARTESIAN_POINT('Ctrl Pts',(84.9747609184714,-2.63120621006221,3.56973334163662));
#10809=CARTESIAN_POINT('Ctrl Pts',(84.9751900523596,-2.63910244121295,3.56389566774748));
#10810=CARTESIAN_POINT('Ctrl Pts',(84.9776149327083,-2.68372118671921,3.53090908457431));
#10811=CARTESIAN_POINT('Ctrl Pts',(84.980073748826,-2.72768115457495,3.49708990838663));
#10812=CARTESIAN_POINT('Ctrl Pts',(84.9825742047632,-2.77094663309581,3.46246528852012));
#10813=CARTESIAN_POINT('Ctrl Pts',(84.9825762399658,-2.7709818482784,3.46243710641392));
#10814=CARTESIAN_POINT('Ctrl Pts',(84.9825782751959,-2.77101706300107,3.46240892377413));
#10815=CARTESIAN_POINT('Ctrl Pts',(84.9825803104536,-2.77105227726383,3.46238074060078));
#10816=CARTESIAN_POINT('Ctrl Pts',(84.9877238771902,-2.86004685909416,3.39115534695546));
#10817=CARTESIAN_POINT('Ctrl Pts',(84.9930545253852,-2.94635632162763,3.31630800407411));
#10818=CARTESIAN_POINT('Ctrl Pts',(84.9984971023633,-3.02969499108077,3.23809704268377));
#10819=CARTESIAN_POINT('Ctrl Pts',(84.9990297304268,-3.03785078094115,3.23044306680363));
#10820=CARTESIAN_POINT('Ctrl Pts',(84.9995634304557,-3.04597811147377,3.22275691735968));
#10821=CARTESIAN_POINT('Ctrl Pts',(85.0000981320124,-3.05407671060235,3.21503886286153));
#10822=CARTESIAN_POINT('Ctrl Pts',(85.0060892369383,-3.14481809056789,3.12856132462402));
#10823=CARTESIAN_POINT('Ctrl Pts',(85.0122055586422,-3.23195384081772,3.03807262820168));
#10824=CARTESIAN_POINT('Ctrl Pts',(85.0183580489291,-3.31514896565735,2.94394188123819));
#10825=CARTESIAN_POINT('Ctrl Pts',(85.0245046105112,-3.39826392144045,2.84990184119039));
#10826=CARTESIAN_POINT('Ctrl Pts',(85.0306869278022,-3.47744610828712,2.75222700492221));
#10827=CARTESIAN_POINT('Ctrl Pts',(85.0368326469943,-3.5523992728702,2.65130570457177));
#10828=CARTESIAN_POINT('Ctrl Pts',(85.0416525936159,-3.61118332093922,2.57215544315203));
#10829=CARTESIAN_POINT('Ctrl Pts',(85.0464499027595,-3.6673678199014,2.4910059570415));
#10830=CARTESIAN_POINT('Ctrl Pts',(85.0511099558291,-3.7206914611155,2.40797628678268));
#10831=CARTESIAN_POINT('Ctrl Pts',(85.0523876421982,-3.73531165717613,2.38521133618301));
#10832=CARTESIAN_POINT('Ctrl Pts',(85.0536550104997,-3.74971663560365,2.36230530365738));
#10833=CARTESIAN_POINT('Ctrl Pts',(85.0549096983235,-3.76390067855733,2.33926124211762));
#10834=CARTESIAN_POINT('Ctrl Pts',(85.0596190440185,-3.81713907009516,2.25276765387323));
#10835=CARTESIAN_POINT('Ctrl Pts',(85.064193515815,-3.86732725704643,2.16437299960269));
#10836=CARTESIAN_POINT('Ctrl Pts',(85.0687410834779,-3.91452920585602,2.0744106404933));
#10837=CARTESIAN_POINT('Ctrl Pts',(85.0698220587615,-3.92574930059326,2.05302622274258));
#10838=CARTESIAN_POINT('Ctrl Pts',(85.070901513875,-3.93680077182231,2.03155301986239));
#10839=CARTESIAN_POINT('Ctrl Pts',(85.071980898965,-3.94768466915442,2.00999512024761));
#10840=CARTESIAN_POINT('Ctrl Pts',(85.079830432555,-4.02683484316675,1.85322117670665));
#10841=CARTESIAN_POINT('Ctrl Pts',(85.0876763508747,-4.09712788891073,1.69196762578581));
#10842=CARTESIAN_POINT('Ctrl Pts',(85.0955238651024,-4.15811534380005,1.52730392757633));
#10843=CARTESIAN_POINT('Ctrl Pts',(85.0989133218668,-4.18445672216733,1.45618325553379));
#10844=CARTESIAN_POINT('Ctrl Pts',(85.102303063988,-4.20906143190783,1.38442637930852));
#10845=CARTESIAN_POINT('Ctrl Pts',(85.1056934694908,-4.23189027752621,1.31211936362746));
#10846=CARTESIAN_POINT('Ctrl Pts',(85.1099652092317,-4.26065347030312,1.22101617488443));
#10847=CARTESIAN_POINT('Ctrl Pts',(85.1141833523306,-4.2865081857872,1.12900683519562));
#10848=CARTESIAN_POINT('Ctrl Pts',(85.1182333576414,-4.30916968856113,1.03625490534938));
#10849=CARTESIAN_POINT('Ctrl Pts',(85.119516655342,-4.31635028517076,1.00686523072654));
#10850=CARTESIAN_POINT('Ctrl Pts',(85.1207830716226,-4.32321018977212,0.977401381275448));
#10851=CARTESIAN_POINT('Ctrl Pts',(85.1220289624946,-4.32974014619538,0.947869635297526));
#10852=CARTESIAN_POINT('Ctrl Pts',(85.1272093075156,-4.35689134218187,0.82507827638232));
#10853=CARTESIAN_POINT('Ctrl Pts',(85.1323260084032,-4.37882950923063,0.701223348312286));
#10854=CARTESIAN_POINT('Ctrl Pts',(85.1374393902874,-4.39546272646208,0.576786473790793));
#10855=CARTESIAN_POINT('Ctrl Pts',(85.1425596171888,-4.41211820971229,0.452183022127615));
#10856=CARTESIAN_POINT('Ctrl Pts',(85.1476768541827,-4.42345416743842,0.32699612501574));
#10857=CARTESIAN_POINT('Ctrl Pts',(85.1528672740182,-4.4294206875847,0.201723058512749));
#10858=CARTESIAN_POINT('Ctrl Pts',(85.1556837299412,-4.43265827559063,0.133746655578993));
#10859=CARTESIAN_POINT('Ctrl Pts',(85.1585219777014,-4.43431563427999,0.0657451159004957));
#10860=CARTESIAN_POINT('Ctrl Pts',(85.1613954767413,-4.43439065261444,-0.002200575292715));
#10861=CARTESIAN_POINT('',(86.4138081402417,-4.43299862504029,0.0034914740243378));
#10862=CARTESIAN_POINT('Ctrl Pts',(85.161395476779,-4.43439065261542,-0.00220057618339957));
#10863=CARTESIAN_POINT('Ctrl Pts',(85.1668210831384,-4.43453229869629,-0.130492449284717));
#10864=CARTESIAN_POINT('Ctrl Pts',(85.1723744448677,-4.42903259483677,-0.258660663528824));
#10865=CARTESIAN_POINT('Ctrl Pts',(85.1781567135762,-4.41786942497314,-0.386319371256166));
#10866=CARTESIAN_POINT('Ctrl Pts',(85.1781587489918,-4.41786549542721,-0.386364308380804));
#10867=CARTESIAN_POINT('Ctrl Pts',(85.1781607844358,-4.41786156517934,-0.38640924544292));
#10868=CARTESIAN_POINT('Ctrl Pts',(85.1781628199082,-4.41785763422956,-0.386454182442532));
#10869=CARTESIAN_POINT('Ctrl Pts',(85.1833480825578,-4.40784373897282,-0.50092891047146));
#10870=CARTESIAN_POINT('Ctrl Pts',(85.1887227609473,-4.3932557495046,-0.615153120549821));
#10871=CARTESIAN_POINT('Ctrl Pts',(85.1942099770911,-4.37415521245614,-0.72874247943483));
#10872=CARTESIAN_POINT('Ctrl Pts',(85.1947668349711,-4.37221683709614,-0.740269841930538));
#10873=CARTESIAN_POINT('Ctrl Pts',(85.1953248518495,-4.37023201915508,-0.751790634686316));
#10874=CARTESIAN_POINT('Ctrl Pts',(85.1958839473777,-4.36820084434691,-0.763304435090718));
#10875=CARTESIAN_POINT('Ctrl Pts',(85.2019449060681,-4.34618159006043,-0.888121510356143));
#10876=CARTESIAN_POINT('Ctrl Pts',(85.2081320915797,-4.31871057529508,-1.0121213732573));
#10877=CARTESIAN_POINT('Ctrl Pts',(85.2143539280782,-4.285916042659,-1.1348122127836));
#10878=CARTESIAN_POINT('Ctrl Pts',(85.2205697224126,-4.25315335752385,-1.25738390450353));
#10879=CARTESIAN_POINT('Ctrl Pts',(85.2268197495983,-4.2150778415336,-1.3786492408531));
#10880=CARTESIAN_POINT('Ctrl Pts',(85.2330300798527,-4.17185438485228,-1.49813870943444));
#10881=CARTESIAN_POINT('Ctrl Pts',(85.2377493203303,-4.13900880692024,-1.5889389589675));
#10882=CARTESIAN_POINT('Ctrl Pts',(85.2424455181467,-4.10318943663691,-1.67871648935425));
#10883=CARTESIAN_POINT('Ctrl Pts',(85.247001766108,-4.06433780339744,-1.76720053099714));
#10884=CARTESIAN_POINT('Ctrl Pts',(85.2484370249745,-4.05209919137351,-1.79507379566279));
#10885=CARTESIAN_POINT('Ctrl Pts',(85.2498583965279,-4.03955984543033,-1.82281835246469));
#10886=CARTESIAN_POINT('Ctrl Pts',(85.2512622264202,-4.02671841734579,-1.85042477828402));
#10887=CARTESIAN_POINT('Ctrl Pts',(85.2561732876982,-3.98179485462209,-1.94700118658597));
#10888=CARTESIAN_POINT('Ctrl Pts',(85.2609605908363,-3.93331931290938,-2.04194920990385));
#10889=CARTESIAN_POINT('Ctrl Pts',(85.2657270366361,-3.8816128907154,-2.13511023544705));
#10890=CARTESIAN_POINT('Ctrl Pts',(85.2666461992026,-3.87164181169204,-2.15307543025598));
#10891=CARTESIAN_POINT('Ctrl Pts',(85.2675645861398,-3.86155050396846,-2.17097430434491));
#10892=CARTESIAN_POINT('Ctrl Pts',(85.2684829353718,-3.85134114898564,-2.18880590722276));
#10893=CARTESIAN_POINT('Ctrl Pts',(85.2760314676801,-3.7674235681314,-2.33537588924219));
#10894=CARTESIAN_POINT('Ctrl Pts',(85.2835775343156,-3.67553289452415,-2.47740499943486));
#10895=CARTESIAN_POINT('Ctrl Pts',(85.2911264850738,-3.57622392108629,-2.6140423864284));
#10896=CARTESIAN_POINT('Ctrl Pts',(85.2949378100764,-3.5260846652396,-2.68302806483719));
#10897=CARTESIAN_POINT('Ctrl Pts',(85.2987498543982,-3.47405393029844,-2.75063862976931));
#10898=CARTESIAN_POINT('Ctrl Pts',(85.3025632343123,-3.42020034436607,-2.81676020277861));
#10899=CARTESIAN_POINT('Ctrl Pts',(85.3079619474277,-3.34395825277632,-2.91037044131991));
#10900=CARTESIAN_POINT('Ctrl Pts',(85.3131978229635,-3.26383738623406,-3.00081748735583));
#10901=CARTESIAN_POINT('Ctrl Pts',(85.3181851131229,-3.17998820549575,-3.08759329103002));
#10902=CARTESIAN_POINT('Ctrl Pts',(85.3184495881628,-3.17554169953457,-3.09219499524378));
#10903=CARTESIAN_POINT('Ctrl Pts',(85.3187133641408,-3.17108471831213,-3.09678636750796));
#10904=CARTESIAN_POINT('Ctrl Pts',(85.3189764282693,-3.16661728747347,-3.10136732949371));
#10905=CARTESIAN_POINT('Ctrl Pts',(85.3242057306658,-3.07781176723478,-3.19242967092221));
#10906=CARTESIAN_POINT('Ctrl Pts',(85.3293753673474,-2.98515211965728,-3.27964505079976));
#10907=CARTESIAN_POINT('Ctrl Pts',(85.3345496931392,-2.88899334977489,-3.36265844604907));
#10908=CARTESIAN_POINT('Ctrl Pts',(85.3397271534056,-2.79277632936137,-3.4457221286967));
#10909=CARTESIAN_POINT('Ctrl Pts',(85.3449096712612,-2.69305575273366,-3.52457838493965));
#10910=CARTESIAN_POINT('Ctrl Pts',(85.3501777623043,-2.5902236990862,-3.5988980996034));
#10911=CARTESIAN_POINT('Ctrl Pts',(85.355044675709,-2.4952225504281,-3.66755819157436));
#10912=CARTESIAN_POINT('Ctrl Pts',(85.3599850713443,-2.3975653103509,-3.73234661030828));
#10913=CARTESIAN_POINT('Ctrl Pts',(85.365069857038,-2.29759293697757,-3.79302791604585));
#10914=CARTESIAN_POINT('Ctrl Pts',(85.3654968768067,-2.28919726755768,-3.79812392573082));
#10915=CARTESIAN_POINT('Ctrl Pts',(85.365924914904,-2.2807852577451,-3.80319099720603));
#10916=CARTESIAN_POINT('Ctrl Pts',(85.3663540133271,-2.27235710222539,-3.80822900614889));
#10917=CARTESIAN_POINT('Ctrl Pts',(85.368779374882,-2.22471925674633,-3.83670497470224));
#10918=CARTESIAN_POINT('Ctrl Pts',(85.3712386857147,-2.17656659910718,-3.86425190211056));
#10919=CARTESIAN_POINT('Ctrl Pts',(85.373739654942,-2.12793796450106,-3.89084727575266));
#10920=CARTESIAN_POINT('Ctrl Pts',(85.373741690305,-2.12789838907449,-3.89086891985731));
#10921=CARTESIAN_POINT('Ctrl Pts',(85.3737437256956,-2.12785881333261,-3.8908905633319));
#10922=CARTESIAN_POINT('Ctrl Pts',(85.3737457611138,-2.12781923727546,-3.89091220617643));
#10923=CARTESIAN_POINT('Ctrl Pts',(85.3789310406537,-2.02699822663038,-3.94604790223953));
#10924=CARTESIAN_POINT('Ctrl Pts',(85.384305734269,-1.92384963727594,-3.99723800442516));
#10925=CARTESIAN_POINT('Ctrl Pts',(85.3897929641781,-1.81872744698372,-4.04432064396025));
#10926=CARTESIAN_POINT('Ctrl Pts',(85.3903498198305,-1.80805942562741,-4.04909868942026));
#10927=CARTESIAN_POINT('Ctrl Pts',(85.3909078344512,-1.79737112238041,-4.05383444201256));
#10928=CARTESIAN_POINT('Ctrl Pts',(85.3914669276933,-1.78666293646813,-4.0585277387613));
#10929=CARTESIAN_POINT('Ctrl Pts',(85.397527897637,-1.67057855540134,-4.10940642658978));
#10930=CARTESIAN_POINT('Ctrl Pts',(85.4037150925775,-1.55215160366985,-4.15529490839237));
#10931=CARTESIAN_POINT('Ctrl Pts',(85.4099369371497,-1.43186248333389,-4.19602723197587));
#10932=CARTESIAN_POINT('Ctrl Pts',(85.4161527397556,-1.31169017446999,-4.23672000083767));
#10933=CARTESIAN_POINT('Ctrl Pts',(85.4224027738622,-1.18965940180539,-4.27226698442839));
#10934=CARTESIAN_POINT('Ctrl Pts',(85.4286131101797,-1.06625232866992,-4.30254509279423));
#10935=CARTESIAN_POINT('Ctrl Pts',(85.4333322860001,-0.972476461172645,
-4.32555314092343));
#10936=CARTESIAN_POINT('Ctrl Pts',(85.4380284193404,-0.877902961242614,
-4.3455193671393));
#10937=CARTESIAN_POINT('Ctrl Pts',(85.4425846016461,-0.782724742264051,
-4.36224498294978));
#10938=CARTESIAN_POINT('Ctrl Pts',(85.4440199279464,-0.752740911120412,
-4.36751402502282));
#10939=CARTESIAN_POINT('Ctrl Pts',(85.4454413651113,-0.722697449141261,
-4.37246139612236));
#10940=CARTESIAN_POINT('Ctrl Pts',(85.4468452580771,-0.692601452000684,
-4.37708074842749));
#10941=CARTESIAN_POINT('Ctrl Pts',(85.45175646596,-0.587317287181475,-4.39324052699138));
#10942=CARTESIAN_POINT('Ctrl Pts',(85.4565439239927,-0.481418915382423,
-4.40554118962475));
#10943=CARTESIAN_POINT('Ctrl Pts',(85.461310529251,-0.375216390901607,-4.41416201521859));
#10944=CARTESIAN_POINT('Ctrl Pts',(85.462229543046,-0.35474027010403,-4.41582413264091));
#10945=CARTESIAN_POINT('Ctrl Pts',(85.4631477816843,-0.334252687663094,
-4.41734946659411));
#10946=CARTESIAN_POINT('Ctrl Pts',(85.4640659826311,-0.313755643078922,
-4.418739304735));
#10947=CARTESIAN_POINT('Ctrl Pts',(85.4716145197362,-0.145249280577096,
-4.43016517487088));
#10948=CARTESIAN_POINT('Ctrl Pts',(85.4791605912643,0.0238986476900566,
-4.43243799545198));
#10949=CARTESIAN_POINT('Ctrl Pts',(85.486709546992,0.19267244386593,-4.42554773183715));
#10950=CARTESIAN_POINT('Ctrl Pts',(85.4905208933619,0.27788361990026,-4.42206894852415));
#10951=CARTESIAN_POINT('Ctrl Pts',(85.4943329590767,0.362999100930133,-4.4162535873237));
#10952=CARTESIAN_POINT('Ctrl Pts',(85.4981463604128,0.447886062404757,-4.40809562328451));
#10953=CARTESIAN_POINT('Ctrl Pts',(85.503545883319,0.56808035944329,-4.39654448827011));
#10954=CARTESIAN_POINT('Ctrl Pts',(85.5087824908673,0.687792560931075,-4.38000999976921));
#10955=CARTESIAN_POINT('Ctrl Pts',(85.5137704524758,0.806516216060299,-4.35833571842177));
#10956=CARTESIAN_POINT('Ctrl Pts',(85.5140341877449,0.812793653135961,-4.3571897047047));
#10957=CARTESIAN_POINT('Ctrl Pts',(85.514297227875,0.819068314902127,-4.35602932510892));
#10958=CARTESIAN_POINT('Ctrl Pts',(85.5145595601936,0.825340122617658,-4.35485455774603));
#10959=CARTESIAN_POINT('Ctrl Pts',(85.5197888746267,0.950361907167116,-4.33143682576176));
#10960=CARTESIAN_POINT('Ctrl Pts',(85.5249585253223,1.07431902705324,-4.30267866714438));
#10961=CARTESIAN_POINT('Ctrl Pts',(85.5301328676191,1.1967191926631,-4.26867868766901));
#10962=CARTESIAN_POINT('Ctrl Pts',(85.5353103444421,1.31919350615623,-4.2346581115997));
#10963=CARTESIAN_POINT('Ctrl Pts',(85.5404928813545,1.44010879488779,-4.19538900741506));
#10964=CARTESIAN_POINT('Ctrl Pts',(85.5457609943259,1.55897377497918,-4.1510151994597));
#10965=CARTESIAN_POINT('Ctrl Pts',(85.5506279157658,1.66878662887889,-4.11002066527285));
#10966=CARTESIAN_POINT('Ctrl Pts',(85.5555683215245,1.77685002086513,-4.06466906424268));
#10967=CARTESIAN_POINT('Ctrl Pts',(85.5606531189954,1.88277897280011,-4.01511361269659));
#10968=CARTESIAN_POINT('Ctrl Pts',(85.5610801535461,1.89167516240454,-4.01095181665468));
#10969=CARTESIAN_POINT('Ctrl Pts',(85.5615082065029,1.90055632770093,-4.00676037537719));
#10970=CARTESIAN_POINT('Ctrl Pts',(85.5619373198668,1.90942225726392,-4.00253938196578));
#10971=CARTESIAN_POINT('Ctrl Pts',(85.5643625504949,1.95953005099265,-3.97868348894449));
#10972=CARTESIAN_POINT('Ctrl Pts',(85.5668217269671,2.00915016073338,-3.95388416756324));
#10973=CARTESIAN_POINT('Ctrl Pts',(85.5693225570282,2.05824232611497,-3.92816125207459));
#10974=CARTESIAN_POINT('Ctrl Pts',(85.5693245923688,2.05828228056004,-3.92814031706783));
#10975=CARTESIAN_POINT('Ctrl Pts',(85.569326627737,2.05832223465556,-3.92811938144936));
#10976=CARTESIAN_POINT('Ctrl Pts',(85.5693286631328,2.05836218840156,-3.92809844521918));
#10977=CARTESIAN_POINT('Ctrl Pts',(85.5745139464288,2.1601465653664,-3.87476224128411));
#10978=CARTESIAN_POINT('Ctrl Pts',(85.5798886432999,2.25993783174311,-3.81730137882095));
#10979=CARTESIAN_POINT('Ctrl Pts',(85.5853758757969,2.35740501692618,-3.75592069956012));
#10980=CARTESIAN_POINT('Ctrl Pts',(85.585932727575,2.36729611875289,-3.7496917051799));
#10981=CARTESIAN_POINT('Ctrl Pts',(85.5864907382973,2.37716326893364,-3.74342238349453));
#10982=CARTESIAN_POINT('Ctrl Pts',(85.5870498276185,2.38700611049728,-3.73711297638262));
#10983=CARTESIAN_POINT('Ctrl Pts',(85.5931107958598,2.49371025929989,-3.66871403782689));
#10984=CARTESIAN_POINT('Ctrl Pts',(85.5992979881655,2.59756026347723,-3.59559879567256));
#10985=CARTESIAN_POINT('Ctrl Pts',(85.6055198292351,2.69815166011257,-3.51807504018558));
#10986=CARTESIAN_POINT('Ctrl Pts',(85.6117356282732,2.79864537241397,-3.44062656803964));
#10987=CARTESIAN_POINT('Ctrl Pts',(85.6179856579474,2.89588705574694,-3.35877841704357));
#10988=CARTESIAN_POINT('Ctrl Pts',(85.6241959890656,2.98950694150772,-3.27286360781744));
#10989=CARTESIAN_POINT('Ctrl Pts',(85.6289150054429,3.06064546306844,-3.20757990811144));
#10990=CARTESIAN_POINT('Ctrl Pts',(85.6336109804167,3.12969489087132,-3.13994605065859));
#10991=CARTESIAN_POINT('Ctrl Pts',(85.6381670017238,3.19638283688527,-3.0700123430786));
#10992=CARTESIAN_POINT('Ctrl Pts',(85.639602474662,3.21739431496035,-3.0479782177028));
#10993=CARTESIAN_POINT('Ctrl Pts',(85.6410240543836,3.23817110296885,-3.02571606961333));
#10994=CARTESIAN_POINT('Ctrl Pts',(85.6424280842009,3.25870398038264,-3.00322828479843));
#10995=CARTESIAN_POINT('Ctrl Pts',(85.6473395029352,3.33052977606849,-2.92456405255317));
#10996=CARTESIAN_POINT('Ctrl Pts',(85.6521271844414,3.39948421486727,-2.8432487856963));
#10997=CARTESIAN_POINT('Ctrl Pts',(85.6568940202897,3.4655445640575,-2.75963994234371));
#10998=CARTESIAN_POINT('Ctrl Pts',(85.6578127941348,3.47827722844288,-2.74352493000865));
#10999=CARTESIAN_POINT('Ctrl Pts',(85.6587307935673,3.49090246941608,-2.72732458602232));
#11000=CARTESIAN_POINT('Ctrl Pts',(85.6596487553285,3.50342024982663,-2.71104128631642));
#11001=CARTESIAN_POINT('Ctrl Pts',(85.6671972879246,3.60635577225999,-2.57714135300609));
#11002=CARTESIAN_POINT('Ctrl Pts',(85.6747433549857,3.70202963259365,-2.43763268107927));
#11003=CARTESIAN_POINT('Ctrl Pts',(85.6822923062878,3.78987033601152,-2.29335499308759));
#11004=CARTESIAN_POINT('Ctrl Pts',(85.6861036452507,3.83421963461832,-2.22051160707096));
#11005=CARTESIAN_POINT('Ctrl Pts',(85.689915703567,3.876571329252,-2.14645237246497));
#11006=CARTESIAN_POINT('Ctrl Pts',(85.6937290975101,3.91684676285031,-2.07128448789889));
#11007=CARTESIAN_POINT('Ctrl Pts',(85.6991276026451,3.97386346197388,-1.96487161347015));
#11008=CARTESIAN_POINT('Ctrl Pts',(85.7043632878672,4.0264673221173,-1.85609789432114));
#11009=CARTESIAN_POINT('Ctrl Pts',(85.709350401024,4.07424747782251,-1.74529782869364));
#11010=CARTESIAN_POINT('Ctrl Pts',(85.7096150758851,4.07678325466876,-1.73941747445799));
#11011=CARTESIAN_POINT('Ctrl Pts',(85.7098790506152,4.07930544138933,-1.73353142445952));
#11012=CARTESIAN_POINT('Ctrl Pts',(85.710142312396,4.08181397543319,-1.72763973265671));
#11013=CARTESIAN_POINT('Ctrl Pts',(85.7153716156603,4.13164226887822,-1.61061004802642));
#11014=CARTESIAN_POINT('Ctrl Pts',(85.720541254681,4.17643585074539,-1.49150545855224));
#11015=CARTESIAN_POINT('Ctrl Pts',(85.7257155847687,4.21600383827358,-1.37079032936255));
#11016=CARTESIAN_POINT('Ctrl Pts',(85.7308930493736,4.2555957953849,-1.25000207309453));
#11017=CARTESIAN_POINT('Ctrl Pts',(85.7360755735318,4.28995542827685,-1.12760128145018));
#11018=CARTESIAN_POINT('Ctrl Pts',(85.7413436731781,4.31893004376428,-1.00407655350216));
#11019=CARTESIAN_POINT('Ctrl Pts',(85.7462105841652,4.34569811649109,-0.889958769861308));
#11020=CARTESIAN_POINT('Ctrl Pts',(85.7511509790384,4.36787016929533,-0.774881197198832));
#11021=CARTESIAN_POINT('Ctrl Pts',(85.7562357652567,4.38536026521319,-0.659249172339784));
#11022=CARTESIAN_POINT('Ctrl Pts',(85.7566627968089,4.38682912201197,-0.649538140069354));
#11023=CARTESIAN_POINT('Ctrl Pts',(85.7570908467547,4.3882649776261,-0.639823174911116));
#11024=CARTESIAN_POINT('Ctrl Pts',(85.7575199570946,4.38966779231492,-0.630104504434078));
#11025=CARTESIAN_POINT('Ctrl Pts',(85.7599452465974,4.39759636317974,-0.575175533271245));
#11026=CARTESIAN_POINT('Ctrl Pts',(85.7624044836573,4.40446934448957,-0.520129343393918));
#11027=CARTESIAN_POINT('Ctrl Pts',(85.7649053766406,4.41028092039038,-0.465010440849745));
#11028=CARTESIAN_POINT('Ctrl Pts',(85.7649074120062,4.41028565017342,-0.464965582027521));
#11029=CARTESIAN_POINT('Ctrl Pts',(85.7649094473993,4.41029037925355,-0.464920723157004));
#11030=CARTESIAN_POINT('Ctrl Pts',(85.76491148282,4.4102951076308,-0.464875864238241));
#11031=CARTESIAN_POINT('Ctrl Pts',(85.7700967600214,4.42234074844375,-0.350596822083761));
#11032=CARTESIAN_POINT('Ctrl Pts',(85.7754714514693,4.42984869433835,-0.23568961969063));
#11033=CARTESIAN_POINT('Ctrl Pts',(85.7809586792566,4.43280591622131,-0.120543270618313));
#11034=CARTESIAN_POINT('Ctrl Pts',(85.781515533675,4.43310602077966,-0.108857997885254));
#11035=CARTESIAN_POINT('Ctrl Pts',(85.7820735470579,4.43335928376502,-0.097170299192586));
#11036=CARTESIAN_POINT('Ctrl Pts',(85.7826326390588,4.43356570855561,-0.0854806057341502));
#11037=CARTESIAN_POINT('Ctrl Pts',(85.7886936055249,4.43580350435964,0.0412442265748516));
#11038=CARTESIAN_POINT('Ctrl Pts',(85.7948807970002,4.43253382778728,0.168208678150159));
#11039=CARTESIAN_POINT('Ctrl Pts',(85.8011026380361,4.42378857895326,0.294905493997303));
#11040=CARTESIAN_POINT('Ctrl Pts',(85.8073184370284,4.41505182264975,0.421479274285908));
#11041=CARTESIAN_POINT('Ctrl Pts',(85.8135684674508,4.40085049379849,0.547785995504968));
#11042=CARTESIAN_POINT('Ctrl Pts',(85.8197787999398,4.38125672575128,0.673333287428772));
#11043=CARTESIAN_POINT('Ctrl Pts',(85.8244979183678,4.366367778657,0.768734385511546));
#11044=CARTESIAN_POINT('Ctrl Pts',(85.8291939947648,4.34836456394254,0.863699892015333));
#11045=CARTESIAN_POINT('Ctrl Pts',(85.8337501192069,4.32713793572511,0.957975214470737));
#11046=CARTESIAN_POINT('Ctrl Pts',(85.835185496382,4.32045062548277,0.987676037559452));
#11047=CARTESIAN_POINT('Ctrl Pts',(85.8366069829929,4.31344347265241,1.01730798006811));
#11048=CARTESIAN_POINT('Ctrl Pts',(85.8380109234052,4.30611335181733,1.0468620476212));
#11049=CARTESIAN_POINT('Ctrl Pts',(85.8429221924765,4.28047109846406,1.1502481861128));
#11050=CARTESIAN_POINT('Ctrl Pts',(85.8477097154777,4.2510308295093,1.25271461048536));
#11051=CARTESIAN_POINT('Ctrl Pts',(85.8524763878623,4.21807742235806,1.35404423792655));
#11052=CARTESIAN_POINT('Ctrl Pts',(85.8533953276866,4.21172452126983,1.37357900401271));
#11053=CARTESIAN_POINT('Ctrl Pts',(85.854313492581,4.20524099771781,1.39307166603808));
#11054=CARTESIAN_POINT('Ctrl Pts',(85.8552316197899,4.19862880964729,1.41252087509184));
#11055=CARTESIAN_POINT('Ctrl Pts',(85.8627801536881,4.14426561758675,1.57242574711574));
#11056=CARTESIAN_POINT('Ctrl Pts',(85.8703262220055,4.08120854121988,1.72939699634938));
#11057=CARTESIAN_POINT('Ctrl Pts',(85.877875174523,4.0098395593787,1.88249343527474));
#11058=CARTESIAN_POINT('Ctrl Pts',(85.8816865123719,3.97380657319945,1.95978922576486));
#11059=CARTESIAN_POINT('Ctrl Pts',(85.8854985695634,3.93565417893046,2.03609667767147));
#11060=CARTESIAN_POINT('Ctrl Pts',(85.8893119623718,3.89542797929008,2.11129089568053));
#11061=CARTESIAN_POINT('Ctrl Pts',(85.8947108243299,3.83847719822097,2.21774811723718));
#11062=CARTESIAN_POINT('Ctrl Pts',(85.8999468333592,3.77711441206833,2.32184149220192));
#11063=CARTESIAN_POINT('Ctrl Pts',(85.9049342448572,3.71139024578863,2.42304354572274));
#11064=CARTESIAN_POINT('Ctrl Pts',(85.9051985884318,3.70790672311085,2.42840747300297));
#11065=CARTESIAN_POINT('Ctrl Pts',(85.9054622336392,3.70441095599939,2.43376326843933));
#11066=CARTESIAN_POINT('Ctrl Pts',(85.9057251677122,3.70090295464595,2.43911085036852));
#11067=CARTESIAN_POINT('Ctrl Pts',(85.9109544741529,3.63113484182334,2.5454650565884));
#11068=CARTESIAN_POINT('Ctrl Pts',(85.9161241161494,3.55684849920931,2.64877966545965));
#11069=CARTESIAN_POINT('Ctrl Pts',(85.9212984489043,3.47832454955109,2.74863835731252));
#11070=CARTESIAN_POINT('Ctrl Pts',(85.9264759161689,3.39975303161816,2.84855754161014));
#11071=CARTESIAN_POINT('Ctrl Pts',(85.9316584426769,3.31693851450593,2.94501631460888));
#11072=CARTESIAN_POINT('Ctrl Pts',(85.9369265442928,3.23020296281884,3.03761670264264));
#11073=CARTESIAN_POINT('Ctrl Pts',(85.9417934590288,3.15007266818491,3.12316520302148));
#11074=CARTESIAN_POINT('Ctrl Pts',(85.946733857384,3.06659539521238,3.20542092856662));
#11075=CARTESIAN_POINT('Ctrl Pts',(85.9518186468861,2.98006082830787,3.28408762527598));
#11076=CARTESIAN_POINT('Ctrl Pts',(85.9522456765139,2.97279350212243,3.29069419378807));
#11077=CARTESIAN_POINT('Ctrl Pts',(85.9526737245234,2.96550460592939,3.29727547871599));
#11078=CARTESIAN_POINT('Ctrl Pts',(85.9531028329146,2.95819430708086,3.30383132081557));
#11079=CARTESIAN_POINT('Ctrl Pts',(85.9555281218844,2.91687703730188,3.34088445670909));
#11080=CARTESIAN_POINT('Ctrl Pts',(85.9579873583054,2.87487695503373,3.37712409721206));
#11081=CARTESIAN_POINT('Ctrl Pts',(85.960488250536,2.83222787467982,3.41252072634323));
#11082=CARTESIAN_POINT('Ctrl Pts',(85.9604902858933,2.83219316462023,3.41254953397744));
#11083=CARTESIAN_POINT('Ctrl Pts',(85.9604923212782,2.83215845413073,3.41257834105347));
#11084=CARTESIAN_POINT('Ctrl Pts',(85.9604943566907,2.83212374321137,3.41260714757129));
#11085=CARTESIAN_POINT('Ctrl Pts',(85.965679636304,2.74369654677406,3.48599268899348));
#11086=CARTESIAN_POINT('Ctrl Pts',(85.9710543299192,2.65223070046746,3.55595012650461));
#11087=CARTESIAN_POINT('Ctrl Pts',(85.9765415596465,2.55804272712359,3.62225293234593));
#11088=CARTESIAN_POINT('Ctrl Pts',(85.9770984135624,2.54848436262974,3.62898146001987));
#11089=CARTESIAN_POINT('Ctrl Pts',(85.9776564264377,2.53889800842257,3.63567235013124));
#11090=CARTESIAN_POINT('Ctrl Pts',(85.978215517926,2.5292840252238,3.64232536642138));
#11091=CARTESIAN_POINT('Ctrl Pts',(85.9842764857699,2.42506129201463,3.71444901460207));
#11092=CARTESIAN_POINT('Ctrl Pts',(85.9904636783336,2.31758557961003,3.78212206470979));
#11093=CARTESIAN_POINT('Ctrl Pts',(85.9966855202337,2.2072967246636,3.84508982248233));
#11094=CARTESIAN_POINT('Ctrl Pts',(86.0029013201123,2.0971149710608,3.9079964323586));
#11095=CARTESIAN_POINT('Ctrl Pts',(86.0091513511975,1.9841256936657,3.96620722381679));
#11096=CARTESIAN_POINT('Ctrl Pts',(86.0153616841953,1.86877864856529,4.01950923836368));
#11097=CARTESIAN_POINT('Ctrl Pts',(86.0200807854772,1.7811288577099,4.06001231690496));
#11098=CARTESIAN_POINT('Ctrl Pts',(86.0247768448104,1.69211491276211,4.09768213792665));
#11099=CARTESIAN_POINT('Ctrl Pts',(86.0293329518913,1.6018881742771,4.13228671122897));
#11100=CARTESIAN_POINT('Ctrl Pts',(86.0307683458769,1.57346238983785,4.14318882470243));
#11101=CARTESIAN_POINT('Ctrl Pts',(86.0321898488375,1.54491659302445,4.1537865598859));
#11102=CARTESIAN_POINT('Ctrl Pts',(86.0335938049568,1.51625653650733,4.16407232853264));
#11103=CARTESIAN_POINT('Ctrl Pts',(86.038505104712,1.41599832570361,4.2000538612504));
#11104=CARTESIAN_POINT('Ctrl Pts',(86.0432926601702,1.31439973612451,4.23236462215131));
#11105=CARTESIAN_POINT('Ctrl Pts',(86.048059365997,1.21179938123318,4.2611213315272));
#11106=CARTESIAN_POINT('Ctrl Pts',(86.048978273268,1.19202047824482,4.26666493969125));
#11107=CARTESIAN_POINT('Ctrl Pts',(86.0498964057115,1.17220419572373,4.27207650595775));
#11108=CARTESIAN_POINT('Ctrl Pts',(86.0508145004724,1.15235274158155,4.27735691175687));
#11109=CARTESIAN_POINT('Ctrl Pts',(86.0583630347551,0.989134968708486,4.32077217334051));
#11110=CARTESIAN_POINT('Ctrl Pts',(86.0659091034719,0.823538392579329,4.35532565885359));
#11111=CARTESIAN_POINT('Ctrl Pts',(86.0734580564011,0.656558076026867,4.38081342825425));
#11112=CARTESIAN_POINT('Ctrl Pts',(86.0772693966408,0.572252503361662,4.3936817772887));
#11113=CARTESIAN_POINT('Ctrl Pts',(86.081081456227,0.48759436535417,4.40423832719151));
#11114=CARTESIAN_POINT('Ctrl Pts',(86.084894851434,0.402712887044264,4.41245178263173));
#11115=CARTESIAN_POINT('Ctrl Pts',(86.0902937643092,0.282539739172888,4.42408019456336));
#11116=CARTESIAN_POINT('Ctrl Pts',(86.0955298192384,0.161887641220141,4.43072612255225));
#11117=CARTESIAN_POINT('Ctrl Pts',(86.1005172727054,0.0412236526647988,
4.43213924387147));
#11118=CARTESIAN_POINT('Ctrl Pts',(86.1007815702943,0.0348293671928713,
4.43221412869195));
#11119=CARTESIAN_POINT('Ctrl Pts',(86.1010451697595,0.0284350604571021,
4.43227431986939));
#11120=CARTESIAN_POINT('Ctrl Pts',(86.1013080583413,0.0220408060320593,
4.43231978062816));
#11121=CARTESIAN_POINT('Ctrl Pts',(86.1065373657472,-0.10515194534687,4.43322407354545));
#11122=CARTESIAN_POINT('Ctrl Pts',(86.1117070089402,-0.232320156652302,
4.42868291170422));
#11123=CARTESIAN_POINT('Ctrl Pts',(86.1168813431883,-0.358961768078289,
4.41869901193295));
#11124=CARTESIAN_POINT('Ctrl Pts',(86.1220588119524,-0.485680096647177,
4.40870906410009));
#11125=CARTESIAN_POINT('Ctrl Pts',(86.1272413402577,-0.611871074700732,
4.39326939905119));
#11126=CARTESIAN_POINT('Ctrl Pts',(86.1325094440154,-0.737024988835311,
4.37242731107123));
#11127=CARTESIAN_POINT('Ctrl Pts',(86.1373763592312,-0.852647899283205,
4.3531724368732));
#11128=CARTESIAN_POINT('Ctrl Pts',(86.1423167583156,-0.967386181203723,
4.32930648297475));
#11129=CARTESIAN_POINT('Ctrl Pts',(86.1474015487429,-1.08083267256491,4.30090627666888));
#11130=CARTESIAN_POINT('Ctrl Pts',(86.1478285801421,-1.09036014761645,4.29852116758537));
#11131=CARTESIAN_POINT('Ctrl Pts',(86.1482566299326,-1.09987854026065,4.29610408895486));
#11132=CARTESIAN_POINT('Ctrl Pts',(86.1486857401145,-1.10938762518145,4.2936550917611));
#11133=CARTESIAN_POINT('Ctrl Pts',(86.1511110151534,-1.16313173862802,4.27981367756529));
#11134=CARTESIAN_POINT('Ctrl Pts',(86.1535702372874,-1.21657742361984,4.26495298866421));
#11135=CARTESIAN_POINT('Ctrl Pts',(86.156071114729,-1.26968136899565,4.24908480116176));
#11136=CARTESIAN_POINT('Ctrl Pts',(86.1560731500848,-1.26972458799573,4.24907188673155));
#11137=CARTESIAN_POINT('Ctrl Pts',(86.1560751854682,-1.26976780676959,4.24905897163408));
#11138=CARTESIAN_POINT('Ctrl Pts',(86.1560772208791,-1.26981102531726,4.24904605586937));
#11139=CARTESIAN_POINT('Ctrl Pts',(86.1612625006485,-1.37991176874156,4.21614269903718));
#11140=CARTESIAN_POINT('Ctrl Pts',(86.1666371943902,-1.48884431124347,4.17880982876281));
#11141=CARTESIAN_POINT('Ctrl Pts',(86.1721244241947,-1.59624463818395,4.13718526681709));
#11142=CARTESIAN_POINT('Ctrl Pts',(86.1726812777381,-1.60714380857506,4.13296113448877));
#11143=CARTESIAN_POINT('Ctrl Pts',(86.1732392902386,-1.61802717472683,4.12869284075756));
#11144=CARTESIAN_POINT('Ctrl Pts',(86.1737983813502,-1.62889434002148,4.12438055483306));
#11145=CARTESIAN_POINT('Ctrl Pts',(86.1798593488598,-1.74670257271797,4.07763213701908));
#11146=CARTESIAN_POINT('Ctrl Pts',(86.1860465410172,-1.86261049357883,4.02570892503116));
#11147=CARTESIAN_POINT('Ctrl Pts',(86.1922683824398,-1.97616227711835,3.96883574864683));
#11148=CARTESIAN_POINT('Ctrl Pts',(86.1984841818319,-2.089603790515,3.91201780180702));
#11149=CARTESIAN_POINT('Ctrl Pts',(86.2047342123595,-2.2006939357567,3.85025981935736));
#11150=CARTESIAN_POINT('Ctrl Pts',(86.2109445447325,-2.30900612111424,3.78381802623826));
#11151=CARTESIAN_POINT('Ctrl Pts',(86.2156636310042,-2.391310016668,3.73333046213615));
#11152=CARTESIAN_POINT('Ctrl Pts',(86.2203596754306,-2.47201235957494,3.68013676304226));
#11153=CARTESIAN_POINT('Ctrl Pts',(86.2249157673569,-2.5508361628422,3.6242342682063));
#11154=CARTESIAN_POINT('Ctrl Pts',(86.2263511750147,-2.57566979057701,3.60662205351151));
#11155=CARTESIAN_POINT('Ctrl Pts',(86.2277726912659,-2.60031664342907,3.58874119683137));
#11156=CARTESIAN_POINT('Ctrl Pts',(86.2291766601421,-2.62476721643445,3.57059227841078));
#11157=CARTESIAN_POINT('Ctrl Pts',(86.234087978986,-2.71029942585828,3.50710431472075));
#11158=CARTESIAN_POINT('Ctrl Pts',(86.2388755546824,-2.79351987259517,3.44046560918281));
#11159=CARTESIAN_POINT('Ctrl Pts',(86.2436422813972,-2.87433795050354,3.37102268006853));
#11160=CARTESIAN_POINT('Ctrl Pts',(86.2445611666889,-2.88991730873579,3.35763611734187));
#11161=CARTESIAN_POINT('Ctrl Pts',(86.2454792772209,-2.90540750752077,3.34414524224346));
#11162=CARTESIAN_POINT('Ctrl Pts',(86.2463973500722,-2.92080805627222,3.330552380765));
#11163=CARTESIAN_POINT('Ctrl Pts',(86.2539458838062,-3.04743369563578,3.21878981936083));
#11164=CARTESIAN_POINT('Ctrl Pts',(86.2614919519773,-3.168003258343,3.10013424064003));
#11165=CARTESIAN_POINT('Ctrl Pts',(86.2690409043641,-3.28179531821978,2.97530068696945));
#11166=CARTESIAN_POINT('Ctrl Pts',(86.2728522435859,-3.33924701730458,2.91227432318858));
#11167=CARTESIAN_POINT('Ctrl Pts',(86.2766643021547,-3.39497025934898,2.84767279345664));
#11168=CARTESIAN_POINT('Ctrl Pts',(86.2804776963446,-3.44886735218826,2.78158629048153));
#11169=CARTESIAN_POINT('Ctrl Pts',(86.285876501233,-3.52517204921117,2.68802446142602));
#11170=CARTESIAN_POINT('Ctrl Pts',(86.2911124583068,-3.5975959138434,2.59130168136755));
#11171=CARTESIAN_POINT('Ctrl Pts',(86.296099821761,-3.66567168304665,2.49166783635782));
#11172=CARTESIAN_POINT('Ctrl Pts',(86.2963642188998,-3.66928061164577,2.48638590657717));
#11173=CARTESIAN_POINT('Ctrl Pts',(86.2966279173858,-3.67287731448961,2.48109580621379));
#11174=CARTESIAN_POINT('Ctrl Pts',(86.2968909044437,-3.67646172009797,2.47579757615328));
#11175=CARTESIAN_POINT('Ctrl Pts',(86.3021202105473,-3.74773501497731,2.37044613027905));
#11176=CARTESIAN_POINT('Ctrl Pts',(86.3072898523626,-3.81446286795207,2.2620959309462));
#11177=CARTESIAN_POINT('Ctrl Pts',(86.3124641851487,-3.87636917814906,2.15116631049352));
#11178=CARTESIAN_POINT('Ctrl Pts',(86.3176416524492,-3.93831299003523,2.04016949094377));
#11179=CARTESIAN_POINT('Ctrl Pts',(86.3228241792064,-3.995429034636,1.92659000537864));
#11180=CARTESIAN_POINT('Ctrl Pts',(86.3280922813235,-4.04747406603953,1.81087827115258));
#11181=CARTESIAN_POINT('Ctrl Pts',(86.3329591953664,-4.09555564998932,1.70397847086176));
#11182=CARTESIAN_POINT('Ctrl Pts',(86.3378995932091,-4.13930931086627,1.59525831342402));
#11183=CARTESIAN_POINT('Ctrl Pts',(86.3429843823386,-4.17857323934634,1.4850992448709));
#11184=CARTESIAN_POINT('Ctrl Pts',(86.3434114132466,-4.18187070372523,1.47584786278491));
#11185=CARTESIAN_POINT('Ctrl Pts',(86.3438394625435,-4.18513652669808,1.4665863141237));
#11186=CARTESIAN_POINT('Ctrl Pts',(86.3442685722297,-4.18837062577084,1.45731481466741));
#11187=CARTESIAN_POINT('Ctrl Pts',(86.3466938550415,-4.20664941356103,1.40491327493541));
#11188=CARTESIAN_POINT('Ctrl Pts',(86.3491530851702,-4.22391446915204,1.35219496580757));
#11189=CARTESIAN_POINT('Ctrl Pts',(86.35165397091,-4.24015157932302,1.29920246144712));
#11190=CARTESIAN_POINT('Ctrl Pts',(86.3516560062688,-4.24016479397886,1.29915933322416));
#11191=CARTESIAN_POINT('Ctrl Pts',(86.3516580416552,-4.24017800795399,1.29911620481949));
#11192=CARTESIAN_POINT('Ctrl Pts',(86.3516600770691,-4.24019122124841,1.29907307623315));
#11193=CARTESIAN_POINT('Ctrl Pts',(86.3571928480507,-4.27610830445762,1.18183864739698));
#11194=CARTESIAN_POINT('Ctrl Pts',(86.3629366538387,-4.30705822960612,1.06303512474668));
#11195=CARTESIAN_POINT('Ctrl Pts',(86.368801100108,-4.33297671141248,0.943052260128244));
#11196=CARTESIAN_POINT('Ctrl Pts',(86.370235611573,-4.33931667218611,0.913703062097574));
#11197=CARTESIAN_POINT('Ctrl Pts',(86.3716773415401,-4.34535556605231,0.884283542759871));
#11198=CARTESIAN_POINT('Ctrl Pts',(86.3731249669716,-4.35109244908456,0.854799881287111));
#11199=CARTESIAN_POINT('Ctrl Pts',(86.3792815320168,-4.3754906758473,0.729409655555755));
#11200=CARTESIAN_POINT('Ctrl Pts',(86.3855440365689,-4.3944270396494,0.602853429710152));
#11201=CARTESIAN_POINT('Ctrl Pts',(86.3918267665125,-4.40785559256641,0.475559283027399));
#11202=CARTESIAN_POINT('Ctrl Pts',(86.3929787870132,-4.41031789293486,0.452218240532605));
#11203=CARTESIAN_POINT('Ctrl Pts',(86.3941314875322,-4.41259496550383,0.428852521820395));
#11204=CARTESIAN_POINT('Ctrl Pts',(86.395284339639,-4.414686474794,0.405464948733126));
#11205=CARTESIAN_POINT('Ctrl Pts',(86.4018609031946,-4.4266177049082,0.272048129774276));
#11206=CARTESIAN_POINT('Ctrl Pts',(86.4084425476444,-4.43251295826403,0.137913142053602));
#11207=CARTESIAN_POINT('Ctrl Pts',(86.4149558832995,-4.43233551419456,0.00354868648530903));
#11208=CARTESIAN_POINT('',(87.6638081402417,-4.43299865229463,-0.00345669697483381));
#11209=CARTESIAN_POINT('Ctrl Pts',(86.4138081402417,-4.43299862504029,0.0034914740243378));
#11210=CARTESIAN_POINT('Ctrl Pts',(86.4194928266304,-4.43309858561255,-0.123424858811329));
#11211=CARTESIAN_POINT('Ctrl Pts',(86.4251775130191,-4.42774379894671,-0.250430731327767));
#11212=CARTESIAN_POINT('Ctrl Pts',(86.4308621994077,-4.41693837642756,-0.37702039578981));
#11213=CARTESIAN_POINT('Ctrl Pts',(86.4365232587161,-4.40617786414065,-0.503083919675518));
#11214=CARTESIAN_POINT('Ctrl Pts',(86.4421843180244,-4.39001197941783,-0.628734283778743));
#11215=CARTESIAN_POINT('Ctrl Pts',(86.4478453773327,-4.36849692902415,-0.753474340045224));
#11216=CARTESIAN_POINT('Ctrl Pts',(86.4535059960479,-4.34698355311981,-0.878204687949842));
#11217=CARTESIAN_POINT('Ctrl Pts',(86.4591666147631,-4.32012190817094,-1.00202447095209));
#11218=CARTESIAN_POINT('Ctrl Pts',(86.4648272334783,-4.2880196406845,-1.12444500136909));
#11219=CARTESIAN_POINT('Ctrl Pts',(86.470488723121,-4.25591243402978,-1.24688436707869));
#11220=CARTESIAN_POINT('Ctrl Pts',(86.4761502127638,-4.21856310384608,-1.36792366142097));
#11221=CARTESIAN_POINT('Ctrl Pts',(86.4818117024065,-4.17612950022084,-1.48708822784166));
#11222=CARTESIAN_POINT('Ctrl Pts',(86.4875141116701,-4.13338919869751,-1.60711408151878));
#11223=CARTESIAN_POINT('Ctrl Pts',(86.4932165209337,-4.08549096873137,-1.72523760539112));
#11224=CARTESIAN_POINT('Ctrl Pts',(86.4989189301973,-4.03264543254052,-1.84099424643591));
#11225=CARTESIAN_POINT('Ctrl Pts',(86.5045890089907,-3.98009951024224,-1.95609459178733));
#11226=CARTESIAN_POINT('Ctrl Pts',(86.510259087784,-3.92266247378685,-2.06885448967915));
#11227=CARTESIAN_POINT('Ctrl Pts',(86.5159291665774,-3.86058712465216,-2.17884282429227));
#11228=CARTESIAN_POINT('Ctrl Pts',(86.5216477410761,-3.79798085029511,-2.289771879849));
#11229=CARTESIAN_POINT('Ctrl Pts',(86.5273663155749,-3.73065677649181,-2.39788138712079));
#11230=CARTESIAN_POINT('Ctrl Pts',(86.5330848900736,-3.65891769727892,-2.50276053279956));
#11231=CARTESIAN_POINT('Ctrl Pts',(86.5388034645724,-3.58717861806602,-2.60763967847833));
#11232=CARTESIAN_POINT('Ctrl Pts',(86.5445220390712,-3.51102483123275,-2.70928816745404));
#11233=CARTESIAN_POINT('Ctrl Pts',(86.5502406135699,-3.43079859236735,-2.80733147643989));
#11234=CARTESIAN_POINT('Ctrl Pts',(86.5559517856266,-3.35067620282369,-2.90524787269393));
#11235=CARTESIAN_POINT('Ctrl Pts',(86.5616629576833,-3.26623502734388,-2.99988249200717));
#11236=CARTESIAN_POINT('Ctrl Pts',(86.56737412974,-3.1777737687688,-3.09083206831509));
#11237=CARTESIAN_POINT('Ctrl Pts',(86.5730783351364,-3.08942041791224,-3.18167070157926));
#11238=CARTESIAN_POINT('Ctrl Pts',(86.5787825405327,-2.99705701594037,-3.26883295112687));
#11239=CARTESIAN_POINT('Ctrl Pts',(86.584486745929,-2.90102301052981,-3.35194786540253));
#11240=CARTESIAN_POINT('Ctrl Pts',(86.5901854119731,-2.80508226371378,-3.43498206680926));
#11241=CARTESIAN_POINT('Ctrl Pts',(86.5958840780173,-2.70547830646356,-3.5139764940675));
#11242=CARTESIAN_POINT('Ctrl Pts',(86.6015827440614,-2.60258764965247,-3.58859673491971));
#11243=CARTESIAN_POINT('Ctrl Pts',(86.6072772930777,-2.49977132667532,-3.66316306603158));
#11244=CARTESIAN_POINT('Ctrl Pts',(86.612971842094,-2.39367335211702,-3.73336126685212));
#11245=CARTESIAN_POINT('Ctrl Pts',(86.6186663911103,-2.2847031770432,-3.79889726010176));
#11246=CARTESIAN_POINT('Ctrl Pts',(86.6243588077042,-2.17577380773753,-3.86440871226442));
#11247=CARTESIAN_POINT('Ctrl Pts',(86.6300512242981,-2.06397471796631,-3.92526122279219));
#11248=CARTESIAN_POINT('Ctrl Pts',(86.635743640892,-1.9497439167623,-3.98120429757736));
#11249=CARTESIAN_POINT('Ctrl Pts',(86.6414351262668,-1.83553180250814,-4.03713822066769));
#11250=CARTESIAN_POINT('Ctrl Pts',(86.6471266116415,-1.7188891264319,-4.08816413001825));
#11251=CARTESIAN_POINT('Ctrl Pts',(86.6528180970163,-1.60027756815729,-4.13407797517809));
#11252=CARTESIAN_POINT('Ctrl Pts',(86.6585099332263,-1.48165869841492,-4.17999465056463));
#11253=CARTESIAN_POINT('Ctrl Pts',(86.6642017694363,-1.36107107734571,-4.22079849092538));
#11254=CARTESIAN_POINT('Ctrl Pts',(86.6698936056463,-1.23899489838011,-4.25633417881962));
#11255=CARTESIAN_POINT('Ctrl Pts',(86.6755870746831,-1.11688369921225,-4.29188006089742));
#11256=CARTESIAN_POINT('Ctrl Pts',(86.6812805437199,-0.993283475745765,
-4.32215467252359));
#11257=CARTESIAN_POINT('Ctrl Pts',(86.6869740127567,-0.868687556312043,
-4.34705313166386));
#11258=CARTESIAN_POINT('Ctrl Pts',(86.6926735353827,-0.743959160086927,
-4.3719780641268));
#11259=CARTESIAN_POINT('Ctrl Pts',(86.6983730580086,-0.618233345895329,
-4.39151535277929));
#11260=CARTESIAN_POINT('Ctrl Pts',(86.7040725806346,-0.492011872695479,
-4.40561157129481));
#11261=CARTESIAN_POINT('Ctrl Pts',(86.7097755559243,-0.36571393689858,-4.41971632903466));
#11262=CARTESIAN_POINT('Ctrl Pts',(86.715478531214,-0.238920141515387,-4.42837342327373));
#11263=CARTESIAN_POINT('Ctrl Pts',(86.7211815065037,-0.112134030461784,
-4.43158154152808));
#11264=CARTESIAN_POINT('Ctrl Pts',(86.7268926498785,0.0148336699714674,
-4.43479425460909));
#11265=CARTESIAN_POINT('Ctrl Pts',(86.7326037932533,0.141793265893701,-4.43254241543301));
#11266=CARTESIAN_POINT('Ctrl Pts',(86.7383149366281,0.268244173801696,-4.42487672859046));
#11267=CARTESIAN_POINT('Ctrl Pts',(86.7408177826528,0.323659899062344,-4.42151732530085));
#11268=CARTESIAN_POINT('Ctrl Pts',(86.7433206286776,0.378978031091081,-4.41711884181208));
#11269=CARTESIAN_POINT('Ctrl Pts',(86.7458234747023,0.434157045701389,-4.41168864038112));
#11270=CARTESIAN_POINT('Ctrl Pts',(86.7515346465291,0.560068440393015,-4.39929762106958));
#11271=CARTESIAN_POINT('Ctrl Pts',(86.7572458183559,0.685643168840897,-4.38149285785934));
#11272=CARTESIAN_POINT('Ctrl Pts',(86.7629569901827,0.810380010705975,-4.35829935161046));
#11273=CARTESIAN_POINT('Ctrl Pts',(86.7686611953483,0.934964694775035,-4.33513413750639));
#11274=CARTESIAN_POINT('Ctrl Pts',(86.7743654005139,1.05871313659917,-4.30659333027187));
#11275=CARTESIAN_POINT('Ctrl Pts',(86.7800696056794,1.18112841818454,-4.27275375604035));
#11276=CARTESIAN_POINT('Ctrl Pts',(86.7857682714923,1.30342482230871,-4.23894704341418));
#11277=CARTESIAN_POINT('Ctrl Pts',(86.7914669373051,1.42439025976567,-4.19985190861399));
#11278=CARTESIAN_POINT('Ctrl Pts',(86.7971656031179,1.54353767212426,-4.15559628148996));
#11279=CARTESIAN_POINT('Ctrl Pts',(86.8028601519027,1.66259900587129,-4.11137262705306));
#11280=CARTESIAN_POINT('Ctrl Pts',(86.8085547006874,1.77984455576229,-4.06199603909253));
#11281=CARTESIAN_POINT('Ctrl Pts',(86.8142492494722,1.89480256774256,-4.00764422438871));
#11282=CARTESIAN_POINT('Ctrl Pts',(86.819941665835,2.00971753171319,-3.95331276265902));
#11283=CARTESIAN_POINT('Ctrl Pts',(86.8256340821978,2.12234630072409,-3.89400994890669));
#11284=CARTESIAN_POINT('Ctrl Pts',(86.8313264985605,2.2322375580017,-3.82996142077784));
#11285=CARTESIAN_POINT('Ctrl Pts',(86.8370179837046,2.34211083823889,-3.7659233703067));
#11286=CARTESIAN_POINT('Ctrl Pts',(86.8427094688486,2.44924715277715,-3.69714135060679));
#11287=CARTESIAN_POINT('Ctrl Pts',(86.8484009539927,2.55322071244419,-3.62388644876546));
#11288=CARTESIAN_POINT('Ctrl Pts',(86.8540927899725,2.65720068127262,-3.55062703132912));
#11289=CARTESIAN_POINT('Ctrl Pts',(86.8597846259523,2.75801718116145,-3.47289441328324));
#11290=CARTESIAN_POINT('Ctrl Pts',(86.8654764619321,2.8552747149209,-3.39100210886596));
#11291=CARTESIAN_POINT('Ctrl Pts',(86.8711699307396,2.9525601491309,-3.30908631185019));
#11292=CARTESIAN_POINT('Ctrl Pts',(86.8768633995471,3.04628428094089,-3.22300871157583));
#11293=CARTESIAN_POINT('Ctrl Pts',(86.8825568683545,3.13608630419801,-3.13312171685392));
#11294=CARTESIAN_POINT('Ctrl Pts',(86.8882563907536,3.2259838096287,-3.04313914961238));
#11295=CARTESIAN_POINT('Ctrl Pts',(86.8939559131527,3.31195059789399,-2.94933938358401));
#11296=CARTESIAN_POINT('Ctrl Pts',(86.8996554355518,3.39366401123373,-2.8521103728392));
#11297=CARTESIAN_POINT('Ctrl Pts',(86.9053584106158,3.47542692504215,-2.75482246256489));
#11298=CARTESIAN_POINT('Ctrl Pts',(86.9110613856797,3.55293108797739,-2.65410148502395));
#11299=CARTESIAN_POINT('Ctrl Pts',(86.9167643607437,3.62589622301142,-2.55036577375708));
#11300=CARTESIAN_POINT('Ctrl Pts',(86.9224755038964,3.69896586239475,-2.44648148696847));
#11301=CARTESIAN_POINT('Ctrl Pts',(86.9281866470491,3.76748327796095,-2.33957418003041));
#11302=CARTESIAN_POINT('Ctrl Pts',(86.9338977902018,3.83121312390325,-2.23008856309149));
#11303=CARTESIAN_POINT('Ctrl Pts',(86.936400638746,3.85914205999862,-2.18210764059535));
#11304=CARTESIAN_POINT('Ctrl Pts',(86.9389034872903,3.8861521373543,-2.13363182912283));
#11305=CARTESIAN_POINT('Ctrl Pts',(86.9414063358346,3.91222646030594,-2.08469976813979));
#11306=CARTESIAN_POINT('Ctrl Pts',(86.9471175075987,3.97172464182866,-1.97304322955773));
#11307=CARTESIAN_POINT('Ctrl Pts',(86.9528286793629,4.02653071554339,-1.85866527777414));
#11308=CARTESIAN_POINT('Ctrl Pts',(86.958539851127,4.07638759126769,-1.74199690176498));
#11309=CARTESIAN_POINT('Ctrl Pts',(86.9642440562285,4.12618365004387,-1.62547084142377));
#11310=CARTESIAN_POINT('Ctrl Pts',(86.9699482613299,4.17104236618554,-1.50666027923305));
#11311=CARTESIAN_POINT('Ctrl Pts',(86.9756524664314,4.21075216512944,-1.38602135764847));
#11312=CARTESIAN_POINT('Ctrl Pts',(86.9813511321787,4.25042340188367,-1.26549958853258));
#11313=CARTESIAN_POINT('Ctrl Pts',(86.987049797926,4.28495554685416,-1.14315337006245));
#11314=CARTESIAN_POINT('Ctrl Pts',(86.9927484636733,4.3141850217428,-1.01945897326479));
#11315=CARTESIAN_POINT('Ctrl Pts',(86.9984430123912,4.34339337965205,-0.895853940098765));
#11316=CARTESIAN_POINT('Ctrl Pts',(87.0041375611091,4.36730660072948,-0.770903054289988));
#11317=CARTESIAN_POINT('Ctrl Pts',(87.009832109827,4.38581101758013,-0.645097448508964));
#11318=CARTESIAN_POINT('Ctrl Pts',(87.0155245261213,4.40430850512718,-0.519338952844576));
#11319=CARTESIAN_POINT('Ctrl Pts',(87.0212169424155,4.41740115767103,-0.392726767871859));
#11320=CARTESIAN_POINT('Ctrl Pts',(87.0269093587097,4.42502652826775,-0.265761592647671));
#11321=CARTESIAN_POINT('Ctrl Pts',(87.0326008437842,4.43265065143359,-0.138817187598398));
#11322=CARTESIAN_POINT('Ctrl Pts',(87.0382923288586,4.434809247751,-0.0115203054542955));
#11323=CARTESIAN_POINT('Ctrl Pts',(87.0439838139331,4.43149184790243,0.115624400427719));
#11324=CARTESIAN_POINT('Ctrl Pts',(87.0496756498424,4.4281742435625,0.242776943771324));
#11325=CARTESIAN_POINT('Ctrl Pts',(87.0553674857517,4.41937998211374,0.369776893159533));
#11326=CARTESIAN_POINT('Ctrl Pts',(87.061059321661,4.4051506982053,0.496121281645249));
#11327=CARTESIAN_POINT('Ctrl Pts',(87.066752790397,4.39091733231779,0.622501914762336));
#11328=CARTESIAN_POINT('Ctrl Pts',(87.0724462591331,4.371245886927,0.74822621636346));
#11329=CARTESIAN_POINT('Ctrl Pts',(87.0781397278691,4.34622959976409,0.872798525511165));
#11330=CARTESIAN_POINT('Ctrl Pts',(87.083839250196,4.32118671398931,0.997503286388406));
#11331=CARTESIAN_POINT('Ctrl Pts',(87.0895387725228,4.29078771852967,1.12105321755604));
#11332=CARTESIAN_POINT('Ctrl Pts',(87.0952382948496,4.25517658371521,1.24296469837311));
#11333=CARTESIAN_POINT('Ctrl Pts',(87.1009412698406,4.21954387634003,1.36495003088954));
#11334=CARTESIAN_POINT('Ctrl Pts',(87.1066442448317,4.17869286775462,1.48529455843778));
#11335=CARTESIAN_POINT('Ctrl Pts',(87.1123472198227,4.13281630837234,1.60353308704611));
#11336=CARTESIAN_POINT('Ctrl Pts',(87.1180583629022,4.08687404226776,1.7219409628389));
#11337=CARTESIAN_POINT('Ctrl Pts',(87.1237695059817,4.03589201286711,1.83823645205888));
#11338=CARTESIAN_POINT('Ctrl Pts',(87.1294806490612,3.98010983348217,1.95197712932774));
#11339=CARTESIAN_POINT('Ctrl Pts',(87.1319834983631,3.95566387112538,2.00182280308249));
#11340=CARTESIAN_POINT('Ctrl Pts',(87.134486347665,3.93029659796724,2.0511781665134));
#11341=CARTESIAN_POINT('Ctrl Pts',(87.136989196967,3.90403080308594,2.10000773535627));
#11342=CARTESIAN_POINT('Ctrl Pts',(87.1427003695097,3.84409571773264,2.21143038179008));
#11343=CARTESIAN_POINT('Ctrl Pts',(87.1484115420525,3.779294315079,2.32045700289408));
#11344=CARTESIAN_POINT('Ctrl Pts',(87.1541227145952,3.70984273353467,2.42663468458687));
#11345=CARTESIAN_POINT('Ctrl Pts',(87.1598269204775,3.64047587112314,2.53268284754278));
#11346=CARTESIAN_POINT('Ctrl Pts',(87.1655311263598,3.56647033164159,2.63588865379617));
#11347=CARTESIAN_POINT('Ctrl Pts',(87.1712353322421,3.48808842249057,2.73582312236871));
#11348=CARTESIAN_POINT('Ctrl Pts',(87.1769339987716,3.40978262999094,2.83566054460506));
#11349=CARTESIAN_POINT('Ctrl Pts',(87.182632665301,3.32710916944895,2.93223263822301));
#11350=CARTESIAN_POINT('Ctrl Pts',(87.1883313318305,3.24037371077588,3.02513920580732));
#11351=CARTESIAN_POINT('Ctrl Pts',(87.194025881331,3.15370091455087,3.11797865259635));
#11352=CARTESIAN_POINT('Ctrl Pts',(87.1997204308315,3.06297223241824,3.20715755325056));
#11353=CARTESIAN_POINT('Ctrl Pts',(87.205414980332,2.96853337508941,3.29230900751741));
#11354=CARTESIAN_POINT('Ctrl Pts',(87.2111073974065,2.87412988208054,3.37742857529855));
#11355=CARTESIAN_POINT('Ctrl Pts',(87.2167998144811,2.77601927231698,3.45852342853764));
#11356=CARTESIAN_POINT('Ctrl Pts',(87.2224922315556,2.67458361653639,3.53526398988182));
#11357=CARTESIAN_POINT('Ctrl Pts',(87.2281837174087,2.57316455459554,3.61199199725209));
#11358=CARTESIAN_POINT('Ctrl Pts',(87.2338752032619,2.46842184679726,3.68436688885085));
#11359=CARTESIAN_POINT('Ctrl Pts',(87.239566689115,2.36076967320276,3.75210015192641));
#11360=CARTESIAN_POINT('Ctrl Pts',(87.2452585258005,2.253110863754,3.81983759018995));
#11361=CARTESIAN_POINT('Ctrl Pts',(87.250950362486,2.14254256967276,3.88293261829609));
#11362=CARTESIAN_POINT('Ctrl Pts',(87.2566421991715,2.02950645605981,3.94114102067048));
#11363=CARTESIAN_POINT('Ctrl Pts',(87.2623356686804,1.91643791565405,3.99936612135254));
#11364=CARTESIAN_POINT('Ctrl Pts',(87.2680291381893,1.80090050209572,4.05270162490488));
#11365=CARTESIAN_POINT('Ctrl Pts',(87.2737226076982,1.68335841105118,4.10095031181106));
#11366=CARTESIAN_POINT('Ctrl Pts',(87.2794221307887,1.56569134337505,4.14925029913494));
#11367=CARTESIAN_POINT('Ctrl Pts',(87.2851216538792,1.44601571207244,4.19245251931413));
#11368=CARTESIAN_POINT('Ctrl Pts',(87.2908211769697,1.32481382075879,4.23040864933005));
#11369=CARTESIAN_POINT('Ctrl Pts',(87.2965241527202,1.20353850770115,4.26838777242991));
#11370=CARTESIAN_POINT('Ctrl Pts',(87.3022271284708,1.08073547782594,4.30111437183663));
#11371=CARTESIAN_POINT('Ctrl Pts',(87.3079301042213,0.956898745256767,4.32849093695782));
#11372=CARTESIAN_POINT('Ctrl Pts',(87.3136412480473,0.832884647779103,4.35590671210877));
#11373=CARTESIAN_POINT('Ctrl Pts',(87.3193523918732,0.707834283578074,4.37795708345785));
#11374=CARTESIAN_POINT('Ctrl Pts',(87.3250635356992,0.58224870086875,4.39459616464774));
#11375=CARTESIAN_POINT('Ctrl Pts',(87.3275663764992,0.527212314134499,4.40188804391854));
#11376=CARTESIAN_POINT('Ctrl Pts',(87.3300692172993,0.472073164742458,4.40814134586292));
#11377=CARTESIAN_POINT('Ctrl Pts',(87.3325720580993,0.416873418278865,4.41335536220827));
#11378=CARTESIAN_POINT('Ctrl Pts',(87.338283229234,0.290914468495186,4.42525309843155));
#11379=CARTESIAN_POINT('Ctrl Pts',(87.3439944003688,0.164251468113924,4.43177252013408));
#11380=CARTESIAN_POINT('Ctrl Pts',(87.3497055715035,0.0373811785528921,
4.43284238920018));
#11381=CARTESIAN_POINT('Ctrl Pts',(87.3554097759797,-0.089334350807393,
4.43391095320778));
#11382=CARTESIAN_POINT('Ctrl Pts',(87.3611139804558,-0.216256270566662,
4.42954318637758));
#11383=CARTESIAN_POINT('Ctrl Pts',(87.366818184932,-0.342882139069563,4.41971954299219));
#11384=CARTESIAN_POINT('Ctrl Pts',(87.3725168500588,-0.469385041272681,
4.40990543934059));
#11385=CARTESIAN_POINT('Ctrl Pts',(87.3782155151857,-0.595592068574799,
4.39464603248982));
#11386=CARTESIAN_POINT('Ctrl Pts',(87.3839141803125,-0.721000691778549,
4.37397382279031));
#11387=CARTESIAN_POINT('Ctrl Pts',(87.3896087284155,-0.846318713011158,
4.35331654781298));
#11388=CARTESIAN_POINT('Ctrl Pts',(87.3953032765185,-0.970839085673708,
4.32725431776791));
#11389=CARTESIAN_POINT('Ctrl Pts',(87.4009978246215,-1.09406479104341,4.2958714171864));
#11390=CARTESIAN_POINT('Ctrl Pts',(87.4066902403111,-1.2172443526039,4.26450026842708));
#11391=CARTESIAN_POINT('Ctrl Pts',(87.4123826560007,-1.33912982465032,4.22781250905882));
#11392=CARTESIAN_POINT('Ctrl Pts',(87.4180750716904,-1.45923509001766,4.18594337659519));
#11393=CARTESIAN_POINT('Ctrl Pts',(87.4237665561668,-1.57932070755703,4.14408109343588));
#11394=CARTESIAN_POINT('Ctrl Pts',(87.4294580406433,-1.69762632090548,4.09703925450177));
#11395=CARTESIAN_POINT('Ctrl Pts',(87.4351495251197,-1.813682185152,4.04500258729982));
#11396=CARTESIAN_POINT('Ctrl Pts',(87.4408413604383,-1.92974520346841,3.99296271238445));
#11397=CARTESIAN_POINT('Ctrl Pts',(87.4465331957568,-2.04355783262413,3.93592756013947));
#11398=CARTESIAN_POINT('Ctrl Pts',(87.4522250310753,-2.15467195407877,3.87412929189339));
#11399=CARTESIAN_POINT('Ctrl Pts',(87.4579184992284,-2.26581795118839,3.81231329538513));
#11400=CARTESIAN_POINT('Ctrl Pts',(87.4636119673815,-2.3742635518877,3.74573165854805));
#11401=CARTESIAN_POINT('Ctrl Pts',(87.4693054355345,-2.47958725703953,3.67466134966573));
#11402=CARTESIAN_POINT('Ctrl Pts',(87.4750049572933,-2.5850229480959,3.60351547495695));
#11403=CARTESIAN_POINT('Ctrl Pts',(87.4807044790521,-2.68732978494485,3.52787162263622));
#11404=CARTESIAN_POINT('Ctrl Pts',(87.4864040008109,-2.78611692151813,3.44804894101438));
#11405=CARTESIAN_POINT('Ctrl Pts',(87.4921069752416,-2.88496390163468,3.36817790418893));
#11406=CARTESIAN_POINT('Ctrl Pts',(87.4978099496723,-2.98028663503646,3.28412325865201));
#11407=CARTESIAN_POINT('Ctrl Pts',(87.5035129241031,-3.07173007020539,3.19624207090077));
#11408=CARTESIAN_POINT('Ctrl Pts',(87.5092240666389,-3.16330447555466,3.10823501501051));
#11409=CARTESIAN_POINT('Ctrl Pts',(87.5149352091748,-3.25098821335561,3.01639076155084));
#11410=CARTESIAN_POINT('Ctrl Pts',(87.5206463517106,-3.3344652950368,2.92110085347889));
#11411=CARTESIAN_POINT('Ctrl Pts',(87.523149207551,-3.37104836052882,2.87934092515465));
#11412=CARTESIAN_POINT('Ctrl Pts',(87.5256520633914,-3.40682406325378,2.83691963875481));
#11413=CARTESIAN_POINT('Ctrl Pts',(87.5281549192318,-3.44176843506732,2.79387169343445));
#11414=CARTESIAN_POINT('Ctrl Pts',(87.5338375449392,-3.52110811672034,2.69613319935708));
#11415=CARTESIAN_POINT('Ctrl Pts',(87.5395201706467,-3.5964119446753,2.59485124280539));
#11416=CARTESIAN_POINT('Ctrl Pts',(87.5452027963541,-3.66734576426601,2.49039435538232));
#11417=CARTESIAN_POINT('Ctrl Pts',(87.5508788258846,-3.7381972465619,2.38605871756327));
#11418=CARTESIAN_POINT('Ctrl Pts',(87.5565548554151,-3.80468858180469,2.27855580652901));
#11419=CARTESIAN_POINT('Ctrl Pts',(87.5622308849455,-3.86652512646031,2.16828790672527));
#11420=CARTESIAN_POINT('Ctrl Pts',(87.5679016376123,-3.92830418321563,2.05812252025028));
#11421=CARTESIAN_POINT('Ctrl Pts',(87.573572390279,-3.98543685943425,1.94519760652178));
#11422=CARTESIAN_POINT('Ctrl Pts',(87.5792431429458,-4.03767152406703,1.82994471603331));
#11423=CARTESIAN_POINT('Ctrl Pts',(87.584909933831,-4.08986969577898,1.71477234515067));
#11424=CARTESIAN_POINT('Ctrl Pts',(87.5905767247163,-4.13717649718736,1.59727559882149));
#11425=CARTESIAN_POINT('Ctrl Pts',(87.5962435156015,-4.17938628647332,1.4779104399248));
#11426=CARTESIAN_POINT('Ctrl Pts',(87.6019084037978,-4.22158190334661,1.3585853592261));
#11427=CARTESIAN_POINT('Ctrl Pts',(87.6075732919941,-4.2586837726074,1.2373934914744));
#11428=CARTESIAN_POINT('Ctrl Pts',(87.6132381801904,-4.29053459634209,1.11481024286272));
#11429=CARTESIAN_POINT('Ctrl Pts',(87.618901742379,-4.32237796460081,0.992255687903418));
#11430=CARTESIAN_POINT('Ctrl Pts',(87.6245653045676,-4.34897263461876,0.86831079114068));
#11431=CARTESIAN_POINT('Ctrl Pts',(87.6302288667562,-4.37021155684452,0.743464826621006));
#11432=CARTESIAN_POINT('Ctrl Pts',(87.6358946104868,-4.39145866006998,0.618570772806246));
#11433=CARTESIAN_POINT('Ctrl Pts',(87.6415603542174,-4.40734582223827,0.49277535519587));
#11434=CARTESIAN_POINT('Ctrl Pts',(87.647226097948,-4.41781739133026,0.366576727111689));
#11435=CARTESIAN_POINT('Ctrl Pts',(87.6527534453792,-4.42803317292469,0.243460734589467));
#11436=CARTESIAN_POINT('Ctrl Pts',(87.6582807928105,-4.43309488937622,0.119961368332007));
#11437=CARTESIAN_POINT('Ctrl Pts',(87.6638081402417,-4.43299865229463,-0.00345669697483381));
#11438=CARTESIAN_POINT('',(88.9113509797465,-4.43441641653233,0.00189839995018913));
#11439=CARTESIAN_POINT('Ctrl Pts',(87.6650202097439,-4.43229847675382,-0.0034084650769976));
#11440=CARTESIAN_POINT('Ctrl Pts',(87.6704932507814,-4.43247486644053,-0.136375602761746));
#11441=CARTESIAN_POINT('Ctrl Pts',(87.6758922634644,-4.42670672871812,-0.269126783054866));
#11442=CARTESIAN_POINT('Ctrl Pts',(87.6812939294348,-4.41502948433978,-0.401177373261769));
#11443=CARTESIAN_POINT('Ctrl Pts',(87.6820309487695,-4.41343620646417,-0.41919474765439));
#11444=CARTESIAN_POINT('Ctrl Pts',(87.6827680174995,-4.4117328828111,-0.437199149181645));
#11445=CARTESIAN_POINT('Ctrl Pts',(87.6835053304052,-4.40991956510187,-0.455189411580503));
#11446=CARTESIAN_POINT('Ctrl Pts',(87.6887178317711,-4.39710014886352,-0.582373225401012));
#11447=CARTESIAN_POINT('Ctrl Pts',(87.6939430646484,-4.3787846963171,-0.708848125842272));
#11448=CARTESIAN_POINT('Ctrl Pts',(87.6992680587665,-4.35502730272325,-0.834168868242767));
#11449=CARTESIAN_POINT('Ctrl Pts',(87.7002866233693,-4.35048298969048,-0.858140213445957));
#11450=CARTESIAN_POINT('Ctrl Pts',(87.7013088380383,-4.34573953157213,-0.882069479404934));
#11451=CARTESIAN_POINT('Ctrl Pts',(87.7023353118557,-4.34079724846068,-0.905953759614343));
#11452=CARTESIAN_POINT('Ctrl Pts',(87.7074381184735,-4.31622817076992,-1.02468729284592));
#11453=CARTESIAN_POINT('Ctrl Pts',(87.7126470002665,-4.28674658211013,-1.14230537053208));
#11454=CARTESIAN_POINT('Ctrl Pts',(87.7180446809552,-4.25242531284092,-1.25841504416937));
#11455=CARTESIAN_POINT('Ctrl Pts',(87.7189358598286,-4.2467587327216,-1.27758522004874));
#11456=CARTESIAN_POINT('Ctrl Pts',(87.7198321852358,-4.24096022935233,-1.2967143930399));
#11457=CARTESIAN_POINT('Ctrl Pts',(87.7207340294856,-4.23503013026258,-1.31580093141052));
#11458=CARTESIAN_POINT('Ctrl Pts',(87.720736064821,-4.23501674686482,-1.31584400703725));
#11459=CARTESIAN_POINT('Ctrl Pts',(87.7207381001845,-4.23500336279679,-1.31588708244684));
#11460=CARTESIAN_POINT('Ctrl Pts',(87.720740135576,-4.23498997805851,-1.31593015763928));
#11461=CARTESIAN_POINT('Ctrl Pts',(87.7259254174359,-4.20089155617928,-1.42566678853588));
#11462=CARTESIAN_POINT('Ctrl Pts',(87.7313001131529,-4.16237657502355,-1.53418712737575));
#11463=CARTESIAN_POINT('Ctrl Pts',(87.736787344819,-4.11958680619465,-1.64112867881909));
#11464=CARTESIAN_POINT('Ctrl Pts',(87.7373441981263,-4.11524442997581,-1.65198128360064));
#11465=CARTESIAN_POINT('Ctrl Pts',(87.737902210388,-4.11085806677358,-1.66281760494681));
#11466=CARTESIAN_POINT('Ctrl Pts',(87.7384613012579,-4.10642789009959,-1.67363724810316));
#11467=CARTESIAN_POINT('Ctrl Pts',(87.7445222703657,-4.05840141460399,-1.79093038676529));
#11468=CARTESIAN_POINT('Ctrl Pts',(87.7507094639741,-4.005221102134,-1.90626706198716));
#11469=CARTESIAN_POINT('Ctrl Pts',(87.7569313067568,-3.94711672539678,-2.01919391889636));
#11470=CARTESIAN_POINT('Ctrl Pts',(87.7631471075195,-3.88906877371245,-2.13201111274348));
#11471=CARTESIAN_POINT('Ctrl Pts',(87.7693971393272,-3.82610663410772,-2.24242336510873));
#11472=CARTESIAN_POINT('Ctrl Pts',(87.7756074729833,-3.75849115474214,-2.35000689449741));
#11473=CARTESIAN_POINT('Ctrl Pts',(87.7803266115315,-3.70711117537159,-2.43175799014097));
#11474=CARTESIAN_POINT('Ctrl Pts',(87.7850227077351,-3.65304257006595,-2.51187816833776));
#11475=CARTESIAN_POINT('Ctrl Pts',(87.7895788522303,-3.59628569676082,-2.59009042555527));
#11476=CARTESIAN_POINT('Ctrl Pts',(87.7910142113194,-3.57840511943216,-2.6147302661911));
#11477=CARTESIAN_POINT('Ctrl Pts',(87.792435680341,-3.56025796526518,-2.63918043531533));
#11478=CARTESIAN_POINT('Ctrl Pts',(87.7938396038648,-3.5418449179304,-2.66343143601119));
#11479=CARTESIAN_POINT('Ctrl Pts',(87.7987508798228,-3.47743146865384,-2.7482675076743));
#11480=CARTESIAN_POINT('Ctrl Pts',(87.8035384099442,-3.40989265204633,-2.83075774095742));
#11481=CARTESIAN_POINT('Ctrl Pts',(87.8083050895569,-3.33957594672189,-2.91081530851117));
#11482=CARTESIAN_POINT('Ctrl Pts',(87.8092240279107,-3.32602002883153,-2.92624910631573));
#11483=CARTESIAN_POINT('Ctrl Pts',(87.8101421913435,-3.31236076197933,-2.94159260545349));
#11484=CARTESIAN_POINT('Ctrl Pts',(87.8110603170918,-3.29860047779486,-2.9568453406073));
#11485=CARTESIAN_POINT('Ctrl Pts',(87.8186088511059,-3.18546785581371,-3.08224841348005));
#11486=CARTESIAN_POINT('Ctrl Pts',(87.826154919603,-3.06550846397169,-3.2015208266937));
#11487=CARTESIAN_POINT('Ctrl Pts',(87.8337038723534,-2.93944514446068,-3.3139489700716));
#11488=CARTESIAN_POINT('Ctrl Pts',(87.8375152217357,-2.87579772595896,-3.37071219922264));
#11489=CARTESIAN_POINT('Ctrl Pts',(87.8413272904779,-2.81059401751932,-3.42572993898006));
#11490=CARTESIAN_POINT('Ctrl Pts',(87.8451406948563,-2.74392526922058,-3.47890548267059));
#11491=CARTESIAN_POINT('Ctrl Pts',(87.8505406971192,-2.64951844635391,-3.55420514348822));
#11492=CARTESIAN_POINT('Ctrl Pts',(87.8557777363124,-2.55199162266314,-3.62558803805759));
#11493=CARTESIAN_POINT('Ctrl Pts',(87.8607660921093,-2.45160000857682,-3.6925894509802));
#11494=CARTESIAN_POINT('Ctrl Pts',(87.8610293819821,-2.44630124954955,-3.69612584537723));
#11495=CARTESIAN_POINT('Ctrl Pts',(87.8612919790672,-2.44099452043001,-3.69965002813721));
#11496=CARTESIAN_POINT('Ctrl Pts',(87.8615538707602,-2.43567986237023,-3.70316192913125));
#11497=CARTESIAN_POINT('Ctrl Pts',(87.8667831820891,-2.32955965183829,-3.77328566402855));
#11498=CARTESIAN_POINT('Ctrl Pts',(87.8719528300163,-2.22049027771163,-3.83883161504912));
#11499=CARTESIAN_POINT('Ctrl Pts',(87.8771271699654,-2.10889404994695,-3.89952825585647));
#11500=CARTESIAN_POINT('Ctrl Pts',(87.8823046444025,-1.9972302199301,-3.96026166519713));
#11501=CARTESIAN_POINT('Ctrl Pts',(87.8874871793512,-1.88303635926708,-4.01613950495026));
#11502=CARTESIAN_POINT('Ctrl Pts',(87.8927552908126,-1.76676550402013,-4.06692343977424));
#11503=CARTESIAN_POINT('Ctrl Pts',(87.8976222086898,-1.65934926801978,-4.11383991868457));
#11504=CARTESIAN_POINT('Ctrl Pts',(87.9025626112088,-1.55015983571756,-4.15640893974705));
#11505=CARTESIAN_POINT('Ctrl Pts',(87.9076474056353,-1.43958038938607,-4.19447285018349));
#11506=CARTESIAN_POINT('Ctrl Pts',(87.9080744423271,-1.43029358701345,-4.1976695745792));
#11507=CARTESIAN_POINT('Ctrl Pts',(87.9085024974378,-1.42099696242394,-4.20083454811592));
#11508=CARTESIAN_POINT('Ctrl Pts',(87.9089316129689,-1.41169073228986,-4.20396769064737));
#11509=CARTESIAN_POINT('Ctrl Pts',(87.9113568433636,-1.35909475162497,-4.22167525876358));
#11510=CARTESIAN_POINT('Ctrl Pts',(87.9138160196822,-1.30619305549409,-4.23836575694949));
#11511=CARTESIAN_POINT('Ctrl Pts',(87.9163168496607,-1.25302836710145,-4.2540254365958));
#11512=CARTESIAN_POINT('Ctrl Pts',(87.9163188850285,-1.25298509758774,-4.25403818164789));
#11513=CARTESIAN_POINT('Ctrl Pts',(87.916320920424,-1.2529418278997,-4.25405092601733));
#11514=CARTESIAN_POINT('Ctrl Pts',(87.916322955847,-1.25289855803742,-4.25406366970412));
#11515=CARTESIAN_POINT('Ctrl Pts',(87.921508234785,-1.14266775958701,-4.28652845456093));
#11516=CARTESIAN_POINT('Ctrl Pts',(87.9268829273223,-1.0310004726749,-4.31464332669523));
#11517=CARTESIAN_POINT('Ctrl Pts',(87.932370155382,-0.918276977479303,-4.33832528957188));
#11518=CARTESIAN_POINT('Ctrl Pts',(87.9329270039934,-0.906837700472616,
-4.34072855548319));
#11519=CARTESIAN_POINT('Ctrl Pts',(87.9334850115367,-0.895387586959527,
-4.34308618704253));
#11520=CARTESIAN_POINT('Ctrl Pts',(87.9340440976675,-0.883927061654988,
-4.34539810978408));
#11521=CARTESIAN_POINT('Ctrl Pts',(87.9401050581766,-0.759685397524938,
-4.37046128281655));
#11522=CARTESIAN_POINT('Ctrl Pts',(87.9462922425437,-0.6342144573966,-4.39015059275159));
#11523=CARTESIAN_POINT('Ctrl Pts',(87.9525140754823,-0.508018926972272,
-4.40440590351206));
#11524=CARTESIAN_POINT('Ctrl Pts',(87.9587298664203,-0.38194594459413,-4.41864737098922));
#11525=CARTESIAN_POINT('Ctrl Pts',(87.9649798878039,-0.255149789147666,
-4.42746576246532));
#11526=CARTESIAN_POINT('Ctrl Pts',(87.9711902104774,-0.128127764278676,
-4.4308432002155));
#11527=CARTESIAN_POINT('Ctrl Pts',(87.9759093388396,-0.0316056877795214,
-4.43340966304138));
#11528=CARTESIAN_POINT('Ctrl Pts',(87.9806054245533,0.0650497834022098,
-4.43283435754993));
#11529=CARTESIAN_POINT('Ctrl Pts',(87.9851615579815,0.161607923050945,-4.42896399908761));
#11530=CARTESIAN_POINT('Ctrl Pts',(87.98659691595,0.192027465706768,-4.42774468671513));
#11531=CARTESIAN_POINT('Ctrl Pts',(87.988018383748,0.222436960284434,-4.42619836172543));
#11532=CARTESIAN_POINT('Ctrl Pts',(87.9894223059185,0.252828124164767,-4.42432032756967));
#11533=CARTESIAN_POINT('Ctrl Pts',(87.9943335722267,0.359143917427554,-4.41775050050313));
#11534=CARTESIAN_POINT('Ctrl Pts',(87.9991210925003,0.465240279733896,-4.40727905639325));
#11535=CARTESIAN_POINT('Ctrl Pts',(88.0038877622561,0.570852296194735,-4.39314703482003));
#11536=CARTESIAN_POINT('Ctrl Pts',(88.0048066973714,0.591212546746425,-4.39042261472395));
#11537=CARTESIAN_POINT('Ctrl Pts',(88.0057248575676,0.611554949592072,-4.38756212091687));
#11538=CARTESIAN_POINT('Ctrl Pts',(88.0066429800793,0.631877824749012,-4.38456723584004));
#11539=CARTESIAN_POINT('Ctrl Pts',(88.0141915051284,0.798966345326882,-4.35994419835522));
#11540=CARTESIAN_POINT('Ctrl Pts',(88.0217375646512,0.964737827260598,-4.32624069876181));
#11541=CARTESIAN_POINT('Ctrl Pts',(88.0292865084281,1.12819761612251,-4.28366264960545));
#11542=CARTESIAN_POINT('Ctrl Pts',(88.0330978408085,1.21072566303948,-4.26216572205602));
#11543=CARTESIAN_POINT('Ctrl Pts',(88.0369098925447,1.29266394782887,-4.23840586407211));
#11544=CARTESIAN_POINT('Ctrl Pts',(88.0407232799098,1.37388139772529,-4.21240539787271));
#11545=CARTESIAN_POINT('Ctrl Pts',(88.0461234659674,1.4888944552994,-4.17558580898191));
#11546=CARTESIAN_POINT('Ctrl Pts',(88.0513606683849,1.60237763358752,-4.13399772909822));
#11547=CARTESIAN_POINT('Ctrl Pts',(88.0563491708192,1.71380263773121,-4.08759591053028));
#11548=CARTESIAN_POINT('Ctrl Pts',(88.0566122778055,1.71967949103894,-4.08514855427455));
#11549=CARTESIAN_POINT('Ctrl Pts',(88.0568746929605,1.72555060835203,-4.08268781300049));
#11550=CARTESIAN_POINT('Ctrl Pts',(88.0571364037082,1.73141590866033,-4.0802136820861));
#11551=CARTESIAN_POINT('Ctrl Pts',(88.0623656985315,1.84861164791632,-4.03077757714906));
#11552=CARTESIAN_POINT('Ctrl Pts',(88.0675353291997,1.96363279254374,-3.9763490223034));
#11553=CARTESIAN_POINT('Ctrl Pts',(88.0727096511316,2.07601922845231,-3.9171289283953));
#11554=CARTESIAN_POINT('Ctrl Pts',(88.0778871076421,2.18847374750829,-3.857872959247));
#11555=CARTESIAN_POINT('Ctrl Pts',(88.0830696239014,2.29829011002147,-3.79381933644778));
#11556=CARTESIAN_POINT('Ctrl Pts',(88.0883377160113,2.40501878853675,-3.72521294407968));
#11557=CARTESIAN_POINT('Ctrl Pts',(88.0932046213541,2.50361964153341,-3.66183120917371));
#11558=CARTESIAN_POINT('Ctrl Pts',(88.0981450109309,2.5995855754952,-3.59456338160326));
#11559=CARTESIAN_POINT('Ctrl Pts',(88.1032297924543,2.69257293712625,-3.52364094582055));
#11560=CARTESIAN_POINT('Ctrl Pts',(88.1036568222865,2.70038219643332,-3.51768474185905));
#11561=CARTESIAN_POINT('Ctrl Pts',(88.1040848705103,2.70817047837773,-3.51170276042284));
#11562=CARTESIAN_POINT('Ctrl Pts',(88.1045139791259,2.71593759613605,-3.5056951373899));
#11563=CARTESIAN_POINT('Ctrl Pts',(88.1069393433764,2.75983811235644,-3.47173945902755));
#11564=CARTESIAN_POINT('Ctrl Pts',(88.1093986574765,2.80306162344316,-3.43696535989147));
#11565=CARTESIAN_POINT('Ctrl Pts',(88.1118996305585,2.84557299403375,-3.4014007773705));
#11566=CARTESIAN_POINT('Ctrl Pts',(88.1119016659844,2.84560759206534,-3.40137183300733));
#11567=CARTESIAN_POINT('Ctrl Pts',(88.111903701438,2.84564218962542,-3.40134288812056));
#11568=CARTESIAN_POINT('Ctrl Pts',(88.1119057369191,2.84567678671398,-3.40131394271026));
#11569=CARTESIAN_POINT('Ctrl Pts',(88.1170910069154,2.93381086180585,-3.3275771899429));
#11570=CARTESIAN_POINT('Ctrl Pts',(88.1224656925541,3.01912129529592,-3.25023320982176));
#11571=CARTESIAN_POINT('Ctrl Pts',(88.1279529163455,3.10132817503194,-3.16955246187055));
#11572=CARTESIAN_POINT('Ctrl Pts',(88.1285097837992,3.10967088849377,-3.16136462693259));
#11573=CARTESIAN_POINT('Ctrl Pts',(88.129067810292,3.11798163009313,-3.15314246987529));
#11574=CARTESIAN_POINT('Ctrl Pts',(88.129626915472,3.12626010235041,-3.14488630290015));
#11575=CARTESIAN_POINT('Ctrl Pts',(88.1356878919153,3.21600283258085,-3.05538537295072));
#11576=CARTESIAN_POINT('Ctrl Pts',(88.1418750959406,3.30195485866196,-2.96188192063048));
#11577=CARTESIAN_POINT('Ctrl Pts',(88.1480969516428,3.38378631555431,-2.86476261645715));
#11578=CARTESIAN_POINT('Ctrl Pts',(88.15431276521,3.46553830472435,-2.76773762625779));
#11579=CARTESIAN_POINT('Ctrl Pts',(88.1605628123134,3.54317802963119,-2.66710402004398));
#11580=CARTESIAN_POINT('Ctrl Pts',(88.1667731628852,3.61641488684677,-2.56326575450496));
#11581=CARTESIAN_POINT('Ctrl Pts',(88.1714920014503,3.67206277696543,-2.48436585887157));
#11582=CARTESIAN_POINT('Ctrl Pts',(88.1761878016584,3.72517030285907,-2.40361326898927));
#11583=CARTESIAN_POINT('Ctrl Pts',(88.1807436466793,3.77548197922601,-2.32111496719795));
#11584=CARTESIAN_POINT('Ctrl Pts',(88.1821793085198,3.79133645925306,-2.29511766850974));
#11585=CARTESIAN_POINT('Ctrl Pts',(88.1836010722604,3.8069131011855,-2.26894734746114));
#11586=CARTESIAN_POINT('Ctrl Pts',(88.1850052792021,3.82220339736006,-2.24260829524297));
#11587=CARTESIAN_POINT('Ctrl Pts',(88.1899168034355,3.87568458874708,-2.1504816368349));
#11588=CARTESIAN_POINT('Ctrl Pts',(88.1947045967808,3.92579673910117,-2.05637417839698));
#11589=CARTESIAN_POINT('Ctrl Pts',(88.1994715479029,3.97259354455629,-1.96064006644912));
#11590=CARTESIAN_POINT('Ctrl Pts',(88.200390202769,3.98161191121198,-1.9421908301261));
#11591=CARTESIAN_POINT('Ctrl Pts',(88.2013080835879,3.99050721394496,-1.92368104026898));
#11592=CARTESIAN_POINT('Ctrl Pts',(88.2022259267408,3.99927992078292,-1.90511302553519));
#11593=CARTESIAN_POINT('Ctrl Pts',(88.2097744805054,4.0714286850071,-1.75240539015164));
#11594=CARTESIAN_POINT('Ctrl Pts',(88.2173205684079,4.13529019115885,-1.59575923575179));
#11595=CARTESIAN_POINT('Ctrl Pts',(88.2248695402585,4.19048433181604,-1.43611651446079));
#11596=CARTESIAN_POINT('Ctrl Pts',(88.2286808534316,4.21835066375185,-1.35551634549971));
#11597=CARTESIAN_POINT('Ctrl Pts',(88.2324928858723,4.24400676709187,-1.27415234284282));
#11598=CARTESIAN_POINT('Ctrl Pts',(88.236306253849,4.2673985488282,-1.19214596267452));
#11599=CARTESIAN_POINT('Ctrl Pts',(88.2416972545699,4.30046777083157,-1.07621263095802));
#11600=CARTESIAN_POINT('Ctrl Pts',(88.2469261659875,4.32873726556118,-0.958913468093504));
#11601=CARTESIAN_POINT('Ctrl Pts',(88.251907075901,4.35187709583085,-0.840660627934606));
#11602=CARTESIAN_POINT('Ctrl Pts',(88.2521787203491,4.35313907537538,-0.834211459396023));
#11603=CARTESIAN_POINT('Ctrl Pts',(88.2524496271672,4.35438579664064,-0.827759467187727));
#11604=CARTESIAN_POINT('Ctrl Pts',(88.2527197824194,4.35561720581304,-0.821304722628005));
#11605=CARTESIAN_POINT('Ctrl Pts',(88.2579490955998,4.37945321922404,-0.696362192282912));
#11606=CARTESIAN_POINT('Ctrl Pts',(88.2631187405,4.39792870993742,-0.570461397596616));
#11607=CARTESIAN_POINT('Ctrl Pts',(88.2682930712937,4.41095577524266,-0.444096649467237));
#11608=CARTESIAN_POINT('Ctrl Pts',(88.273470536565,4.42399073201151,-0.317655352799297));
#11609=CARTESIAN_POINT('Ctrl Pts',(88.278653056201,4.43157026328032,-0.190749581896201));
#11610=CARTESIAN_POINT('Ctrl Pts',(88.2839211452246,4.43364893135705,-0.0638892175160819));
#11611=CARTESIAN_POINT('Ctrl Pts',(88.2887880663573,4.43556930771089,0.0533106600021103));
#11612=CARTESIAN_POINT('Ctrl Pts',(88.2937284667628,4.43279464093632,0.170472300102315));
#11613=CARTESIAN_POINT('Ctrl Pts',(88.2988132543505,4.42532704257903,0.287181357734377));
#11614=CARTESIAN_POINT('Ctrl Pts',(88.299240263372,4.42469993047012,0.296982321813913));
#11615=CARTESIAN_POINT('Ctrl Pts',(88.2996682906498,4.42403973806537,0.306780120379378));
#11616=CARTESIAN_POINT('Ctrl Pts',(88.3000973781779,4.42334647486158,0.316574522647752));
#11617=CARTESIAN_POINT('Ctrl Pts',(88.3025226835781,4.41942798531884,0.371934828309909));
#11618=CARTESIAN_POINT('Ctrl Pts',(88.3049819359955,4.41445307170498,0.427185484136135));
#11619=CARTESIAN_POINT('Ctrl Pts',(88.3074828440316,4.40842550340863,0.482281762922626));
#11620=CARTESIAN_POINT('Ctrl Pts',(88.3074848791918,4.40842059836357,0.482326598537384));
#11621=CARTESIAN_POINT('Ctrl Pts',(88.3074869143795,4.40841569262152,0.482371434050032));
#11622=CARTESIAN_POINT('Ctrl Pts',(88.3074889495948,4.40841078618251,0.482416269460595));
#11623=CARTESIAN_POINT('Ctrl Pts',(88.3126742520122,4.39591020693204,0.596647507606413));
#11624=CARTESIAN_POINT('Ctrl Pts',(88.3180489665222,4.37884196458973,0.710528809899669));
#11625=CARTESIAN_POINT('Ctrl Pts',(88.3235362150093,4.35727595214971,0.823677263995305));
#11626=CARTESIAN_POINT('Ctrl Pts',(88.324093059376,4.35508743953416,0.835159535922351));
#11627=CARTESIAN_POINT('Ctrl Pts',(88.3246510626323,4.35285263999814,0.846634230001444));
#11628=CARTESIAN_POINT('Ctrl Pts',(88.3252101444366,4.35057164841986,0.858100925614195));
#11629=CARTESIAN_POINT('Ctrl Pts',(88.3312711206446,4.3258435396182,0.982410764987429));
#11630=CARTESIAN_POINT('Ctrl Pts',(88.3374583186823,4.29568264521297,1.1057850158928));
#11631=CARTESIAN_POINT('Ctrl Pts',(88.34368016388,4.26022787552279,1.2277347657466));
#11632=CARTESIAN_POINT('Ctrl Pts',(88.3498959671657,4.22480753526435,1.34956609258924));
#11633=CARTESIAN_POINT('Ctrl Pts',(88.3561459994899,4.18410394590584,1.46997581808843));
#11634=CARTESIAN_POINT('Ctrl Pts',(88.3623563326784,4.13829217149236,1.58849812001653));
#11635=CARTESIAN_POINT('Ctrl Pts',(88.3670758699542,4.10347755358855,1.67856903972076));
#11636=CARTESIAN_POINT('Ctrl Pts',(88.3717723604219,4.06571167236231,1.76755266132706));
#11637=CARTESIAN_POINT('Ctrl Pts',(88.376328904677,4.02494199509197,1.85517697637475));
#11638=CARTESIAN_POINT('Ctrl Pts',(88.3777638830742,4.01210252665498,1.88277223105159));
#11639=CARTESIAN_POINT('Ctrl Pts',(88.3791849817519,3.99896531190463,1.91023232068102));
#11640=CARTESIAN_POINT('Ctrl Pts',(88.3805885494597,3.9855292098289,1.93754780151039));
#11641=CARTESIAN_POINT('Ctrl Pts',(88.3854995300537,3.93851727290297,2.03312266798681));
#11642=CARTESIAN_POINT('Ctrl Pts',(88.3902867462941,3.88798972519749,2.12699235899576));
#11643=CARTESIAN_POINT('Ctrl Pts',(88.3950531015701,3.83427102944813,2.21900529470237));
#11644=CARTESIAN_POINT('Ctrl Pts',(88.395972404337,3.82391012624636,2.23675213510622));
#11645=CARTESIAN_POINT('Ctrl Pts',(88.3968909310737,3.81343042827611,2.25443003525906));
#11646=CARTESIAN_POINT('Ctrl Pts',(88.3978094201026,3.80283413819877,2.27203809196612));
#11647=CARTESIAN_POINT('Ctrl Pts',(88.4053579462217,3.71574940457759,2.41674844971666));
#11648=CARTESIAN_POINT('Ctrl Pts',(88.4129040072771,3.62079221164668,2.55674564623762));
#11649=CARTESIAN_POINT('Ctrl Pts',(88.4204529529702,3.5185357059676,2.69119109358107));
#11650=CARTESIAN_POINT('Ctrl Pts',(88.4242643804918,3.4669068725042,2.75907197377261));
#11651=CARTESIAN_POINT('Ctrl Pts',(88.428076527498,3.41341680396074,2.8255368598138));
#11652=CARTESIAN_POINT('Ctrl Pts',(88.4318900102808,3.35813659260551,2.89047338262495));
#11653=CARTESIAN_POINT('Ctrl Pts',(88.4375750651803,3.27572608905717,2.98727929946844));
#11654=CARTESIAN_POINT('Ctrl Pts',(88.4430790529799,3.18909069641634,3.08048460237573));
#11655=CARTESIAN_POINT('Ctrl Pts',(88.4483028396688,3.09842148560063,3.16950016809463));
#11656=CARTESIAN_POINT('Ctrl Pts',(88.4535321800864,3.00765587877515,3.25861037173157));
#11657=CARTESIAN_POINT('Ctrl Pts',(88.4587018647028,2.91312064720813,3.34379064768385));
#11658=CARTESIAN_POINT('Ctrl Pts',(88.4638762505298,2.81517843687189,3.42469376862551));
#11659=CARTESIAN_POINT('Ctrl Pts',(88.4690537706853,2.7171768990968,3.50564589576117));
#11660=CARTESIAN_POINT('Ctrl Pts',(88.4742363605741,2.61576406817588,3.58231533116556));
#11661=CARTESIAN_POINT('Ctrl Pts',(88.4795045372405,2.51133909339373,3.65438155550048));
#11662=CARTESIAN_POINT('Ctrl Pts',(88.484371474871,2.41486741609302,3.72095901508639));
#11663=CARTESIAN_POINT('Ctrl Pts',(88.4893119047049,2.3158244805113,3.78360797795596));
#11664=CARTESIAN_POINT('Ctrl Pts',(88.4943967323435,2.21455627826925,3.84210047577926));
#11665=CARTESIAN_POINT('Ctrl Pts',(88.494823817067,2.20605056180728,3.84701337628132));
#11666=CARTESIAN_POINT('Ctrl Pts',(88.4952519204668,2.19752913362981,3.85189698180434));
#11667=CARTESIAN_POINT('Ctrl Pts',(88.4956810845568,2.18899219116201,3.85675117223813));
#11668=CARTESIAN_POINT('Ctrl Pts',(88.4981059652812,2.1407564050935,3.8841785201655));
#11669=CARTESIAN_POINT('Ctrl Pts',(88.5005647830725,2.09202633885257,3.91066624584325));
#11670=CARTESIAN_POINT('Ctrl Pts',(88.5030652419166,2.04284128277649,3.93619269992195));
#11671=CARTESIAN_POINT('Ctrl Pts',(88.5030672774364,2.04280124326366,3.93621347994879));
#11672=CARTESIAN_POINT('Ctrl Pts',(88.5030693129837,2.04276120344924,3.93623425933878));
#11673=CARTESIAN_POINT('Ctrl Pts',(88.5030713485587,2.04272116333327,3.93625503809191));
#11674=CARTESIAN_POINT('Ctrl Pts',(88.5082566148495,1.94072606743195,3.98918522740411));
#11675=CARTESIAN_POINT('Ctrl Pts',(88.5136312927532,1.83648974135252,4.03812022670876));
#11676=CARTESIAN_POINT('Ctrl Pts',(88.519118503124,1.7303695935858,4.08290589957153));
#11677=CARTESIAN_POINT('Ctrl Pts',(88.5196753212208,1.71960098536341,4.08745055367526));
#11678=CARTESIAN_POINT('Ctrl Pts',(88.5202332980985,1.70881302213459,4.09195249017283));
#11679=CARTESIAN_POINT('Ctrl Pts',(88.5207923534241,1.69800610649153,4.09641155483363));
#11680=CARTESIAN_POINT('Ctrl Pts',(88.5268532637511,1.58084463135547,4.14475380257966));
#11681=CARTESIAN_POINT('Ctrl Pts',(88.5330403934088,1.46144966914817,4.18805624318386));
#11682=CARTESIAN_POINT('Ctrl Pts',(88.5392621675087,1.34030510213326,4.22616340826203));
#11683=CARTESIAN_POINT('Ctrl Pts',(88.5454778997516,1.21927817650744,4.26423356813276));
#11684=CARTESIAN_POINT('Ctrl Pts',(88.5517278583337,1.09650512442358,4.29711890313276));
#11685=CARTESIAN_POINT('Ctrl Pts',(88.5579381145954,0.972470658038841,4.32470683472953));
#11686=CARTESIAN_POINT('Ctrl Pts',(88.5626572782554,0.87821706821998,4.34567085920162));
#11687=CARTESIAN_POINT('Ctrl Pts',(88.5673533963492,0.78323215765188,4.3635764621201));
#11688=CARTESIAN_POINT('Ctrl Pts',(88.5719095600084,0.687713116578562,4.37822909513413));
#11689=CARTESIAN_POINT('Ctrl Pts',(88.5733448188024,0.657623208939517,4.38284489078186));
#11690=CARTESIAN_POINT('Ctrl Pts',(88.5747661893163,0.62748068168726,4.38713782493833));
#11691=CARTESIAN_POINT('Ctrl Pts',(88.5761700169476,0.597292765902473,4.39110170631488));
#11692=CARTESIAN_POINT('Ctrl Pts',(88.5810811532897,0.491683667606262,4.40496890870523));
#11693=CARTESIAN_POINT('Ctrl Pts',(88.585868537906,0.385544406328172,4.41496466401966));
#11694=CARTESIAN_POINT('Ctrl Pts',(88.5906350694113,0.279181058186347,4.42127495133937));
#11695=CARTESIAN_POINT('Ctrl Pts',(88.5915540734545,0.258673830472536,4.42249159693455));
#11696=CARTESIAN_POINT('Ctrl Pts',(88.5924723023208,0.238158117201613,4.42357124503042));
#11697=CARTESIAN_POINT('Ctrl Pts',(88.5933904934974,0.217635889383263,4.42451522648365));
#11698=CARTESIAN_POINT('Ctrl Pts',(88.6009389625034,0.0489222221519416,
4.4322757178973));
#11699=CARTESIAN_POINT('Ctrl Pts',(88.6084849660381,-0.120233894879764,
4.43087153852246));
#11700=CARTESIAN_POINT('Ctrl Pts',(88.6160338539244,-0.288816798694789,
4.42031473652558));
#11701=CARTESIAN_POINT('Ctrl Pts',(88.6198451026491,-0.373930180537376,
4.41498486558931));
#11702=CARTESIAN_POINT('Ctrl Pts',(88.6236570707348,-0.458897106836972,
4.40732116841263));
#11703=CARTESIAN_POINT('Ctrl Pts',(88.6274703744389,-0.543584661866787,
4.39732050911107));
#11704=CARTESIAN_POINT('Ctrl Pts',(88.6331553118013,-0.669838294695528,
4.38241135785432));
#11705=CARTESIAN_POINT('Ctrl Pts',(88.6386594526455,-0.795438008294129,
4.36199051247216));
#11706=CARTESIAN_POINT('Ctrl Pts',(88.6438830995456,-0.919787444953118,
4.3358893920313));
#11707=CARTESIAN_POINT('Ctrl Pts',(88.649112301792,-1.04426912718779,4.30976051305939));
#11708=CARTESIAN_POINT('Ctrl Pts',(88.6542818371798,-1.16757034109364,4.27831575586976));
#11709=CARTESIAN_POINT('Ctrl Pts',(88.659456061486,-1.28920107037514,4.24166440484217));
#11710=CARTESIAN_POINT('Ctrl Pts',(88.6646334208795,-1.41090549629898,4.20499084658517));
#11711=CARTESIAN_POINT('Ctrl Pts',(88.6698158376551,-1.53093722145745,4.16310403275407));
#11712=CARTESIAN_POINT('Ctrl Pts',(88.6750838287784,-1.64880821876827,4.11615843292719));
#11713=CARTESIAN_POINT('Ctrl Pts',(88.6799506632503,-1.75770335915673,4.07278773275157));
#11714=CARTESIAN_POINT('Ctrl Pts',(88.6848909813306,-1.86475477089872,4.02509910080773));
#11715=CARTESIAN_POINT('Ctrl Pts',(88.6899756930262,-1.969580903352,3.97325408725581));
#11716=CARTESIAN_POINT('Ctrl Pts',(88.6904026931122,-1.97838391328691,3.96890028578768));
#11717=CARTESIAN_POINT('Ctrl Pts',(88.6908307114877,-1.98717126031601,3.96451717697275));
#11718=CARTESIAN_POINT('Ctrl Pts',(88.6912597901471,-1.99594273513131,3.96010485846834));
#11719=CARTESIAN_POINT('Ctrl Pts',(88.6936858775379,-2.04553822066947,3.93515682142974));
#11720=CARTESIAN_POINT('Ctrl Pts',(88.6961459363321,-2.09462526231771,3.9092755064484));
#11721=CARTESIAN_POINT('Ctrl Pts',(88.6986476831803,-2.14316399688096,3.8824816417897));
#11722=CARTESIAN_POINT('Ctrl Pts',(88.6986497189937,-2.14320349560607,3.88245983810024));
#11723=CARTESIAN_POINT('Ctrl Pts',(88.6986517548349,-2.14324299396828,3.88243803380654));
#11724=CARTESIAN_POINT('Ctrl Pts',(88.6986537907036,-2.14328249196755,3.88241622890861));
#11725=CARTESIAN_POINT('Ctrl Pts',(88.7038390036501,-2.24388108934445,3.82688070335949));
#11726=CARTESIAN_POINT('Ctrl Pts',(88.7092136440908,-2.34239745323425,3.76726498132466));
#11727=CARTESIAN_POINT('Ctrl Pts',(88.7147008378216,-2.43850516198815,3.70378103859378));
#11728=CARTESIAN_POINT('Ctrl Pts',(88.715257811622,-2.44826050842178,3.69733714494214));
#11729=CARTESIAN_POINT('Ctrl Pts',(88.7158159450729,-2.45799102189141,3.69085343770561));
#11730=CARTESIAN_POINT('Ctrl Pts',(88.7163751577785,-2.46769635055009,3.68433016662363));
#11731=CARTESIAN_POINT('Ctrl Pts',(88.7224362182404,-2.57288813752917,3.61362730161045));
#11732=CARTESIAN_POINT('Ctrl Pts',(88.7286235276674,-2.67512390579113,3.53827128339158));
#11733=CARTESIAN_POINT('Ctrl Pts',(88.7348455065168,-2.7740059773852,3.4585786252878));
#11734=CARTESIAN_POINT('Ctrl Pts',(88.7410614424553,-2.87279201272477,3.37896336629461));
#11735=CARTESIAN_POINT('Ctrl Pts',(88.7473116295912,-2.96823112133555,3.29502015789511));
#11736=CARTESIAN_POINT('Ctrl Pts',(88.7535221324707,-3.05996086175842,3.20708998389174));
#11737=CARTESIAN_POINT('Ctrl Pts',(88.7582392319246,-3.12963288620504,3.14030386627584));
#11738=CARTESIAN_POINT('Ctrl Pts',(88.7629333181917,-3.19716706686283,3.07121555595729));
#11739=CARTESIAN_POINT('Ctrl Pts',(88.7674874312259,-3.26229226916579,2.99988097650433));
#11740=CARTESIAN_POINT('Ctrl Pts',(88.7689249016892,-3.28284853424279,2.97736476968212));
#11741=CARTESIAN_POINT('Ctrl Pts',(88.7703484266155,-3.30316453263051,2.95462505731032));
#11742=CARTESIAN_POINT('Ctrl Pts',(88.7717543279102,-3.32323105067908,2.9316644304787));
#11743=CARTESIAN_POINT('Ctrl Pts',(88.7766673796261,-3.39335534838363,2.85142640275877));
#11744=CARTESIAN_POINT('Ctrl Pts',(88.7814567905682,-3.46054933268302,2.76859868729222));
#11745=CARTESIAN_POINT('Ctrl Pts',(88.7862254087508,-3.52479785884816,2.68353934964454));
#11746=CARTESIAN_POINT('Ctrl Pts',(88.7871423864923,-3.53715247944622,2.66718293016405));
#11747=CARTESIAN_POINT('Ctrl Pts',(88.7880585953786,-3.5493982739841,2.65074386475562));
#11748=CARTESIAN_POINT('Ctrl Pts',(88.788974766708,-3.56153525544711,2.6342245144915));
#11749=CARTESIAN_POINT('Ctrl Pts',(88.7965234801215,-3.6615368510353,2.49811477505377));
#11750=CARTESIAN_POINT('Ctrl Pts',(88.8040697256586,-3.7541562003804,2.35655529785458));
#11751=CARTESIAN_POINT('Ctrl Pts',(88.8116188533203,-3.83884021040688,2.21039810832349));
#11752=CARTESIAN_POINT('Ctrl Pts',(88.8154300303283,-3.88159293183581,2.13661065297148));
#11753=CARTESIAN_POINT('Ctrl Pts',(88.8192419260727,-3.92232226499099,2.06165118863399));
#11754=CARTESIAN_POINT('Ctrl Pts',(88.8230551567911,-3.9609519189178,1.98562858541869));
#11755=CARTESIAN_POINT('Ctrl Pts',(88.828393156557,-4.01502813377317,1.87920737250479));
#11756=CARTESIAN_POINT('Ctrl Pts',(88.8335742164791,-4.06474427856229,1.77057398406374));
#11757=CARTESIAN_POINT('Ctrl Pts',(88.838511287705,-4.10970385415131,1.66005705526204));
#11758=CARTESIAN_POINT('Ctrl Pts',(88.8388322416987,-4.1126266305665,1.6528724617967));
#11759=CARTESIAN_POINT('Ctrl Pts',(88.8391521645551,-4.1155292997402,1.64567992572836));
#11760=CARTESIAN_POINT('Ctrl Pts',(88.8394710323585,-4.11841175074111,1.63847954472992));
#11761=CARTESIAN_POINT('Ctrl Pts',(88.8447004338847,-4.16568367190082,1.52039398394477));
#11762=CARTESIAN_POINT('Ctrl Pts',(88.8498701415704,-4.20787696739411,1.40034346845488));
#11763=CARTESIAN_POINT('Ctrl Pts',(88.8550445021581,-4.24481089794598,1.27879640065804));
#11764=CARTESIAN_POINT('Ctrl Pts',(88.8602219967361,-4.28176719852342,1.15717571461982));
#11765=CARTESIAN_POINT('Ctrl Pts',(88.8654045125985,-4.31345736365714,1.03405662772249));
#11766=CARTESIAN_POINT('Ctrl Pts',(88.870672558463,-4.33973936023666,0.909930938328787));
#11767=CARTESIAN_POINT('Ctrl Pts',(88.8755395577144,-4.36402055690264,0.795254708676689));
#11768=CARTESIAN_POINT('Ctrl Pts',(88.8804800061319,-4.38368570117873,0.679718783991746));
#11769=CARTESIAN_POINT('Ctrl Pts',(88.8855648133698,-4.39865768232481,0.563730302321979));
#11770=CARTESIAN_POINT('Ctrl Pts',(88.8859916895257,-4.39991459954097,0.553992919001472));
#11771=CARTESIAN_POINT('Ctrl Pts',(88.8864195830966,-4.40113846038811,0.544252323380795));
#11772=CARTESIAN_POINT('Ctrl Pts',(88.8868485360378,-4.40232923011608,0.534508743603727));
#11773=CARTESIAN_POINT('Ctrl Pts',(88.8892736617257,-4.4090613584635,0.47942250141758));
#11774=CARTESIAN_POINT('Ctrl Pts',(88.8917327225631,-4.41473568588615,0.424242022646549));
#11775=CARTESIAN_POINT('Ctrl Pts',(88.8942334257734,-4.41934736579121,0.36901192318767));
#11776=CARTESIAN_POINT('Ctrl Pts',(88.8942354594229,-4.41935111615261,0.368967008354615));
#11777=CARTESIAN_POINT('Ctrl Pts',(88.8942374931,-4.41935486581136,0.368922093488603));
#11778=CARTESIAN_POINT('Ctrl Pts',(88.8942395268047,-4.41935861476748,0.368877178589694));
#11779=CARTESIAN_POINT('Ctrl Pts',(88.8997640300927,-4.42954255200204,0.246867078456412));
#11780=CARTESIAN_POINT('Ctrl Pts',(88.9054973428673,-4.4345535582682,0.124431760651417));
#11781=CARTESIAN_POINT('Ctrl Pts',(88.9113509797045,-4.43441641653331,0.00189840082963779));
#11782=CARTESIAN_POINT('',(90.165602803248,-4.43009162062031,0.000681083854117898));
#11783=CARTESIAN_POINT('Ctrl Pts',(88.9113509797466,-4.43441641653234,0.00189839995022082));
#11784=CARTESIAN_POINT('Ctrl Pts',(88.9173338959108,-4.43427624595586,-0.123341145899187));
#11785=CARTESIAN_POINT('Ctrl Pts',(88.9234449643459,-4.42875229890772,-0.248759022069367));
#11786=CARTESIAN_POINT('Ctrl Pts',(88.9295950982453,-4.41787437557558,-0.373858329363207));
#11787=CARTESIAN_POINT('Ctrl Pts',(88.935738216371,-4.40700886124961,-0.498814929448322));
#11788=CARTESIAN_POINT('Ctrl Pts',(88.9419199606888,-4.39080193034475,-0.62345371073549));
#11789=CARTESIAN_POINT('Ctrl Pts',(88.9480676269832,-4.36932421936612,-0.747291815820922));
#11790=CARTESIAN_POINT('Ctrl Pts',(88.9528821545821,-4.35250401031208,-0.844275280142007));
#11791=CARTESIAN_POINT('Ctrl Pts',(88.9576756507821,-4.3324506045635,-0.940770445025382));
#11792=CARTESIAN_POINT('Ctrl Pts',(88.9623343406754,-4.30906855001,-1.03650676714499));
#11793=CARTESIAN_POINT('Ctrl Pts',(88.9636191068494,-4.30262028376824,-1.06290877953536));
#11794=CARTESIAN_POINT('Ctrl Pts',(88.9648936204995,-4.29591894294468,-1.08925278486935));
#11795=CARTESIAN_POINT('Ctrl Pts',(88.9661554953129,-4.28896273647101,-1.11553244321305));
#11796=CARTESIAN_POINT('Ctrl Pts',(88.9708462361282,-4.26310457583513,-1.21322126678081));
#11797=CARTESIAN_POINT('Ctrl Pts',(88.9754002049082,-4.23378922342771,-1.31003355369056));
#11798=CARTESIAN_POINT('Ctrl Pts',(88.9799269630748,-4.20130111295997,-1.40578832719475));
#11799=CARTESIAN_POINT('Ctrl Pts',(88.9810305276956,-4.19338093521012,-1.42913209251784));
#11800=CARTESIAN_POINT('Ctrl Pts',(88.982132475133,-4.18527211786431,-1.45241323844826));
#11801=CARTESIAN_POINT('Ctrl Pts',(88.9832343927969,-4.17697862060375,-1.47562958383669));
#11802=CARTESIAN_POINT('Ctrl Pts',(88.9910366261682,-4.11825572032538,-1.64001513702863));
#11803=CARTESIAN_POINT('Ctrl Pts',(88.9988374491339,-4.05027694435988,-1.80115607695242));
#11804=CARTESIAN_POINT('Ctrl Pts',(89.0066420079153,-3.97348734743145,-1.95800388872241));
#11805=CARTESIAN_POINT('Ctrl Pts',(89.0100812937322,-3.93964797495716,-2.02712303684359));
#11806=CARTESIAN_POINT('Ctrl Pts',(89.0135212944197,-3.90409705741618,-2.09540797673298));
#11807=CARTESIAN_POINT('Ctrl Pts',(89.0169624108972,-3.86687043079813,-2.16276657324726));
#11808=CARTESIAN_POINT('Ctrl Pts',(89.0209259000541,-3.82399268111743,-2.2403504239092));
#11809=CARTESIAN_POINT('Ctrl Pts',(89.024866759478,-3.77885276701861,-2.31668898180908));
#11810=CARTESIAN_POINT('Ctrl Pts',(89.0286617337184,-3.7313376756158,-2.39150141749011));
#11811=CARTESIAN_POINT('Ctrl Pts',(89.03025348207,-3.71140814154716,-2.42288043711618));
#11812=CARTESIAN_POINT('Ctrl Pts',(89.0318195653583,-3.69106108346295,-2.45399043620517));
#11813=CARTESIAN_POINT('Ctrl Pts',(89.03335088858,-3.67028971707157,-2.48480844640054));
#11814=CARTESIAN_POINT('Ctrl Pts',(89.0385383040655,-3.59992592571498,-2.5892056246388));
#11815=CARTESIAN_POINT('Ctrl Pts',(89.0436616318504,-3.52517434547603,-2.69057398178545));
#11816=CARTESIAN_POINT('Ctrl Pts',(89.0487810018849,-3.44631601856658,-2.78850971963755));
#11817=CARTESIAN_POINT('Ctrl Pts',(89.0539031865022,-3.3674143360712,-2.8864993016614));
#11818=CARTESIAN_POINT('Ctrl Pts',(89.0590217429199,-3.28440117759914,-2.98105218564797));
#11819=CARTESIAN_POINT('Ctrl Pts',(89.0642128413372,-3.19759783039276,-3.0717841564076));
#11820=CARTESIAN_POINT('Ctrl Pts',(89.0690717194451,-3.11634973037239,-3.15670945563363));
#11821=CARTESIAN_POINT('Ctrl Pts',(89.0739945734964,-3.03178069708182,-3.23828745757245));
#11822=CARTESIAN_POINT('Ctrl Pts',(89.0790519277941,-2.94418994334224,-3.31622257692865));
#11823=CARTESIAN_POINT('Ctrl Pts',(89.0794056240146,-2.9380641082281,-3.3216731258781));
#11824=CARTESIAN_POINT('Ctrl Pts',(89.0797599781006,-2.93192348817042,-3.32710587734651));
#11825=CARTESIAN_POINT('Ctrl Pts',(89.0801150141767,-2.92576818301997,-3.33252073945192));
#11826=CARTESIAN_POINT('Ctrl Pts',(89.0832867255829,-2.87077982306099,-3.38089435851757));
#11827=CARTESIAN_POINT('Ctrl Pts',(89.0865130198547,-2.81462079959568,-3.42783891667989));
#11828=CARTESIAN_POINT('Ctrl Pts',(89.0898115136332,-2.75737118641255,-3.47328798007162));
#11829=CARTESIAN_POINT('Ctrl Pts',(89.0898135509579,-2.75733582601542,-3.4733160518234));
#11830=CARTESIAN_POINT('Ctrl Pts',(89.0898155883101,-2.75730046520219,-3.47334412300495));
#11831=CARTESIAN_POINT('Ctrl Pts',(89.0898176256899,-2.75726510397288,-3.47337219361629));
#11832=CARTESIAN_POINT('Ctrl Pts',(89.0950027180926,-2.66727145434008,-3.54481136050984));
#11833=CARTESIAN_POINT('Ctrl Pts',(89.100377214712,-2.5743147573871,-3.61275793309621));
#11834=CARTESIAN_POINT('Ctrl Pts',(89.1058642294585,-2.47871632386883,-3.67699232012963));
#11835=CARTESIAN_POINT('Ctrl Pts',(89.1064208614938,-2.46901830899426,-3.68350859888005));
#11836=CARTESIAN_POINT('Ctrl Pts',(89.1069786514708,-2.45929315181934,-3.68998667577098));
#11837=CARTESIAN_POINT('Ctrl Pts',(89.1075375191209,-2.44954121765714,-3.69642632268717));
#11838=CARTESIAN_POINT('Ctrl Pts',(89.1135980364993,-2.34378851136875,-3.7662596580647));
#11839=CARTESIAN_POINT('Ctrl Pts',(89.1197847509611,-2.23488089520999,-3.83157395890725));
#11840=CARTESIAN_POINT('Ctrl Pts',(89.12600608789,-2.12326351852121,-3.89212417639549));
#11841=CARTESIAN_POINT('Ctrl Pts',(89.1322213835749,-2.01175452815221,-3.95261559645066));
#11842=CARTESIAN_POINT('Ctrl Pts',(89.1384708837593,-1.8975411877036,-4.00835252387812));
#11843=CARTESIAN_POINT('Ctrl Pts',(89.1446806593068,-1.78107766297801,-4.0591318470126));
#11844=CARTESIAN_POINT('Ctrl Pts',(89.1493984900141,-1.69259536776018,-4.09771105944098));
#11845=CARTESIAN_POINT('Ctrl Pts',(89.1540932717488,-1.60281148049522,-4.13342978859183));
#11846=CARTESIAN_POINT('Ctrl Pts',(89.158648061512,-1.51188218000379,-4.16605936590582));
#11847=CARTESIAN_POINT('Ctrl Pts',(89.1600841171735,-1.48321356003308,-4.17634697338509));
#11848=CARTESIAN_POINT('Ctrl Pts',(89.1615062570085,-1.454431448233,-4.18632737743233));
#11849=CARTESIAN_POINT('Ctrl Pts',(89.1629108159405,-1.42554176845313,-4.19599309903408));
#11850=CARTESIAN_POINT('Ctrl Pts',(89.1678221860351,-1.32452221984552,-4.22979156411283));
#11851=CARTESIAN_POINT('Ctrl Pts',(89.1726098369038,-1.22224222059819,-4.25989086882007));
#11852=CARTESIAN_POINT('Ctrl Pts',(89.1773766575176,-1.11903781963725,-4.28641505536395));
#11853=CARTESIAN_POINT('Ctrl Pts',(89.1782947088245,-1.09916148216865,-4.29152340033682));
#11854=CARTESIAN_POINT('Ctrl Pts',(89.1792119875025,-1.07925070535549,-4.29649917095072));
#11855=CARTESIAN_POINT('Ctrl Pts',(89.1801292285449,-1.05930767157052,-4.30134329367298));
#11856=CARTESIAN_POINT('Ctrl Pts',(89.1876773215829,-0.895193913554452,
-4.34120619481496));
#11857=CARTESIAN_POINT('Ctrl Pts',(89.1952229477402,-0.728894477958929,
-4.37215881116081));
#11858=CARTESIAN_POINT('Ctrl Pts',(89.2027714574259,-0.561408571912545,
-4.39401892309368));
#11859=CARTESIAN_POINT('Ctrl Pts',(89.2065817866909,-0.476865201647971,
-4.40505344880866));
#11860=CARTESIAN_POINT('Ctrl Pts',(89.2103928348589,-0.392019694905821,
-4.41377030824008));
#11861=CARTESIAN_POINT('Ctrl Pts',(89.2142052180091,-0.307001836397285,
-4.42014104547019));
#11862=CARTESIAN_POINT('Ctrl Pts',(89.2195926977515,-0.186858615635747,
-4.42914387032225));
#11863=CARTESIAN_POINT('Ctrl Pts',(89.2248182814199,-0.0663462498244123,
-4.43317662849193));
#11864=CARTESIAN_POINT('Ctrl Pts',(89.2297959854322,0.0540658861819156,
-4.43199935600868));
#11865=CARTESIAN_POINT('Ctrl Pts',(89.2300702234772,0.0606997858047717,
-4.43193449620516));
#11866=CARTESIAN_POINT('Ctrl Pts',(89.2303437091406,0.0673333681263032,
-4.43185382405887));
#11867=CARTESIAN_POINT('Ctrl Pts',(89.230616428044,0.0739665500860772,-4.43175730007139));
#11868=CARTESIAN_POINT('Ctrl Pts',(89.2358448414531,0.201134183399653,-4.429906796479));
#11869=CARTESIAN_POINT('Ctrl Pts',(89.2410135380339,0.328159136093043,-4.4226139610929));
#11870=CARTESIAN_POINT('Ctrl Pts',(89.2461868698266,0.454539645633857,-4.40989243909039));
#11871=CARTESIAN_POINT('Ctrl Pts',(89.2513633410308,0.580996848576844,-4.39716319709366));
#11872=CARTESIAN_POINT('Ctrl Pts',(89.2565448156254,0.706808705286119,-4.37899829750856));
#11873=CARTESIAN_POINT('Ctrl Pts',(89.2618118126829,0.831466778434383,-4.35545611086801));
#11874=CARTESIAN_POINT('Ctrl Pts',(89.2666780531963,0.946639838009085,-4.3337052078098));
#11875=CARTESIAN_POINT('Ctrl Pts',(89.2716177425898,1.06082850511061,-4.30736401137064));
#11876=CARTESIAN_POINT('Ctrl Pts',(89.2767018141772,1.17362740550761,-4.27651819701333));
#11877=CARTESIAN_POINT('Ctrl Pts',(89.2771284065388,1.18309209310655,-4.27392999805395));
#11878=CARTESIAN_POINT('Ctrl Pts',(89.2775560154217,1.1925470248249,-4.2713100942397));
#11879=CARTESIAN_POINT('Ctrl Pts',(89.2779846827297,1.20199197711683,-4.26865854129652));
#11880=CARTESIAN_POINT('Ctrl Pts',(89.2804174194646,1.25559317779004,-4.25361067053862));
#11881=CARTESIAN_POINT('Ctrl Pts',(89.2828843198736,1.30887186588578,-4.23754382354898));
#11882=CARTESIAN_POINT('Ctrl Pts',(89.2853931704633,1.36178458164836,-4.22047084351471));
#11883=CARTESIAN_POINT('Ctrl Pts',(89.2853952084884,1.36182756445652,-4.22045697454928));
#11884=CARTESIAN_POINT('Ctrl Pts',(89.2853972465412,1.36187054702332,-4.22044310492));
#11885=CARTESIAN_POINT('Ctrl Pts',(89.2853992846217,1.3619135293488,-4.22042923462687));
#11886=CARTESIAN_POINT('Ctrl Pts',(89.2905841332388,1.47125997204108,-4.18514340037289));
#11887=CARTESIAN_POINT('Ctrl Pts',(89.2959585034097,1.5793424061195,-4.14545545754308));
#11888=CARTESIAN_POINT('Ctrl Pts',(89.3014455490792,1.68580003074203,-4.10151105507363));
#11889=CARTESIAN_POINT('Ctrl Pts',(89.302003417907,1.69662359479236,-4.09704322051065));
#11890=CARTESIAN_POINT('Ctrl Pts',(89.3025624514413,1.70743033956042,-4.09253142511774));
#11891=CARTESIAN_POINT('Ctrl Pts',(89.3031225689211,1.7182198701591,-4.08797584763621));
#11892=CARTESIAN_POINT('Ctrl Pts',(89.3091844405166,1.83498956834246,-4.03867310895781));
#11893=CARTESIAN_POINT('Ctrl Pts',(89.3153727346175,1.94974656906805,-3.98423749500221));
#11894=CARTESIAN_POINT('Ctrl Pts',(89.3215958436397,2.06203998517011,-3.92490373965682));
#11895=CARTESIAN_POINT('Ctrl Pts',(89.3278129035323,2.17422424724299,-3.86562765927303));
#11896=CARTESIAN_POINT('Ctrl Pts',(89.3340643594162,2.28394991416172,-3.80146327097515));
#11897=CARTESIAN_POINT('Ctrl Pts',(89.3402762346915,2.39079602407734,-3.73267606524159));
#11898=CARTESIAN_POINT('Ctrl Pts',(89.3449806575245,2.47171350178485,-3.68058163530958));
#11899=CARTESIAN_POINT('Ctrl Pts',(89.3496622601,2.55098187085607,-3.62583411085816));
#11900=CARTESIAN_POINT('Ctrl Pts',(89.3542037665837,2.62832529390225,-3.56843478513252));
#11901=CARTESIAN_POINT('Ctrl Pts',(89.3556546766786,2.65303479364132,-3.55009697994909));
#11902=CARTESIAN_POINT('Ctrl Pts',(89.3570912877247,2.67754750425057,-3.53148875628806));
#11903=CARTESIAN_POINT('Ctrl Pts',(89.3585097756134,2.70185356454807,-3.5126108696137));
#11904=CARTESIAN_POINT('Ctrl Pts',(89.3634345461209,2.78624044571976,-3.4470697675156));
#11905=CARTESIAN_POINT('Ctrl Pts',(89.3682363559925,2.86823411515067,-3.37841200418008));
#11906=CARTESIAN_POINT('Ctrl Pts',(89.3730177436943,2.94774968628422,-3.30698727416143));
#11907=CARTESIAN_POINT('Ctrl Pts',(89.3739221568034,2.96279028315424,-3.29347708294421));
#11908=CARTESIAN_POINT('Ctrl Pts',(89.3748258392316,2.97774232400135,-3.27986778830696));
#11909=CARTESIAN_POINT('Ctrl Pts',(89.3757294849248,2.9926053801036,-3.26616160620787));
#11910=CARTESIAN_POINT('Ctrl Pts',(89.3832795785564,3.11678841562773,-3.15164442435767));
#11911=CARTESIAN_POINT('Ctrl Pts',(89.3908271894445,3.23476418346696,-3.03036523766907));
#11912=CARTESIAN_POINT('Ctrl Pts',(89.3983776688004,3.3458269082551,-2.90305519283047));
#11913=CARTESIAN_POINT('Ctrl Pts',(89.4021881937133,3.40187729389938,-2.83880521946445));
#11914=CARTESIAN_POINT('Ctrl Pts',(89.4059994334832,3.45616613254501,-2.77301887523525));
#11915=CARTESIAN_POINT('Ctrl Pts',(89.4098120041868,3.50859783251089,-2.70578840584286));
#11916=CARTESIAN_POINT('Ctrl Pts',(89.4148177941302,3.57743906767941,-2.61751683431374));
#11917=CARTESIAN_POINT('Ctrl Pts',(89.4196987459627,3.64290697351561,-2.52661684222504));
#11918=CARTESIAN_POINT('Ctrl Pts',(89.4243603851711,3.70459795403511,-2.43326738627589));
#11919=CARTESIAN_POINT('Ctrl Pts',(89.4249932219271,3.71297275917051,-2.42059481248169));
#11920=CARTESIAN_POINT('Ctrl Pts',(89.4256220169306,3.72127791977721,-2.40787716541439));
#11921=CARTESIAN_POINT('Ctrl Pts',(89.4262465338218,3.72951239114612,-2.39511495825405));
#11922=CARTESIAN_POINT('Ctrl Pts',(89.4314769467693,3.79847719621511,-2.28822975705153));
#11923=CARTESIAN_POINT('Ctrl Pts',(89.4366474907802,3.86283200099393,-2.17844509759039));
#11924=CARTESIAN_POINT('Ctrl Pts',(89.4418224571373,3.92230987519417,-2.06618623351969));
#11925=CARTESIAN_POINT('Ctrl Pts',(89.4470005519071,3.9818237054423,-1.95385950580816));
#11926=CARTESIAN_POINT('Ctrl Pts',(89.4521834368465,4.0364543234949,-1.83905547073047));
#11927=CARTESIAN_POINT('Ctrl Pts',(89.4574515713837,4.08596831636072,-1.7222297335028));
#11928=CARTESIAN_POINT('Ctrl Pts',(89.4623194214103,4.13172012656755,-1.61428067410462));
#11929=CARTESIAN_POINT('Ctrl Pts',(89.4672605040975,4.17310344574936,-1.50460496351978));
#11930=CARTESIAN_POINT('Ctrl Pts',(89.4723457326437,4.20996469303591,-1.39358768311256));
#11931=CARTESIAN_POINT('Ctrl Pts',(89.4727717610203,4.21305284083464,-1.38428691888595));
#11932=CARTESIAN_POINT('Ctrl Pts',(89.4731988011121,4.21610927368266,-1.37497672018469));
#11933=CARTESIAN_POINT('Ctrl Pts',(89.4736268946167,4.21913391429703,-1.36565730306687));
#11934=CARTESIAN_POINT('Ctrl Pts',(89.4760478287954,4.23623871911896,-1.31295457531239));
#11935=CARTESIAN_POINT('Ctrl Pts',(89.4785025261831,4.25232646398416,-1.25995813713637));
#11936=CARTESIAN_POINT('Ctrl Pts',(89.4809986540732,4.26738392615008,-1.20671064490624));
#11937=CARTESIAN_POINT('Ctrl Pts',(89.4810006752033,4.26739611826994,-1.20666753008381));
#11938=CARTESIAN_POINT('Ctrl Pts',(89.4810026963606,4.26740830971445,-1.20662441509673));
#11939=CARTESIAN_POINT('Ctrl Pts',(89.4810047175451,4.26742050048366,-1.20658129994494));
#11940=CARTESIAN_POINT('Ctrl Pts',(89.4861917547402,4.29870610289723,-1.0959333602064));
#11941=CARTESIAN_POINT('Ctrl Pts',(89.4915680031363,4.32562082854711,-0.983895404350818));
#11942=CARTESIAN_POINT('Ctrl Pts',(89.4970565467966,4.34808585448519,-0.870849151089466));
#11943=CARTESIAN_POINT('Ctrl Pts',(89.4976120258965,4.35035947261769,-0.859408077665633));
#11944=CARTESIAN_POINT('Ctrl Pts',(89.498168655221,4.35258753077173,-0.847956716715763));
#11945=CARTESIAN_POINT('Ctrl Pts',(89.4987263550352,4.35476995967272,-0.836495490889139));
#11946=CARTESIAN_POINT('Ctrl Pts',(89.5047871538682,4.37848749050107,-0.711940699322092));
#11947=CARTESIAN_POINT('Ctrl Pts',(89.5109738447826,4.3968140506005,-0.586215222197355));
#11948=CARTESIAN_POINT('Ctrl Pts',(89.5171949220758,4.4096950871461,-0.459824704450336));
#11949=CARTESIAN_POINT('Ctrl Pts',(89.5234099701794,4.42256363996781,-0.333556678734284));
#11950=CARTESIAN_POINT('Ctrl Pts',(89.5296589876668,4.42999759358508,-0.206624906597751));
#11951=CARTESIAN_POINT('Ctrl Pts',(89.5358681517012,4.43198454857099,-0.0795271829341869));
#11952=CARTESIAN_POINT('Ctrl Pts',(89.5406269195087,4.43350737150969,0.0178818325815445));
#11953=CARTESIAN_POINT('Ctrl Pts',(89.5453621565787,4.43183064963855,0.115391277068648));
#11954=CARTESIAN_POINT('Ctrl Pts',(89.5499579312158,4.42680655288177,0.212763109606407));
#11955=CARTESIAN_POINT('Ctrl Pts',(89.5513543258259,4.42528001553263,0.242348873240857));
#11956=CARTESIAN_POINT('Ctrl Pts',(89.5527378451727,4.42344446848295,0.271921568999827));
#11957=CARTESIAN_POINT('Ctrl Pts',(89.5541052372566,4.42129586055704,0.301473570175083));
#11958=CARTESIAN_POINT('Ctrl Pts',(89.5589866201823,4.41362565523155,0.406969744726389));
#11959=CARTESIAN_POINT('Ctrl Pts',(89.563742402052,4.40210444461492,0.512207558966018));
#11960=CARTESIAN_POINT('Ctrl Pts',(89.5684762919852,4.38697600267487,0.616929843529802));
#11961=CARTESIAN_POINT('Ctrl Pts',(89.5694306922429,4.38392595523184,0.638042918989072));
#11962=CARTESIAN_POINT('Ctrl Pts',(89.5703842026667,4.38072925578238,0.659135206687543));
#11963=CARTESIAN_POINT('Ctrl Pts',(89.5713376731298,4.37738784884745,0.680204850114617));
#11964=CARTESIAN_POINT('Ctrl Pts',(89.5788844684349,4.35094034454968,0.846972770317364));
#11965=CARTESIAN_POINT('Ctrl Pts',(89.5864288425466,4.31543097305138,1.01232512314864));
#11966=CARTESIAN_POINT('Ctrl Pts',(89.593976139271,4.27107536506261,1.17527016033225));
#11967=CARTESIAN_POINT('Ctrl Pts',(89.597793584079,4.24864016851367,1.2576882378122));
#11968=CARTESIAN_POINT('Ctrl Pts',(89.6016117602949,4.2239410393046,1.33948992067119));
#11969=CARTESIAN_POINT('Ctrl Pts',(89.60543128547,4.19700173026486,1.42054371498032));
#11970=CARTESIAN_POINT('Ctrl Pts',(89.6111185526549,4.15688914001854,1.54123269160687));
#11971=CARTESIAN_POINT('Ctrl Pts',(89.6165795575936,4.11143224684027,1.6601375750728));
#11972=CARTESIAN_POINT('Ctrl Pts',(89.6218045518171,4.06073151655111,1.77669543562417));
#11973=CARTESIAN_POINT('Ctrl Pts',(89.6270350820097,4.00997706798581,1.89337679118843));
#11974=CARTESIAN_POINT('Ctrl Pts',(89.6322066309984,3.95425048069523,2.0078268626318));
#11975=CARTESIAN_POINT('Ctrl Pts',(89.6373837123003,3.89375777934207,2.11958730871945));
#11976=CARTESIAN_POINT('Ctrl Pts',(89.6425639213951,3.83322853063225,2.23141527615749));
#11977=CARTESIAN_POINT('Ctrl Pts',(89.6477500340735,3.76792710080369,2.34055010825465));
#11978=CARTESIAN_POINT('Ctrl Pts',(89.6530226807491,3.69810344281083,2.4465445067072));
#11979=CARTESIAN_POINT('Ctrl Pts',(89.6578902916207,3.63364352018499,2.54439659465884));
#11980=CARTESIAN_POINT('Ctrl Pts',(89.6628320995932,3.56532911573377,2.63957259728861));
#11981=CARTESIAN_POINT('Ctrl Pts',(89.6679188913664,3.49339515664647,2.73173174790067));
#11982=CARTESIAN_POINT('Ctrl Pts',(89.6683500243098,3.48729836698028,2.73954273125576));
#11983=CARTESIAN_POINT('Ctrl Pts',(89.6687821987406,3.48117557438164,2.74733207408508));
#11984=CARTESIAN_POINT('Ctrl Pts',(89.6692154577563,3.47502692045516,2.75509958611351));
#11985=CARTESIAN_POINT('Ctrl Pts',(89.6716194560804,3.44091025305919,2.79819871440032));
#11986=CARTESIAN_POINT('Ctrl Pts',(89.6740569175401,3.40599811156927,2.84062486370988));
#11987=CARTESIAN_POINT('Ctrl Pts',(89.676535320568,3.3703179949989,2.88234419597204));
#11988=CARTESIAN_POINT('Ctrl Pts',(89.6765373770621,3.37028838885844,2.88237881324713));
#11989=CARTESIAN_POINT('Ctrl Pts',(89.6765394335843,3.37025878218922,2.88241343003576));
#11990=CARTESIAN_POINT('Ctrl Pts',(89.6765414901348,3.37022917499128,2.8824480463379));
#11991=CARTESIAN_POINT('Ctrl Pts',(89.6817246002952,3.29561035476463,2.96969127792232));
#11992=CARTESIAN_POINT('Ctrl Pts',(89.6870971351162,3.21742057117278,3.05407878664307));
#11993=CARTESIAN_POINT('Ctrl Pts',(89.6925821699911,3.13593264311377,3.13533383337643));
#11994=CARTESIAN_POINT('Ctrl Pts',(89.6931379074117,3.12767638003009,3.14356650119223));
#11995=CARTESIAN_POINT('Ctrl Pts',(89.6936947997026,3.11938630326912,3.15176700506032));
#11996=CARTESIAN_POINT('Ctrl Pts',(89.6942527668554,3.11106272600721,3.15993505256923));
#11997=CARTESIAN_POINT('Ctrl Pts',(89.7003103652556,3.02069739167921,3.24861187032716));
#11998=CARTESIAN_POINT('Ctrl Pts',(89.7064941172793,2.92637771691585,3.33346463487352));
#11999=CARTESIAN_POINT('Ctrl Pts',(89.7127124239763,2.82849292331517,3.41416809356799));
#12000=CARTESIAN_POINT('Ctrl Pts',(89.7189246893456,2.73070322861293,3.49479314570166));
#12001=CARTESIAN_POINT('Ctrl Pts',(89.72517109202,2.62935555257194,3.5712772566176));
#12002=CARTESIAN_POINT('Ctrl Pts',(89.7313776590001,2.52485602787657,3.64333458333348));
#12003=CARTESIAN_POINT('Ctrl Pts',(89.7360710253056,2.44583415480109,3.69782387352403));
#12004=CARTESIAN_POINT('Ctrl Pts',(89.7407414940435,2.36500744803604,3.7497834056166));
#12005=CARTESIAN_POINT('Ctrl Pts',(89.7452715010768,2.28248170464977,3.79895922126368));
#12006=CARTESIAN_POINT('Ctrl Pts',(89.7467277117614,2.25595307712563,3.8147672205978));
#12007=CARTESIAN_POINT('Ctrl Pts',(89.7481694077278,2.22924922615302,3.83028735963664));
#12008=CARTESIAN_POINT('Ctrl Pts',(89.7495926837077,2.2023746782247,3.84551066645313));
#12009=CARTESIAN_POINT('Ctrl Pts',(89.7545174974658,2.10938347676613,3.89818629079531));
#12010=CARTESIAN_POINT('Ctrl Pts',(89.7593195488321,2.01443638926538,3.94745303884877));
#12011=CARTESIAN_POINT('Ctrl Pts',(89.7641013390683,1.9178892102015,3.99336711653667));
#12012=CARTESIAN_POINT('Ctrl Pts',(89.764998372304,1.89977757749617,4.00198030357279));
#12013=CARTESIAN_POINT('Ctrl Pts',(89.765894692523,1.88160949962352,4.01047556339915));
#12014=CARTESIAN_POINT('Ctrl Pts',(89.7667909764052,1.86338713528538,4.01885334158174));
#12015=CARTESIAN_POINT('Ctrl Pts',(89.7743368307102,1.70997223056509,4.08938623280268));
#12016=CARTESIAN_POINT('Ctrl Pts',(89.7818801906671,1.55270916543701,4.15159685260309));
#12017=CARTESIAN_POINT('Ctrl Pts',(89.7894264133058,1.39254406239966,4.20511595881072));
#12018=CARTESIAN_POINT('Ctrl Pts',(89.7932274826785,1.31186811406322,4.23207379522788));
#12019=CARTESIAN_POINT('Ctrl Pts',(89.7970292629555,1.23045586309233,4.25682554070753));
#12020=CARTESIAN_POINT('Ctrl Pts',(89.800832368387,1.14842847364711,4.2793188753807));
#12021=CARTESIAN_POINT('Ctrl Pts',(89.805778431349,1.04174917166579,4.30857219257627));
#12022=CARTESIAN_POINT('Ctrl Pts',(89.810604176573,0.933969361096981,4.33380130625309));
#12023=CARTESIAN_POINT('Ctrl Pts',(89.8152137598078,0.825396603966911,4.35470532685636));
#12024=CARTESIAN_POINT('Ctrl Pts',(89.8158964139658,0.80931757028313,4.3578010983951));
#12025=CARTESIAN_POINT('Ctrl Pts',(89.8165743272599,0.793221238163659,4.36080200005832));
#12026=CARTESIAN_POINT('Ctrl Pts',(89.8172471883871,0.777108703461246,4.36370704470046));
#12027=CARTESIAN_POINT('Ctrl Pts',(89.8224691458586,0.65206214100666,4.3862525878435));
#12028=CARTESIAN_POINT('Ctrl Pts',(89.8276307488096,0.526115646042954,4.40343949263792));
#12029=CARTESIAN_POINT('Ctrl Pts',(89.8327962608015,0.399763398328317,4.41518556770788));
#12030=CARTESIAN_POINT('Ctrl Pts',(89.8379649469734,0.273333507817401,4.42693886067961));
#12031=CARTESIAN_POINT('Ctrl Pts',(89.8431379071372,0.146497411646854,4.4332442417418));
#12032=CARTESIAN_POINT('Ctrl Pts',(89.8483956324844,0.01976430259382,4.43406208281381));
#12033=CARTESIAN_POINT('Ctrl Pts',(89.8532570899878,-0.0974170987240542,
4.43481828427993));
#12034=CARTESIAN_POINT('Ctrl Pts',(89.8581914608689,-0.214510963110474,
4.43088287360859));
#12035=CARTESIAN_POINT('Ctrl Pts',(89.8632699008244,-0.331102946416727,
4.42226261826606));
#12036=CARTESIAN_POINT('Ctrl Pts',(89.8636918505398,-0.340790164263757,
4.42154639156649));
#12037=CARTESIAN_POINT('Ctrl Pts',(89.8641147948164,-0.350473943311404,
4.42079783849864));
#12038=CARTESIAN_POINT('Ctrl Pts',(89.8645387744674,-0.360154060141499,
4.42001697073321));
#12039=CARTESIAN_POINT('Ctrl Pts',(89.8670300356084,-0.417033438293562,
4.41542867147029));
#12040=CARTESIAN_POINT('Ctrl Pts',(89.8695571253028,-0.473785165872243,
4.40972479577506));
#12041=CARTESIAN_POINT('Ctrl Pts',(89.8721284688833,-0.530360614488174,
4.40291002433756));
#12042=CARTESIAN_POINT('Ctrl Pts',(89.8721305157863,-0.530405651043084,
4.40290459947862));
#12043=CARTESIAN_POINT('Ctrl Pts',(89.8721325627174,-0.530450687486401,
4.40289917391584));
#12044=CARTESIAN_POINT('Ctrl Pts',(89.8721346096765,-0.530495723818192,
4.40289374764922));
#12045=CARTESIAN_POINT('Ctrl Pts',(89.8773174883639,-0.644527236988256,
4.38915449827478));
#12046=CARTESIAN_POINT('Ctrl Pts',(89.8826906006202,-0.758158274707413,
4.37085577659649));
#12047=CARTESIAN_POINT('Ctrl Pts',(89.8881773330672,-0.871007550141101,
4.34807159512846));
#12048=CARTESIAN_POINT('Ctrl Pts',(89.8887424788253,-0.882631278824343,
4.34572477329344));
#12049=CARTESIAN_POINT('Ctrl Pts',(89.8893088300326,-0.894246682134268,
4.34333039628311));
#12050=CARTESIAN_POINT('Ctrl Pts',(89.8898763029661,-0.905853322338966,
4.34088856817269));
#12051=CARTESIAN_POINT('Ctrl Pts',(89.8959456543481,-1.02999100999629,4.31477223390734));
#12052=CARTESIAN_POINT('Ctrl Pts',(89.9021427817368,-1.15313066849812,4.28322378915472));
#12053=CARTESIAN_POINT('Ctrl Pts',(89.9083758714525,-1.27478404874763,4.24638798134476));
#12054=CARTESIAN_POINT('Ctrl Pts',(89.9146028639203,-1.39631842688783,4.20958820655599));
#12055=CARTESIAN_POINT('Ctrl Pts',(89.9208653940798,-1.51636957290059,4.16751175951246));
#12056=CARTESIAN_POINT('Ctrl Pts',(89.9270891863883,-1.63447285878813,4.12033933563166));
#12057=CARTESIAN_POINT('Ctrl Pts',(89.9317114380169,-1.72218515355638,4.08530558092051));
#12058=CARTESIAN_POINT('Ctrl Pts',(89.9363122075619,-1.80882584158771,4.04745984070014));
#12059=CARTESIAN_POINT('Ctrl Pts',(89.9407721234367,-1.89413224688722,4.00674055007368));
#12060=CARTESIAN_POINT('Ctrl Pts',(89.9423130277404,-1.92360567435756,3.99267200440341));
#12061=CARTESIAN_POINT('Ctrl Pts',(89.9438371182328,-1.95291941697748,3.9782606411765));
#12062=CARTESIAN_POINT('Ctrl Pts',(89.9453394717082,-1.98206136903127,3.96350461204857));
#12063=CARTESIAN_POINT('Ctrl Pts',(89.9503538005096,-2.07932698055376,3.91425416396182));
#12064=CARTESIAN_POINT('Ctrl Pts',(89.955250113313,-2.1747713328336,3.86135855748933));
#12065=CARTESIAN_POINT('Ctrl Pts',(89.9601286446972,-2.26823055634348,3.80515107825526));
#12066=CARTESIAN_POINT('Ctrl Pts',(89.9609401275364,-2.28377633233121,3.79580166523648));
#12067=CARTESIAN_POINT('Ctrl Pts',(89.9617511183963,-2.29926728034706,3.7863605533578));
#12068=CARTESIAN_POINT('Ctrl Pts',(89.962562078582,-2.31470275989553,3.77682919509475));
#12069=CARTESIAN_POINT('Ctrl Pts',(89.9701235366887,-2.45862441478185,3.68795804274576));
#12070=CARTESIAN_POINT('Ctrl Pts',(89.9776824090846,-2.59772786769584,3.59124350771912));
#12071=CARTESIAN_POINT('Ctrl Pts',(89.985244053236,-2.73117933405758,3.48727195385883));
#12072=CARTESIAN_POINT('Ctrl Pts',(89.9890536844359,-2.79841350426469,3.43489005548395));
#12073=CARTESIAN_POINT('Ctrl Pts',(89.9928640041446,-2.86421232880433,3.38066564527305));
#12074=CARTESIAN_POINT('Ctrl Pts',(89.9966756281,-2.92846479451651,3.32467103867188));
#12075=CARTESIAN_POINT('Ctrl Pts',(90.0006119242939,-2.99481885756006,3.26684493635301));
#12076=CARTESIAN_POINT('Ctrl Pts',(90.0045291630206,-3.05950369332435,3.20710090106199));
#12077=CARTESIAN_POINT('Ctrl Pts',(90.0083031414468,-3.12222395701885,3.14538182858948));
#12078=CARTESIAN_POINT('Ctrl Pts',(90.0099848246292,-3.15017207985835,3.11787983613289));
#12079=CARTESIAN_POINT('Ctrl Pts',(90.0116380621922,-3.17772961640656,3.08998615730642));
#12080=CARTESIAN_POINT('Ctrl Pts',(90.0132518649428,-3.20486813651541,3.06169815698806));
#12081=CARTESIAN_POINT('Ctrl Pts',(90.0184927423126,-3.29300137078605,2.96983194803096));
#12082=CARTESIAN_POINT('Ctrl Pts',(90.0236726666322,-3.37715683995339,2.87423383398628));
#12083=CARTESIAN_POINT('Ctrl Pts',(90.0288555389961,-3.45699080402158,2.77527061821678));
#12084=CARTESIAN_POINT('Ctrl Pts',(90.034041481007,-3.53687205115229,2.67624878975064));
#12085=CARTESIAN_POINT('Ctrl Pts',(90.0392307359719,-3.61242631811392,2.573857690922));
#12086=CARTESIAN_POINT('Ctrl Pts',(90.0445033950305,-3.68333694365767,2.46850028678336));
#12087=CARTESIAN_POINT('Ctrl Pts',(90.0493797745034,-3.74891810772849,2.37106127600172));
#12088=CARTESIAN_POINT('Ctrl Pts',(90.054327937649,-3.8105276228146,2.27108461766728));
#12089=CARTESIAN_POINT('Ctrl Pts',(90.0594187312763,-3.86794016046396,2.16892013463666));
#12090=CARTESIAN_POINT('Ctrl Pts',(90.0598401599257,-3.87269291415439,2.16046270279974));
#12091=CARTESIAN_POINT('Ctrl Pts',(90.0602625660136,-3.87741693269434,2.15199026474082));
#12092=CARTESIAN_POINT('Ctrl Pts',(90.0606859897318,-3.88211210247967,2.14350301148524));
#12093=CARTESIAN_POINT('Ctrl Pts',(90.0630498662488,-3.90832414758128,2.09612064294574));
#12094=CARTESIAN_POINT('Ctrl Pts',(90.0654455307188,-3.93363656390953,2.04827750127295));
#12095=CARTESIAN_POINT('Ctrl Pts',(90.0678800983053,-3.95802962213333,2.0000102121832));
#12096=CARTESIAN_POINT('Ctrl Pts',(90.0678820203875,-3.95804888036328,1.99997210533559));
#12097=CARTESIAN_POINT('Ctrl Pts',(90.0678839424939,-3.95806813802033,1.99993399822355));
#12098=CARTESIAN_POINT('Ctrl Pts',(90.0678858646246,-3.95808739510449,1.9998958908471));
#12099=CARTESIAN_POINT('Ctrl Pts',(90.0732309642032,-4.01163788139567,1.8939261332634));
#12100=CARTESIAN_POINT('Ctrl Pts',(90.0787724672161,-4.06087636930101,1.78565972066588));
#12101=CARTESIAN_POINT('Ctrl Pts',(90.0844273157989,-4.10565742180452,1.67547174493592));
#12102=CARTESIAN_POINT('Ctrl Pts',(90.0851576778716,-4.11144119865498,1.66124022004765));
#12103=CARTESIAN_POINT('Ctrl Pts',(90.0858899307157,-4.11715062444602,1.64697671170688));
#12104=CARTESIAN_POINT('Ctrl Pts',(90.0866238953809,-4.12278539225322,1.63268209105214));
#12105=CARTESIAN_POINT('Ctrl Pts',(90.0926958776793,-4.16940100197741,1.51442478562329));
#12106=CARTESIAN_POINT('Ctrl Pts',(90.0988843397485,-4.21090677877972,1.39403285447817));
#12107=CARTESIAN_POINT('Ctrl Pts',(90.1051009695411,-4.24716787846438,1.27196470229976));
#12108=CARTESIAN_POINT('Ctrl Pts',(90.1056667642231,-4.25046811316574,1.26085490267277));
#12109=CARTESIAN_POINT('Ctrl Pts',(90.1062327922292,-4.25372490028258,1.24973125374402));
#12110=CARTESIAN_POINT('Ctrl Pts',(90.1067989869812,-4.25693813637941,1.23859412245778));
#12111=CARTESIAN_POINT('Ctrl Pts',(90.1133457850976,-4.29409215088169,1.10981767253204));
#12112=CARTESIAN_POINT('Ctrl Pts',(90.1199146002839,-4.32542476178032,0.979232877876883));
#12113=CARTESIAN_POINT('Ctrl Pts',(90.1264255217307,-4.35081835891402,0.847375981929201));
#12114=CARTESIAN_POINT('Ctrl Pts',(90.1311208337292,-4.3691307993701,0.752288171287351));
#12115=CARTESIAN_POINT('Ctrl Pts',(90.1357859242796,-4.38435482539701,0.656535837450231));
#12116=CARTESIAN_POINT('Ctrl Pts',(90.1403067822695,-4.39629686998514,0.560308977345115));
#12117=CARTESIAN_POINT('Ctrl Pts',(90.1420457297909,-4.40089037610365,0.523295326341313));
#12118=CARTESIAN_POINT('Ctrl Pts',(90.1437633373064,-4.40499818958299,0.486212003666932));
#12119=CARTESIAN_POINT('Ctrl Pts',(90.1454531163204,-4.4086089998006,0.449071857940345));
#12120=CARTESIAN_POINT('Ctrl Pts',(90.1515246864034,-4.42158305564537,0.315623048476399));
#12121=CARTESIAN_POINT('Ctrl Pts',(90.1575222905921,-4.42863360464323,0.181494394818817));
#12122=CARTESIAN_POINT('Ctrl Pts',(90.1635243306403,-4.42988874177923,0.0471916357765029));
#12123=CARTESIAN_POINT('Ctrl Pts',(90.1642165712484,-4.43003350204195,0.0317019318033428));
#12124=CARTESIAN_POINT('Ctrl Pts',(90.1649088715641,-4.43010114383871,0.016209846318666));
#12125=CARTESIAN_POINT('Ctrl Pts',(90.1656012380541,-4.43009164223147,0.000716109671487679));
#12126=CARTESIAN_POINT('',(90.4404529603198,-0.735086155396302,-4.37342048255888));
#12127=CARTESIAN_POINT('Ctrl Pts',(90.165602803248,-4.43009162062031,0.000681083854117794));
#12128=CARTESIAN_POINT('Ctrl Pts',(90.1707097639098,-4.43002067830906,-0.113602183773604));
#12129=CARTESIAN_POINT('Ctrl Pts',(90.1758092756259,-4.42575708944723,-0.227727827826633));
#12130=CARTESIAN_POINT('Ctrl Pts',(90.1809092724363,-4.41731798229872,-0.34152341032841));
#12131=CARTESIAN_POINT('Ctrl Pts',(90.1817440651521,-4.41593662747877,-0.360150034402737));
#12132=CARTESIAN_POINT('Ctrl Pts',(90.182578870865,-4.41444328573784,-0.378767814898256));
#12133=CARTESIAN_POINT('Ctrl Pts',(90.1834137243702,-4.41283789931972,-0.39737599070201));
#12134=CARTESIAN_POINT('Ctrl Pts',(90.1873690216296,-4.40523203738054,-0.485536208395152));
#12135=CARTESIAN_POINT('Ctrl Pts',(90.1913231750305,-4.39511257454556,-0.573451544421442));
#12136=CARTESIAN_POINT('Ctrl Pts',(90.1951514067466,-4.38226713767787,-0.660932921087678));
#12137=CARTESIAN_POINT('Ctrl Pts',(90.1970739920729,-4.3758160003741,-0.704867150667409));
#12138=CARTESIAN_POINT('Ctrl Pts',(90.1989648177762,-4.36867737148063,-0.748691109347414));
#12139=CARTESIAN_POINT('Ctrl Pts',(90.2008080786697,-4.36082494922787,-0.792375921086213));
#12140=CARTESIAN_POINT('Ctrl Pts',(90.2063330165938,-4.33728832147512,-0.923315536818702));
#12141=CARTESIAN_POINT('Ctrl Pts',(90.2117707070029,-4.30791923130784,-1.05310610318921));
#12142=CARTESIAN_POINT('Ctrl Pts',(90.2171864362058,-4.27282885090481,-1.1812175042564));
#12143=CARTESIAN_POINT('Ctrl Pts',(90.222607978033,-4.2377008085011,-1.3094664054481));
#12144=CARTESIAN_POINT('Ctrl Pts',(90.2280078812813,-4.196838766294,-1.4360324910925));
#12145=CARTESIAN_POINT('Ctrl Pts',(90.2334727330767,-4.15039594311375,-1.56038459183445));
#12146=CARTESIAN_POINT('Ctrl Pts',(90.238510241917,-4.10758487684942,-1.67501255069715));
#12147=CARTESIAN_POINT('Ctrl Pts',(90.2436034111239,-4.06003122346315,-1.78775984788406));
#12148=CARTESIAN_POINT('Ctrl Pts',(90.2488311501934,-4.00789342145565,-1.89821015136766));
#12149=CARTESIAN_POINT('Ctrl Pts',(90.2492864425789,-4.00335265460874,-1.90782944978414));
#12150=CARTESIAN_POINT('Ctrl Pts',(90.2497427556707,-3.99877711660143,-1.91743135832675));
#12151=CARTESIAN_POINT('Ctrl Pts',(90.2502001415952,-3.99416691131452,-1.92701562069959));
#12152=CARTESIAN_POINT('Ctrl Pts',(90.2543767125297,-3.95206931195706,-2.01453329342759));
#12153=CARTESIAN_POINT('Ctrl Pts',(90.2586431109681,-3.90708214149884,-2.10057634447874));
#12154=CARTESIAN_POINT('Ctrl Pts',(90.2630407733878,-3.85930451175408,-2.1849389832888));
#12155=CARTESIAN_POINT('Ctrl Pts',(90.2630430193588,-3.85928011079705,-2.18498206891559));
#12156=CARTESIAN_POINT('Ctrl Pts',(90.263045265364,-3.85925570911223,-2.18502515410467));
#12157=CARTESIAN_POINT('Ctrl Pts',(90.2630475114035,-3.85923130669968,-2.18506823885598));
#12158=CARTESIAN_POINT('Ctrl Pts',(90.2681680836276,-3.80359812841056,-2.28329384034211));
#12159=CARTESIAN_POINT('Ctrl Pts',(90.2734765479204,-3.74402771634766,-2.37949948803224));
#12160=CARTESIAN_POINT('Ctrl Pts',(90.2788975726521,-3.68072380227128,-2.47336583383366));
#12161=CARTESIAN_POINT('Ctrl Pts',(90.2794264372809,-3.67454799554213,-2.48252325195699));
#12162=CARTESIAN_POINT('Ctrl Pts',(90.2799563732119,-3.66833669354543,-2.49165839202724));
#12163=CARTESIAN_POINT('Ctrl Pts',(90.2804873104987,-3.66209011058952,-2.50077094920276));
#12164=CARTESIAN_POINT('Ctrl Pts',(90.286453103996,-3.59190136154591,-2.6031627677783));
#12165=CARTESIAN_POINT('Ctrl Pts',(90.2925448128886,-3.51725277362374,-2.70270561453334));
#12166=CARTESIAN_POINT('Ctrl Pts',(90.2986730318616,-3.4384478477376,-2.79901488110601));
#12167=CARTESIAN_POINT('Ctrl Pts',(90.3047953212409,-3.35971917258546,-2.89523095994728));
#12168=CARTESIAN_POINT('Ctrl Pts',(90.3109537094259,-3.27684247910983,-2.98821992204621));
#12169=CARTESIAN_POINT('Ctrl Pts',(90.3170752134955,-3.19014680520275,-3.0776320499727));
#12170=CARTESIAN_POINT('Ctrl Pts',(90.3215723695297,-3.12645592652094,-3.14331856852439));
#12171=CARTESIAN_POINT('Ctrl Pts',(90.3260495078073,-3.06070174567111,-3.20707679023385));
#12172=CARTESIAN_POINT('Ctrl Pts',(90.330383628066,-2.99291157132991,-3.26864370849903));
#12173=CARTESIAN_POINT('Ctrl Pts',(90.3319451500303,-2.96848773445356,-3.29082539461065));
#12174=CARTESIAN_POINT('Ctrl Pts',(90.3334881074185,-2.94379998517365,-3.3127223158421));
#12175=CARTESIAN_POINT('Ctrl Pts',(90.3350067478521,-2.91885090253306,-3.33432114308619));
#12176=CARTESIAN_POINT('Ctrl Pts',(90.3399047748643,-2.83838334879142,-3.40398321511733));
#12177=CARTESIAN_POINT('Ctrl Pts',(90.3446814655348,-2.75535080696006,-3.47071309838439));
#12178=CARTESIAN_POINT('Ctrl Pts',(90.349439212882,-2.67011784007389,-3.53449765480226));
#12179=CARTESIAN_POINT('Ctrl Pts',(90.3502490910346,-2.6556092264956,-3.54535525503769));
#12180=CARTESIAN_POINT('Ctrl Pts',(90.3510584202878,-2.64103675453277,-3.55612758341785));
#12181=CARTESIAN_POINT('Ctrl Pts',(90.351867705681,-2.62640209807326,-3.5668146597885));
#12182=CARTESIAN_POINT('Ctrl Pts',(90.3597037234976,-2.48470001160771,-3.67029375573646));
#12183=CARTESIAN_POINT('Ctrl Pts',(90.3675357087112,-2.33716889767475,-3.76578490968642));
#12184=CARTESIAN_POINT('Ctrl Pts',(90.3753689217696,-2.18480170157244,-3.85268100517606));
#12185=CARTESIAN_POINT('Ctrl Pts',(90.3786586312147,-2.12081214832146,-3.88917470245394));
#12186=CARTESIAN_POINT('Ctrl Pts',(90.3819485489868,-2.0559694098737,-3.92415183380878));
#12187=CARTESIAN_POINT('Ctrl Pts',(90.3852390350962,-1.99034626550601,-3.95756476271203));
#12188=CARTESIAN_POINT('Ctrl Pts',(90.3892655267015,-1.910044744358,-3.99845138956899));
#12189=CARTESIAN_POINT('Ctrl Pts',(90.3932928919654,-1.82857022065426,-4.03699774700701));
#12190=CARTESIAN_POINT('Ctrl Pts',(90.397199183523,-1.74598958993834,-4.07291147552513));
#12191=CARTESIAN_POINT('Ctrl Pts',(90.3986951560361,-1.7143641078544,-4.08666517258424));
#12192=CARTESIAN_POINT('Ctrl Pts',(90.4001733716245,-1.68257689504952,-4.10003253309289));
#12193=CARTESIAN_POINT('Ctrl Pts',(90.401626980939,-1.6506335816544,-4.11299636490675));
#12194=CARTESIAN_POINT('Ctrl Pts',(90.4060004509793,-1.55452582923043,-4.15200060729765));
#12195=CARTESIAN_POINT('Ctrl Pts',(90.4102366354247,-1.45706409460434,-4.18748717072495));
#12196=CARTESIAN_POINT('Ctrl Pts',(90.4144432581645,-1.35857177087372,-4.2194740926336));
#12197=CARTESIAN_POINT('Ctrl Pts',(90.4152883106816,-1.33878602082146,-4.22589982428307));
#12198=CARTESIAN_POINT('Ctrl Pts',(90.4161321702282,-1.31895852969768,-4.23218440060831));
#12199=CARTESIAN_POINT('Ctrl Pts',(90.416975710102,-1.29909168785376,-4.238328071728));
#12200=CARTESIAN_POINT('Ctrl Pts',(90.4220255776036,-1.18015846121885,-4.27510727575999));
#12201=CARTESIAN_POINT('Ctrl Pts',(90.4270643029064,-1.05981722550044,-4.30683500699945));
#12202=CARTESIAN_POINT('Ctrl Pts',(90.4321674075888,-0.938541675499302,
-4.33338727789315));
#12203=CARTESIAN_POINT('Ctrl Pts',(90.4350118798256,-0.870942643839946,
-4.34818752246638));
#12204=CARTESIAN_POINT('Ctrl Pts',(90.4378766204331,-0.803053670559433,
-4.36138050238944));
#12205=CARTESIAN_POINT('Ctrl Pts',(90.4407762354097,-0.734959324739651,
-4.37295071025681));
#12206=CARTESIAN_POINT('',(90.4430005297901,-3.92880598357857,-2.05328335682078));
#12207=CARTESIAN_POINT('Origin',(90.4430005297901,0.,0.));
#12208=CARTESIAN_POINT('',(90.3466277144114,-4.43267344052904,-0.00114624657387179));
#12209=CARTESIAN_POINT('Ctrl Pts',(90.44300052979,-3.92880598357866,-2.05328335682061));
#12210=CARTESIAN_POINT('Ctrl Pts',(90.4401546791341,-3.95817780288558,-1.9970825508976));
#12211=CARTESIAN_POINT('Ctrl Pts',(90.4372863887623,-3.98633994636562,-1.94025870731795));
#12212=CARTESIAN_POINT('Ctrl Pts',(90.4289966894566,-4.06376532669901,-1.77522750359804));
#12213=CARTESIAN_POINT('Ctrl Pts',(90.4235406572539,-4.10990743027711,-1.66561748571758));
#12214=CARTESIAN_POINT('Ctrl Pts',(90.4101039791726,-4.21234597660604,-1.39199840839599));
#12215=CARTESIAN_POINT('Ctrl Pts',(90.4021252561662,-4.26353658600981,-1.22628504654762));
#12216=CARTESIAN_POINT('Ctrl Pts',(90.3864480400268,-4.34544435073715,-0.893010766269091));
#12217=CARTESIAN_POINT('Ctrl Pts',(90.3787599890444,-4.37647550152217,-0.725823258773799));
#12218=CARTESIAN_POINT('Ctrl Pts',(90.3628263225225,-4.42120597826071,-0.37281819892494));
#12219=CARTESIAN_POINT('Ctrl Pts',(90.3546129001533,-4.4329514196714,-0.187081780487825));
#12220=CARTESIAN_POINT('Ctrl Pts',(90.3464395730826,-4.432999849613,-0.00115469958862167));
#12221=CARTESIAN_POINT('',(89.0991895136418,-4.43415067741399,0.00275531766146416));
#12222=CARTESIAN_POINT('Ctrl Pts',(90.3466277144115,-4.43267344052904,-0.00114624657387175));
#12223=CARTESIAN_POINT('Ctrl Pts',(90.3459760545727,-4.43268280628598,0.0136036900692794));
#12224=CARTESIAN_POINT('Ctrl Pts',(90.3453245604975,-4.43261864583851,0.028354689417639));
#12225=CARTESIAN_POINT('Ctrl Pts',(90.3446731946637,-4.43248090953104,0.0431060695119233));
#12226=CARTESIAN_POINT('Ctrl Pts',(90.344672848187,-4.43248083626586,0.0431139161172652));
#12227=CARTESIAN_POINT('Ctrl Pts',(90.3446725017102,-4.43248076297986,0.0431217627225287));
#12228=CARTESIAN_POINT('Ctrl Pts',(90.3446721552336,-4.43248068967303,0.0431296093277615));
#12229=CARTESIAN_POINT('Ctrl Pts',(90.3389921652848,-4.43127892899438,0.171763487653303));
#12230=CARTESIAN_POINT('Ctrl Pts',(90.3333254577855,-4.42448064780808,0.300383748035732));
#12231=CARTESIAN_POINT('Ctrl Pts',(90.3276943091825,-4.41211904933905,0.428480496774987));
#12232=CARTESIAN_POINT('Ctrl Pts',(90.322063328146,-4.39975781871486,0.556573433731334));
#12233=CARTESIAN_POINT('Ctrl Pts',(90.3164678949856,-4.38183358365999,0.68414293178754));
#12234=CARTESIAN_POINT('Ctrl Pts',(90.3109043007945,-4.35841557100791,0.810682913480534));
#12235=CARTESIAN_POINT('Ctrl Pts',(90.3053380135185,-4.3349862227533,0.937284147464959));
#12236=CARTESIAN_POINT('Ctrl Pts',(90.2998034946352,-4.30605764424883,1.06285486888758));
#12237=CARTESIAN_POINT('Ctrl Pts',(90.294271839873,-4.27173637083049,1.18689170676658));
#12238=CARTESIAN_POINT('Ctrl Pts',(90.2887388252984,-4.237406660426,1.31095903585345));
#12239=CARTESIAN_POINT('Ctrl Pts',(90.2832084659097,-4.19768136407558,1.43349166454669));
#12240=CARTESIAN_POINT('Ctrl Pts',(90.2776289597445,-4.1527071038058,1.55398972719301));
#12241=CARTESIAN_POINT('Ctrl Pts',(90.2720441535644,-4.10769012214737,1.6746022518568));
#12242=CARTESIAN_POINT('Ctrl Pts',(90.266409763153,-4.05741385183719,1.79317617249455));
#12243=CARTESIAN_POINT('Ctrl Pts',(90.2606550472161,-4.00206984023319,1.9092157782696));
#12244=CARTESIAN_POINT('Ctrl Pts',(90.2569210652864,-3.96615954656902,1.98450877202425));
#12245=CARTESIAN_POINT('Ctrl Pts',(90.2531360399043,-3.92811657238451,2.05873488702302));
#12246=CARTESIAN_POINT('Ctrl Pts',(90.2492776676841,-3.88800440969381,2.1317606826182));
#12247=CARTESIAN_POINT('Ctrl Pts',(90.2492763279321,-3.88799048144944,2.13178603954383));
#12248=CARTESIAN_POINT('Ctrl Pts',(90.2492749881712,-3.88797655295561,2.13181139632481));
#12249=CARTESIAN_POINT('Ctrl Pts',(90.2492736484015,-3.88796262421228,2.13183675296122));
#12250=CARTESIAN_POINT('Ctrl Pts',(90.2437698354437,-3.83074294134805,2.23600255309212));
#12251=CARTESIAN_POINT('Ctrl Pts',(90.2381095631735,-3.76920679329261,2.33790767168564));
#12252=CARTESIAN_POINT('Ctrl Pts',(90.2323689587691,-3.70358949296031,2.4372061160339));
#12253=CARTESIAN_POINT('Ctrl Pts',(90.2319061972759,-3.69829995239287,2.4452107603427));
#12254=CARTESIAN_POINT('Ctrl Pts',(90.2314429137612,-3.69298391719379,2.45319845497206));
#12255=CARTESIAN_POINT('Ctrl Pts',(90.2309791481032,-3.68764152432475,2.46116901329943));
#12256=CARTESIAN_POINT('Ctrl Pts',(90.2247676729956,-3.6160878425176,2.56792319786844));
#12257=CARTESIAN_POINT('Ctrl Pts',(90.2184702026454,-3.53980092786857,2.67160582658075));
#12258=CARTESIAN_POINT('Ctrl Pts',(90.2121706056719,-3.45910916386875,2.77181810402713));
#12259=CARTESIAN_POINT('Ctrl Pts',(90.2079905892352,-3.40556718312877,2.83831267005192));
#12260=CARTESIAN_POINT('Ctrl Pts',(90.2038097784381,-3.3500840281035,2.90328168903946));
#12261=CARTESIAN_POINT('Ctrl Pts',(90.1997593752413,-3.29262497090729,2.96648169062228));
#12262=CARTESIAN_POINT('Ctrl Pts',(90.1977093955917,-3.26354394064544,2.99846831289321));
#12263=CARTESIAN_POINT('Ctrl Pts',(90.1956928204815,-3.2339573432479,3.03000119100896));
#12264=CARTESIAN_POINT('Ctrl Pts',(90.1937266595148,-3.20386440940588,3.06104529690031));
#12265=CARTESIAN_POINT('Ctrl Pts',(90.1876561158611,-3.11095214451587,3.15689431597545));
#12266=CARTESIAN_POINT('Ctrl Pts',(90.1816787366797,-3.01370303685225,3.24854285841778));
#12267=CARTESIAN_POINT('Ctrl Pts',(90.1757040350591,-2.9126910429949,3.33581269637835));
#12268=CARTESIAN_POINT('Ctrl Pts',(90.1681125337462,-2.78434443546821,3.44669841612231));
#12269=CARTESIAN_POINT('Ctrl Pts',(90.1605253070486,-2.6499183111191,3.55052330344395));
#12270=CARTESIAN_POINT('Ctrl Pts',(90.1529375359557,-2.51027349497431,3.64673662984613));
#12271=CARTESIAN_POINT('Ctrl Pts',(90.1455402580452,-2.37413450222593,3.74053449293175));
#12272=CARTESIAN_POINT('Ctrl Pts',(90.1381422793008,-2.23303135047545,3.82710087663271));
#12273=CARTESIAN_POINT('Ctrl Pts',(90.1307390996494,-2.08773673855552,3.90588875544471));
#12274=CARTESIAN_POINT('Ctrl Pts',(90.1284590629084,-2.04298879658348,3.93015390459643));
#12275=CARTESIAN_POINT('Ctrl Pts',(90.1261785467046,-1.99784343142811,3.95368080944968));
#12276=CARTESIAN_POINT('Ctrl Pts',(90.1238974385569,-1.95232333151512,3.97645254663137));
#12277=CARTESIAN_POINT('Ctrl Pts',(90.120288095957,-1.88029797141564,4.01248371909665));
#12278=CARTESIAN_POINT('Ctrl Pts',(90.116677252201,-1.80733007453952,4.04662617558732));
#12279=CARTESIAN_POINT('Ctrl Pts',(90.1132013108187,-1.73343462572613,4.0785860963781));
#12280=CARTESIAN_POINT('Ctrl Pts',(90.111124500852,-1.68928347709965,4.0976815513159));
#12281=CARTESIAN_POINT('Ctrl Pts',(90.1090958488609,-1.64480210839157,4.11599744313679));
#12282=CARTESIAN_POINT('Ctrl Pts',(90.1071444485185,-1.60000201691604,4.13346793574427));
#12283=CARTESIAN_POINT('Ctrl Pts',(90.1019203393616,-1.48006734076534,4.18023832848366));
#12284=CARTESIAN_POINT('Ctrl Pts',(90.0967384730707,-1.35817365721744,4.22177250611973));
#12285=CARTESIAN_POINT('Ctrl Pts',(90.0915271953053,-1.23480490907399,4.25789063602616));
#12286=CARTESIAN_POINT('Ctrl Pts',(90.0863120059555,-1.11134356036681,4.29403587619543));
#12287=CARTESIAN_POINT('Ctrl Pts',(90.0810669370124,-0.986404860549503,
4.32475649417719));
#12288=CARTESIAN_POINT('Ctrl Pts',(90.0757071653272,-0.86049691958104,4.34991189709947));
#12289=CARTESIAN_POINT('Ctrl Pts',(90.0708892919712,-0.74731886840151,4.37252396951906));
#12290=CARTESIAN_POINT('Ctrl Pts',(90.0659782570646,-0.633356997208761,
4.39063952015416));
#12291=CARTESIAN_POINT('Ctrl Pts',(90.0609079765421,-0.518999354946138,
4.40418981303012));
#12292=CARTESIAN_POINT('Ctrl Pts',(90.0603292350039,-0.50594612889639,4.40573649615903));
#12293=CARTESIAN_POINT('Ctrl Pts',(90.059748418682,-0.492887707095587,4.40722373908085));
#12294=CARTESIAN_POINT('Ctrl Pts',(90.0591654292988,-0.479824635580856,
4.40865146974588));
#12295=CARTESIAN_POINT('Ctrl Pts',(90.0577243294216,-0.44753384041861,4.41218069779911));
#12296=CARTESIAN_POINT('Ctrl Pts',(90.0562699471261,-0.415215046300762,
4.41534625760791));
#12297=CARTESIAN_POINT('Ctrl Pts',(90.0548008128143,-0.382877139566811,
4.41814722958272));
#12298=CARTESIAN_POINT('Ctrl Pts',(90.054798789602,-0.382832605550807,4.41815108692982));
#12299=CARTESIAN_POINT('Ctrl Pts',(90.0547967663617,-0.382788071498567,
4.41815494358551));
#12300=CARTESIAN_POINT('Ctrl Pts',(90.0547947430934,-0.382743537410013,
4.41815879954982));
#12301=CARTESIAN_POINT('Ctrl Pts',(90.0496438568243,-0.269367556159388,
4.42797540860405));
#12302=CARTESIAN_POINT('Ctrl Pts',(90.0443007339449,-0.155424616051288,
4.43333011903269));
#12303=CARTESIAN_POINT('Ctrl Pts',(90.0388435098811,-0.0412975804935338,
4.43421162112182));
#12304=CARTESIAN_POINT('Ctrl Pts',(90.0382961246298,-0.0298501018289632,
4.43430003992907));
#12305=CARTESIAN_POINT('Ctrl Pts',(90.0377475914027,-0.0184008069736915,
4.43434347760861));
#12306=CARTESIAN_POINT('Ctrl Pts',(90.0371979890515,-0.00695010601547379,
4.43434193920902));
#12307=CARTESIAN_POINT('Ctrl Pts',(90.0311772445115,0.118489214107905,4.43432508645914));
#12308=CARTESIAN_POINT('Ctrl Pts',(90.0250287201998,0.244102444284032,4.42890783060357));
#12309=CARTESIAN_POINT('Ctrl Pts',(90.0188450467448,0.369392047656091,4.41812376066608));
#12310=CARTESIAN_POINT('Ctrl Pts',(90.0126681507393,0.494544330717774,4.40735151031929));
#12311=CARTESIAN_POINT('Ctrl Pts',(90.006456522929,0.619373750359978,4.39122455526414));
#12312=CARTESIAN_POINT('Ctrl Pts',(90.000285056382,0.743397398104673,4.36981636870766));
#12313=CARTESIAN_POINT('Ctrl Pts',(89.9959935887821,0.82964002161633,4.35492970631035));
#12314=CARTESIAN_POINT('Ctrl Pts',(89.9917216379227,0.915496123635736,4.3374886777928));
#12315=CARTESIAN_POINT('Ctrl Pts',(89.9875975120029,1.00075473745206,4.31734639597503));
#12316=CARTESIAN_POINT('Ctrl Pts',(89.9857957713041,1.03800236699153,4.30854667219763));
#12317=CARTESIAN_POINT('Ctrl Pts',(89.9840222448516,1.0751353056168,4.29923153576687));
#12318=CARTESIAN_POINT('Ctrl Pts',(89.9822876314567,1.11213296432513,4.28938962248299));
#12319=CARTESIAN_POINT('Ctrl Pts',(89.9765854089283,1.23375596320608,4.25703614255743));
#12320=CARTESIAN_POINT('Ctrl Pts',(89.9709595043935,1.35406248890358,4.21956869603409));
#12321=CARTESIAN_POINT('Ctrl Pts',(89.9653350664398,1.47267873857721,4.17729808545643));
#12322=CARTESIAN_POINT('Ctrl Pts',(89.9578181933815,1.63120538582459,4.12080482934344));
#12323=CARTESIAN_POINT('Ctrl Pts',(89.9503038612709,1.78672211242187,4.05573225669743));
#12324=CARTESIAN_POINT('Ctrl Pts',(89.9427866730361,1.93829788308465,3.98247424239128));
#12325=CARTESIAN_POINT('Ctrl Pts',(89.9390572458216,2.01349765013797,3.9461294784061));
#12326=CARTESIAN_POINT('Ctrl Pts',(89.9353271292559,2.087726831229,3.90776935015616));
#12327=CARTESIAN_POINT('Ctrl Pts',(89.9315957262388,2.16086825554478,3.86743854561077));
#12328=CARTESIAN_POINT('Ctrl Pts',(89.9278649168943,2.23399804293748,3.8271141577639));
#12329=CARTESIAN_POINT('Ctrl Pts',(89.9241328014689,2.30604442307921,3.78481713282482));
#12330=CARTESIAN_POINT('Ctrl Pts',(89.9205306438533,2.376750530202,3.7404077105897));
#12331=CARTESIAN_POINT('Ctrl Pts',(89.9186992771012,2.41269810040138,3.71782959268345));
#12332=CARTESIAN_POINT('Ctrl Pts',(89.9169015017109,2.44829851603235,3.69470588076957));
#12333=CARTESIAN_POINT('Ctrl Pts',(89.9151545674447,2.48351371273066,3.67102106409027));
#12334=CARTESIAN_POINT('Ctrl Pts',(89.909966158297,2.58810313674178,3.60067696362935));
#12335=CARTESIAN_POINT('Ctrl Pts',(89.9048786606799,2.68962634065957,3.52588468656838));
#12336=CARTESIAN_POINT('Ctrl Pts',(89.8997947770881,2.78770740362052,3.44697707147542));
#12337=CARTESIAN_POINT('Ctrl Pts',(89.894707958871,2.88584508297904,3.36802390768252));
#12338=CARTESIAN_POINT('Ctrl Pts',(89.8896244151715,2.98053775781111,3.28494948472798));
#12339=CARTESIAN_POINT('Ctrl Pts',(89.8844647479072,3.07139943366342,3.19807491930894));
#12340=CARTESIAN_POINT('Ctrl Pts',(89.8796601096812,3.15600905260015,3.11717806366051));
#12341=CARTESIAN_POINT('Ctrl Pts',(89.8747890322157,3.23729699614213,3.03298564457149));
#12342=CARTESIAN_POINT('Ctrl Pts',(89.8697792690141,3.3149702118713,2.94579257164261));
#12343=CARTESIAN_POINT('Ctrl Pts',(89.8694011092043,3.32083334098665,2.93921084022147));
#12344=CARTESIAN_POINT('Ctrl Pts',(89.8690221591742,3.32667589746338,2.93261200491482));
#12345=CARTESIAN_POINT('Ctrl Pts',(89.8686423878504,3.33249776686566,2.92599618919944));
#12346=CARTESIAN_POINT('Ctrl Pts',(89.8656595065444,3.37822514098612,2.87403283182651));
#12347=CARTESIAN_POINT('Ctrl Pts',(89.8626258184445,3.4226750807397,2.82102318451257));
#12348=CARTESIAN_POINT('Ctrl Pts',(89.8595259106998,3.46579114681716,2.76703463778351));
#12349=CARTESIAN_POINT('Ctrl Pts',(89.8595237212501,3.46582159948368,2.76699650593709));
#12350=CARTESIAN_POINT('Ctrl Pts',(89.8595215317674,3.46585205148511,2.76695837360231));
#12351=CARTESIAN_POINT('Ctrl Pts',(89.8595193422516,3.46588250282147,2.76692024077916));
#12352=CARTESIAN_POINT('Ctrl Pts',(89.8543692890127,3.53750838798797,2.67722640338861));
#12353=CARTESIAN_POINT('Ctrl Pts',(89.8490257750254,3.60565138707983,2.58456934156202));
#12354=CARTESIAN_POINT('Ctrl Pts',(89.8435650967696,3.67009301325766,2.48926904948137));
#12355=CARTESIAN_POINT('Ctrl Pts',(89.8429876971703,3.67690692306713,2.47919221508768));
#12356=CARTESIAN_POINT('Ctrl Pts',(89.8424089876202,3.68367945113089,2.46908587614747));
#12357=CARTESIAN_POINT('Ctrl Pts',(89.8418290583168,3.69041034074978,2.45895044489462));
#12358=CARTESIAN_POINT('Ctrl Pts',(89.8357717864202,3.76071344199256,2.35308743274409));
#12359=CARTESIAN_POINT('Ctrl Pts',(89.8295819965756,3.82647422612893,2.2440445425874));
#12360=CARTESIAN_POINT('Ctrl Pts',(89.8233520562633,3.88744639021242,2.1322702560433));
#12361=CARTESIAN_POINT('Ctrl Pts',(89.8171280486777,3.94836049094936,2.02060241133594));
#12362=CARTESIAN_POINT('Ctrl Pts',(89.8108643291039,4.00449544456473,1.90620852481146));
#12363=CARTESIAN_POINT('Ctrl Pts',(89.8046358010831,4.05564734243885,1.78954584458124));
#12364=CARTESIAN_POINT('Ctrl Pts',(89.7986575819535,4.10474357406174,1.67757154434262));
#12365=CARTESIAN_POINT('Ctrl Pts',(89.7927121698193,4.14924971933642,1.56350533409205));
#12366=CARTESIAN_POINT('Ctrl Pts',(89.7868942478997,4.18893902239296,1.44773755178359));
#12367=CARTESIAN_POINT('Ctrl Pts',(89.786341412979,4.19271040898246,1.43673697913376));
#12368=CARTESIAN_POINT('Ctrl Pts',(89.7857897292086,4.19643829007812,1.42572107921797));
#12369=CARTESIAN_POINT('Ctrl Pts',(89.7852392778258,4.20012246378047,1.41469021034695));
#12370=CARTESIAN_POINT('Ctrl Pts',(89.7809239099003,4.22900524166714,1.32821162349435));
#12371=CARTESIAN_POINT('Ctrl Pts',(89.7767787296868,4.25504566299023,1.24076433038674));
#12372=CARTESIAN_POINT('Ctrl Pts',(89.7726824676602,4.27841042913659,1.15260502021653));
#12373=CARTESIAN_POINT('Ctrl Pts',(89.7710559962329,4.28768769809445,1.11760027732866));
#12374=CARTESIAN_POINT('Ctrl Pts',(89.7694372371741,4.29654329660154,1.08248272629045));
#12375=CARTESIAN_POINT('Ctrl Pts',(89.76781859898,4.30498822491254,1.04726622783332));
#12376=CARTESIAN_POINT('Ctrl Pts',(89.762124261694,4.33469731638056,0.923375279880136));
#12377=CARTESIAN_POINT('Ctrl Pts',(89.7564313736596,4.35932573440998,0.798257745962767));
#12378=CARTESIAN_POINT('Ctrl Pts',(89.7507376434564,4.37879903795454,0.67234307589075));
#12379=CARTESIAN_POINT('Ctrl Pts',(89.745043485553,4.39827380428987,0.546418947391886));
#12380=CARTESIAN_POINT('Ctrl Pts',(89.7393484389035,4.41259273882384,0.419696198040109));
#12381=CARTESIAN_POINT('Ctrl Pts',(89.7336518270546,4.42166204872297,0.292608380861909));
#12382=CARTESIAN_POINT('Ctrl Pts',(89.7295357695024,4.42821503188084,0.200781733101244));
#12383=CARTESIAN_POINT('Ctrl Pts',(89.7256197692987,4.43167936859243,0.10874537863679));
#12384=CARTESIAN_POINT('Ctrl Pts',(89.7217806440399,4.43222774455031,0.01672425278658));
#12385=CARTESIAN_POINT('Ctrl Pts',(89.7203048537282,4.43243854463399,-0.0186494005462728));
#12386=CARTESIAN_POINT('Ctrl Pts',(89.7188404231871,4.43221850992994,-0.0540213489622811));
#12387=CARTESIAN_POINT('Ctrl Pts',(89.7173803551925,4.43157755931919,-0.0893808614021613));
#12388=CARTESIAN_POINT('Ctrl Pts',(89.7121165382498,4.4292668130411,-0.216858486659978));
#12389=CARTESIAN_POINT('Ctrl Pts',(89.706909188104,4.42148516166803,-0.344173750615162));
#12390=CARTESIAN_POINT('Ctrl Pts',(89.7016933708314,4.40824775351063,-0.47082209257879));
#12391=CARTESIAN_POINT('Ctrl Pts',(89.6964743766283,4.39500228250815,-0.597547575471347));
#12392=CARTESIAN_POINT('Ctrl Pts',(89.6912465347313,4.37629401782769,-0.723605202379522));
#12393=CARTESIAN_POINT('Ctrl Pts',(89.6859288490779,4.35218306602042,-0.848483653270712));
#12394=CARTESIAN_POINT('Ctrl Pts',(89.6810303022826,4.3299725343339,-0.963519211080887));
#12395=CARTESIAN_POINT('Ctrl Pts',(89.6760550647583,4.30317726307267,-1.07755466769261));
#12396=CARTESIAN_POINT('Ctrl Pts',(89.6709326451315,4.27188377187853,-1.19018586613403));
#12397=CARTESIAN_POINT('Ctrl Pts',(89.6704866500888,4.26915913333694,-1.19999235599975));
#12398=CARTESIAN_POINT('Ctrl Pts',(89.6700395393016,4.26640040577432,-1.20978823152006));
#12399=CARTESIAN_POINT('Ctrl Pts',(89.6695912662433,4.2636076520595,-1.21957324377747));
#12400=CARTESIAN_POINT('Ctrl Pts',(89.6675923262973,4.25115420017972,-1.26320658625381));
#12401=CARTESIAN_POINT('Ctrl Pts',(89.6655702300742,4.23802442648274,-1.30662318331853));
#12402=CARTESIAN_POINT('Ctrl Pts',(89.6635207911676,4.22422522690175,-1.34979954849863));
#12403=CARTESIAN_POINT('Ctrl Pts',(89.6635188497135,4.22421215478146,-1.34984044990279));
#12404=CARTESIAN_POINT('Ctrl Pts',(89.6635169082349,4.22419908206048,-1.34988135109147));
#12405=CARTESIAN_POINT('Ctrl Pts',(89.6635149667318,4.22418600873881,-1.34992225206465));
#12406=CARTESIAN_POINT('Ctrl Pts',(89.6583048644347,4.18910322043729,-1.45968167056365));
#12407=CARTESIAN_POINT('Ctrl Pts',(89.6529079930652,4.14959267157002,-1.56817878203137));
#12408=CARTESIAN_POINT('Ctrl Pts',(89.6474012560416,4.1058005181601,-1.67505030023803));
#12409=CARTESIAN_POINT('Ctrl Pts',(89.6468528707784,4.1014395015599,-1.685693039375));
#12410=CARTESIAN_POINT('Ctrl Pts',(89.6463033959711,4.097036059829,-1.69631963423943));
#12411=CARTESIAN_POINT('Ctrl Pts',(89.6457529075683,4.0925903612991,-1.70692971118167));
#12412=CARTESIAN_POINT('Ctrl Pts',(89.6396818443409,4.04356095990179,-1.82394298092083));
#12413=CARTESIAN_POINT('Ctrl Pts',(89.6334880310768,3.98938717627061,-1.93895075589036));
#12414=CARTESIAN_POINT('Ctrl Pts',(89.6272624154904,3.93030319386788,-2.05150138426143));
#12415=CARTESIAN_POINT('Ctrl Pts',(89.6210427178731,3.87127537573925,-2.16394502383309));
#12416=CARTESIAN_POINT('Ctrl Pts',(89.6147916260043,3.8073470026313,-2.27393638612393));
#12417=CARTESIAN_POINT('Ctrl Pts',(89.6085823649858,3.73878303508661,-2.38105355206892));
#12418=CARTESIAN_POINT('Ctrl Pts',(89.6041348249192,3.6896723612287,-2.45777892823504));
#12419=CARTESIAN_POINT('Ctrl Pts',(89.5997088512995,3.63818159748146,-2.5330322726376));
#12420=CARTESIAN_POINT('Ctrl Pts',(89.5954279326346,3.58427791445395,-2.60655391409357));
#12421=CARTESIAN_POINT('Ctrl Pts',(89.5937364158637,3.56297898518335,-2.63560447526638));
#12422=CARTESIAN_POINT('Ctrl Pts',(89.5920675461215,3.5413036738783,-2.66438421010478));
#12423=CARTESIAN_POINT('Ctrl Pts',(89.5904289414706,3.51925137591093,-2.6928753608655));
#12424=CARTESIAN_POINT('Ctrl Pts',(89.5846453544389,3.44141601490496,-2.79343717116831));
#12425=CARTESIAN_POINT('Ctrl Pts',(89.5789579691856,3.35927397910321,-2.89069572507703));
#12426=CARTESIAN_POINT('Ctrl Pts',(89.5732719335314,3.27329233069242,-2.98443916131024));
#12427=CARTESIAN_POINT('Ctrl Pts',(89.5657253493348,3.15917631233561,-3.1088567304979));
#12428=CARTESIAN_POINT('Ctrl Pts',(89.5581810590132,3.03829189927785,-3.22709219992152));
#12429=CARTESIAN_POINT('Ctrl Pts',(89.5506337359625,2.91136391121407,-3.33843728344095));
#12430=CARTESIAN_POINT('Ctrl Pts',(89.5468091382022,2.84704329109342,-3.39486128360517));
#12431=CARTESIAN_POINT('Ctrl Pts',(89.5429837790236,2.78117040080886,-3.44951501313159));
#12432=CARTESIAN_POINT('Ctrl Pts',(89.5391570428513,2.71383792200217,-3.50230130715213));
#12433=CARTESIAN_POINT('Ctrl Pts',(89.5342574925378,2.62762898237659,-3.56988608221051));
#12434=CARTESIAN_POINT('Ctrl Pts',(89.5294761247725,2.53889519243924,-3.63424724803423));
#12435=CARTESIAN_POINT('Ctrl Pts',(89.5249098565493,2.44779504547448,-3.69499323623541));
#12436=CARTESIAN_POINT('Ctrl Pts',(89.5241721915046,2.43307812769937,-3.70480654327509));
#12437=CARTESIAN_POINT('Ctrl Pts',(89.5234401399771,2.41829955003909,-3.71452544867758));
#12438=CARTESIAN_POINT('Ctrl Pts',(89.522714110562,2.40346009316782,-3.72414824077537));
#12439=CARTESIAN_POINT('Ctrl Pts',(89.5174882232391,2.2966471625415,-3.79341213861807));
#12440=CARTESIAN_POINT('Ctrl Pts',(89.5123205431825,2.18691980194012,-3.85806396624029));
#12441=CARTESIAN_POINT('Ctrl Pts',(89.5071461802061,2.07470347374617,-3.91783526245825));
#12442=CARTESIAN_POINT('Ctrl Pts',(89.5019686383418,1.96241820505896,-3.97764327938085));
#12443=CARTESIAN_POINT('Ctrl Pts',(89.4967840377611,1.84764079703562,-4.03256437854672));
#12444=CARTESIAN_POINT('Ctrl Pts',(89.4915114992318,1.73082731385916,-4.0823636412585));
#12445=CARTESIAN_POINT('Ctrl Pts',(89.4866513945994,1.62315133433679,-4.12826745515198));
#12446=CARTESIAN_POINT('Ctrl Pts',(89.4817161226339,1.51374484382532,-4.16981953397608));
#12447=CARTESIAN_POINT('Ctrl Pts',(89.4766351649714,1.40299072259745,-4.20686624248983));
#12448=CARTESIAN_POINT('Ctrl Pts',(89.4761960741052,1.3934194712202,-4.21006777897402));
#12449=CARTESIAN_POINT('Ctrl Pts',(89.4757558952248,1.38383813607468,-4.21323569409507));
#12450=CARTESIAN_POINT('Ctrl Pts',(89.4753145828178,1.37424695298452,-4.21636990312836));
#12451=CARTESIAN_POINT('Ctrl Pts',(89.4729470438029,1.32279247355333,-4.23318420984324));
#12452=CARTESIAN_POINT('Ctrl Pts',(89.4705468144635,1.2710556184954,-4.24902812032458));
#12453=CARTESIAN_POINT('Ctrl Pts',(89.4681067685567,1.21907612530969,-4.26388921464172));
#12454=CARTESIAN_POINT('Ctrl Pts',(89.4681047207161,1.21903250083773,-4.2639016870102));
#12455=CARTESIAN_POINT('Ctrl Pts',(89.4681026728475,1.21898887619474,-4.26391415868658));
#12456=CARTESIAN_POINT('Ctrl Pts',(89.4681006249508,1.21894525138081,-4.26392662967084));
#12457=CARTESIAN_POINT('Ctrl Pts',(89.4629203670265,1.1085940830698,-4.29547261369915));
#12458=CARTESIAN_POINT('Ctrl Pts',(89.4575502385208,0.99684079441647,-4.32266856133506));
#12459=CARTESIAN_POINT('Ctrl Pts',(89.4520672413171,0.884065361812501,-4.34543406395382));
#12460=CARTESIAN_POINT('Ctrl Pts',(89.4515107322709,0.872618967423584,-4.34774469948338));
#12461=CARTESIAN_POINT('Ctrl Pts',(89.4509530604866,0.8611620838353,-4.35000971158681));
#12462=CARTESIAN_POINT('Ctrl Pts',(89.4503943064768,0.849695135570088,-4.35222902864808));
#12463=CARTESIAN_POINT('Ctrl Pts',(89.4443379353231,0.72540413546552,-4.37628435101583));
#12464=CARTESIAN_POINT('Ctrl Pts',(89.4381549530938,0.599925051924999,-4.39496914330591));
#12465=CARTESIAN_POINT('Ctrl Pts',(89.4319370866374,0.473761887533089,-4.40822664556218));
#12466=CARTESIAN_POINT('Ctrl Pts',(89.4257253525158,0.347723150833167,-4.42147107268344));
#12467=CARTESIAN_POINT('Ctrl Pts',(89.4194791529364,0.221001690369546,-4.42929928245315));
#12468=CARTESIAN_POINT('Ctrl Pts',(89.4132725672592,0.0940938886779707,
-4.4316966952617));
#12469=CARTESIAN_POINT('Ctrl Pts',(89.4085779942434,-0.00189736517690565,
-4.43351006416758));
#12470=CARTESIAN_POINT('Ctrl Pts',(89.4039062033646,-0.0979982089428208,
-4.43221631699086));
#12471=CARTESIAN_POINT('Ctrl Pts',(89.3993747311469,-0.193980083124144,
-4.42766206395347));
#12472=CARTESIAN_POINT('Ctrl Pts',(89.3979196587155,-0.224800216698573,
-4.42619967651687));
#12473=CARTESIAN_POINT('Ctrl Pts',(89.3964790542012,-0.255607682421183,
-4.42440112899348));
#12474=CARTESIAN_POINT('Ctrl Pts',(89.3950568090295,-0.286393777394904,
-4.42226145416874));
#12475=CARTESIAN_POINT('Ctrl Pts',(89.3901348141735,-0.392935887093349,
-4.41485663487967));
#12476=CARTESIAN_POINT('Ctrl Pts',(89.3853357505001,-0.49922878422454,-4.40353431601429));
#12477=CARTESIAN_POINT('Ctrl Pts',(89.3805570394582,-0.605007279598262,
-4.38853760211599));
#12478=CARTESIAN_POINT('Ctrl Pts',(89.3796568223334,-0.624933910886723,
-4.38571251004663));
#12479=CARTESIAN_POINT('Ctrl Pts',(89.3787573274687,-0.644842433755186,
-4.38275699670061));
#12480=CARTESIAN_POINT('Ctrl Pts',(89.3778578691136,-0.664731277729952,
-4.37967264392692));
#12481=CARTESIAN_POINT('Ctrl Pts',(89.370312436378,-0.831576061088442,-4.35379843168113));
#12482=CARTESIAN_POINT('Ctrl Pts',(89.3627694916172,-0.997038937407362,
-4.3188612788562));
#12483=CARTESIAN_POINT('Ctrl Pts',(89.3552236782343,-1.16012719389742,-4.27507484043943));
#12484=CARTESIAN_POINT('Ctrl Pts',(89.3514222905434,-1.24228688421828,-4.25301635322521));
#12485=CARTESIAN_POINT('Ctrl Pts',(89.3476201903182,-1.32384343025632,-4.2287112733854));
#12486=CARTESIAN_POINT('Ctrl Pts',(89.3438167633393,-1.4046668649752,-4.20218277744718));
#12487=CARTESIAN_POINT('Ctrl Pts',(89.3388999276965,-1.50915041278619,-4.16788837529321));
#12488=CARTESIAN_POINT('Ctrl Pts',(89.3341006624582,-1.61234760269368,-4.12967926390135));
#12489=CARTESIAN_POINT('Ctrl Pts',(89.3295154930798,-1.71384201048532,-4.08747165098001));
#12490=CARTESIAN_POINT('Ctrl Pts',(89.328805309349,-1.72956218813386,-4.08093423490279));
#12491=CARTESIAN_POINT('Ctrl Pts',(89.3281002617829,-1.74524142451454,-4.07430093925114));
#12492=CARTESIAN_POINT('Ctrl Pts',(89.3274007090456,-1.76087807294772,-4.06757150451766));
#12493=CARTESIAN_POINT('Ctrl Pts',(89.3221790911871,-1.87759350889313,-4.01734150082212));
#12494=CARTESIAN_POINT('Ctrl Pts',(89.3170180067439,-1.99210299405547,-3.96214565755558));
#12495=CARTESIAN_POINT('Ctrl Pts',(89.3118532957462,-2.10394889892861,-3.90218784561099));
#12496=CARTESIAN_POINT('Ctrl Pts',(89.3066854717779,-2.21586221764339,-3.8421938947801));
#12497=CARTESIAN_POINT('Ctrl Pts',(89.3015136565798,-2.32510848812348,-3.77743193022012));
#12498=CARTESIAN_POINT('Ctrl Pts',(89.2962574801352,-2.43124102518457,-3.70814962596672));
#12499=CARTESIAN_POINT('Ctrl Pts',(89.2913965944474,-2.52939186464553,-3.6440776975029));
#12500=CARTESIAN_POINT('Ctrl Pts',(89.2864631150228,-2.62488007739734,-3.57613942144677));
#12501=CARTESIAN_POINT('Ctrl Pts',(89.2813859570345,-2.71736351929902,-3.50456902506535));
#12502=CARTESIAN_POINT('Ctrl Pts',(89.280965182924,-2.7250281691072,-3.49863756302613));
#12503=CARTESIAN_POINT('Ctrl Pts',(89.2805434219692,-2.73267221049811,-3.49268115218793));
#12504=CARTESIAN_POINT('Ctrl Pts',(89.2801206337067,-2.74029546476355,-3.48669992454199));
#12505=CARTESIAN_POINT('Ctrl Pts',(89.2776303505565,-2.78519751936587,-3.45146964086056));
#12506=CARTESIAN_POINT('Ctrl Pts',(89.2751043453965,-2.82937745257098,-3.41537913983434));
#12507=CARTESIAN_POINT('Ctrl Pts',(89.272534204999,-2.87279726675529,-3.37845914541868));
#12508=CARTESIAN_POINT('Ctrl Pts',(89.272532154234,-2.87283191226985,-3.37842968623679));
#12509=CARTESIAN_POINT('Ctrl Pts',(89.2725301034409,-2.87286655730067,-3.37840022652676));
#12510=CARTESIAN_POINT('Ctrl Pts',(89.2725280526196,-2.8729012018477,-3.37837076628866));
#12511=CARTESIAN_POINT('Ctrl Pts',(89.267394586954,-2.95962089722541,-3.3046280537393));
#12512=CARTESIAN_POINT('Ctrl Pts',(89.2620740500415,-3.04355784971649,-3.22735275435274));
#12513=CARTESIAN_POINT('Ctrl Pts',(89.2566412400769,-3.12443440269525,-3.14681070859945));
#12514=CARTESIAN_POINT('Ctrl Pts',(89.2561104809455,-3.13233564888054,-3.13894214214445));
#12515=CARTESIAN_POINT('Ctrl Pts',(89.2555786502419,-3.1402076796009,-3.13104243735842));
#12516=CARTESIAN_POINT('Ctrl Pts',(89.2550458177106,-3.14805023258091,-3.12311186850192));
#12517=CARTESIAN_POINT('Ctrl Pts',(89.2490662896212,-3.23606056055093,-3.03411381291612));
#12518=CARTESIAN_POINT('Ctrl Pts',(89.2429611108263,-3.3203597317995,-2.94122308399473));
#12519=CARTESIAN_POINT('Ctrl Pts',(89.2368189778671,-3.40062431570516,-2.84481744754777));
#12520=CARTESIAN_POINT('Ctrl Pts',(89.230524199038,-3.48288365571837,-2.74601591339912));
#12521=CARTESIAN_POINT('Ctrl Pts',(89.2241910551195,-3.56090549561551,-2.64352276011619));
#12522=CARTESIAN_POINT('Ctrl Pts',(89.2178971949538,-3.63438366563388,-2.53776568946566));
#12523=CARTESIAN_POINT('Ctrl Pts',(89.2130203306477,-3.69131900502992,-2.45581870154376));
#12524=CARTESIAN_POINT('Ctrl Pts',(89.2081671301908,-3.74552798451576,-2.37190969139733));
#12525=CARTESIAN_POINT('Ctrl Pts',(89.203450944175,-3.79675155356332,-2.2861754455767));
#12526=CARTESIAN_POINT('Ctrl Pts',(89.2022381243405,-3.80992426565039,-2.26412792805309));
#12527=CARTESIAN_POINT('Ctrl Pts',(89.2010343655256,-3.82289941671646,-2.24195993893644));
#12528=CARTESIAN_POINT('Ctrl Pts',(89.1998415954324,-3.83567234774371,-2.2196743013848));
#12529=CARTESIAN_POINT('Ctrl Pts',(89.1951763176034,-3.88563107178533,-2.13250855891273));
#12530=CARTESIAN_POINT('Ctrl Pts',(89.1906487149425,-3.93253987688793,-2.04357290095941));
#12531=CARTESIAN_POINT('Ctrl Pts',(89.1861496000012,-3.9764769173674,-1.95319328049147));
#12532=CARTESIAN_POINT('Ctrl Pts',(89.1850273570829,-3.98743641344001,-1.93064931565556));
#12533=CARTESIAN_POINT('Ctrl Pts',(89.183906886628,-3.99821112416203,-1.90801528272099));
#12534=CARTESIAN_POINT('Ctrl Pts',(89.1827864940954,-4.00880247330086,-1.88529578119841));
#12535=CARTESIAN_POINT('Ctrl Pts',(89.1748845966895,-4.08350107387963,-1.72505982378282));
#12536=CARTESIAN_POINT('Ctrl Pts',(89.1669864847308,-4.14908402662789,-1.5605718235667));
#12537=CARTESIAN_POINT('Ctrl Pts',(89.1590869820462,-4.20512713898647,-1.39293918911362));
#12538=CARTESIAN_POINT('Ctrl Pts',(89.1555023501855,-4.23055835081728,-1.31687094705638));
#12539=CARTESIAN_POINT('Ctrl Pts',(89.1519174478846,-4.25402437590823,-1.24015520149134));
#12540=CARTESIAN_POINT('Ctrl Pts',(89.148331846413,-4.2754819634251,-1.16289553034143));
#12541=CARTESIAN_POINT('Ctrl Pts',(89.1427150953485,-4.3090947138875,-1.04187027318577));
#12542=CARTESIAN_POINT('Ctrl Pts',(89.1372836934939,-4.33746672531892,-0.919420208707981));
#12543=CARTESIAN_POINT('Ctrl Pts',(89.1321181629932,-4.36026314630882,-0.796029961547062));
#12544=CARTESIAN_POINT('Ctrl Pts',(89.1269499946497,-4.38307120857622,-0.672576703613198));
#12545=CARTESIAN_POINT('Ctrl Pts',(89.1218422568243,-4.40064724792524,-0.548252281346481));
#12546=CARTESIAN_POINT('Ctrl Pts',(89.1167340340962,-4.41291781279323,-0.42354027505825));
#12547=CARTESIAN_POINT('Ctrl Pts',(89.1116198553237,-4.42520268479577,-0.298682858067726));
#12548=CARTESIAN_POINT('Ctrl Pts',(89.1065048462763,-4.43216934172322,-0.173437033166085));
#12549=CARTESIAN_POINT('Ctrl Pts',(89.1013127266966,-4.43378718263489,-0.0483001100602392));
#12550=CARTESIAN_POINT('Ctrl Pts',(89.1006065026572,-4.43400723884241,-0.0312791801777059));
#12551=CARTESIAN_POINT('Ctrl Pts',(89.0998988341112,-4.43412840683536,-0.0142602819635385));
#12552=CARTESIAN_POINT('Ctrl Pts',(89.0991895136419,-4.43415067741398,0.00275531765885942));
#12553=CARTESIAN_POINT('',(87.8465491621224,-4.4326266415555,-0.00371887732998788));
#12554=CARTESIAN_POINT('Ctrl Pts',(89.0991895136049,-4.43415067741516,0.002755318546424));
#12555=CARTESIAN_POINT('Ctrl Pts',(89.0940584661118,-4.43431177720561,0.125841925458626));
#12556=CARTESIAN_POINT('Ctrl Pts',(89.0888408531867,-4.42929579503223,0.248794764078206));
#12557=CARTESIAN_POINT('Ctrl Pts',(89.0834488483057,-4.41909585617478,0.371254491423685));
#12558=CARTESIAN_POINT('Ctrl Pts',(89.0812972309806,-4.41502568827878,0.420120632462279));
#12559=CARTESIAN_POINT('Ctrl Pts',(89.0791178449291,-4.4101299607236,0.468908825028051));
#12560=CARTESIAN_POINT('Ctrl Pts',(89.0769051096917,-4.40440763049221,0.517598479163535));
#12561=CARTESIAN_POINT('Ctrl Pts',(89.0769030860234,-4.40440239710597,0.517643008534498));
#12562=CARTESIAN_POINT('Ctrl Pts',(89.0769010623273,-4.40439716302833,0.517687537823121));
#12563=CARTESIAN_POINT('Ctrl Pts',(89.0768990386032,-4.40439192825929,0.517732067029408));
#12564=CARTESIAN_POINT('Ctrl Pts',(89.0717108190989,-4.39097155572819,0.631891551906531));
#12565=CARTESIAN_POINT('Ctrl Pts',(89.0663335032324,-4.37298416348157,0.745663962758008));
#12566=CARTESIAN_POINT('Ctrl Pts',(89.0608439791029,-4.35050280379623,0.858666722074836));
#12567=CARTESIAN_POINT('Ctrl Pts',(89.0602882381941,-4.34822686676297,0.870106740311668));
#12568=CARTESIAN_POINT('Ctrl Pts',(89.0597313472792,-4.3459049034978,0.88153884000792));
#12569=CARTESIAN_POINT('Ctrl Pts',(89.059173386134,-4.34353701162595,0.892962604077999));
#12570=CARTESIAN_POINT('Ctrl Pts',(89.0531113618511,-4.31781081518433,1.01707722352647));
#12571=CARTESIAN_POINT('Ctrl Pts',(89.0469235432333,-4.28665918413459,1.14021231604018));
#12572=CARTESIAN_POINT('Ctrl Pts',(89.0407014325302,-4.25022497621635,1.2618801082538));
#12573=CARTESIAN_POINT('Ctrl Pts',(89.0344853528745,-4.21382608371527,1.38342996874662));
#12574=CARTESIAN_POINT('Ctrl Pts',(89.0282353979775,-4.17215519818587,1.50351550910955));
#12575=CARTESIAN_POINT('Ctrl Pts',(89.0220254139412,-4.12539113653842,1.62167231983811));
#12576=CARTESIAN_POINT('Ctrl Pts',(89.0173485759035,-4.09017237574424,1.71065809880283));
#12577=CARTESIAN_POINT('Ctrl Pts',(89.0126945260154,-4.05206364381119,1.7985526796479));
#12578=CARTESIAN_POINT('Ctrl Pts',(89.0081811492928,-4.0110095527276,1.88508764521091));
#12579=CARTESIAN_POINT('Ctrl Pts',(89.0067059079872,-3.99759062170222,1.9133724446919));
#12580=CARTESIAN_POINT('Ctrl Pts',(89.0052456958246,-3.98385719741542,1.94151161348086));
#12581=CARTESIAN_POINT('Ctrl Pts',(89.0038046294465,-3.9698079180284,1.96949471348206));
#12582=CARTESIAN_POINT('Ctrl Pts',(88.9988257358338,-3.92126756730704,2.06617650412137));
#12583=CARTESIAN_POINT('Ctrl Pts',(88.9939667019039,-3.86912750892133,2.16107532962121));
#12584=CARTESIAN_POINT('Ctrl Pts',(88.989126359296,-3.81371772843866,2.25403148593715));
#12585=CARTESIAN_POINT('Ctrl Pts',(88.9882817194165,-3.80404872066293,2.27025233702862));
#12586=CARTESIAN_POINT('Ctrl Pts',(88.9874376486925,-3.79428007802033,2.28641414022231));
#12587=CARTESIAN_POINT('Ctrl Pts',(88.9865936095589,-3.78441346018295,2.30251617972391));
#12588=CARTESIAN_POINT('Ctrl Pts',(88.9790454423553,-3.69617717089062,2.44651529259893));
#12589=CARTESIAN_POINT('Ctrl Pts',(88.9714997196197,-3.60010770911251,2.58573895241691));
#12590=CARTESIAN_POINT('Ctrl Pts',(88.9639510940841,-3.49678444365902,2.71935321020572));
#12591=CARTESIAN_POINT('Ctrl Pts',(88.9601386366122,-3.4446006979513,2.78683551848134));
#12592=CARTESIAN_POINT('Ctrl Pts',(88.9563254547329,-3.39056617040065,2.85288623395623));
#12593=CARTESIAN_POINT('Ctrl Pts',(88.9525109323959,-3.33475286920143,2.91739344910565));
#12594=CARTESIAN_POINT('Ctrl Pts',(88.9472306677637,-3.25749313015944,3.00668776608181));
#12595=CARTESIAN_POINT('Ctrl Pts',(88.9421023660308,-3.17661953470607,3.09285158050349));
#12596=CARTESIAN_POINT('Ctrl Pts',(88.9372143103819,-3.09227639170099,3.175404546789));
#12597=CARTESIAN_POINT('Ctrl Pts',(88.9368392356173,-3.08580449637623,3.18173907663354));
#12598=CARTESIAN_POINT('Ctrl Pts',(88.9364655754075,-3.0793121923559,3.18805233001413));
#12599=CARTESIAN_POINT('Ctrl Pts',(88.9360933696384,-3.07279955490985,3.19434408214872));
#12600=CARTESIAN_POINT('Ctrl Pts',(88.9308649365839,-2.98131551105713,3.28272531524506));
#12601=CARTESIAN_POINT('Ctrl Pts',(88.9256960264991,-2.88609324516521,3.3671459059386));
#12602=CARTESIAN_POINT('Ctrl Pts',(88.9205222252319,-2.78749823238605,3.44726151214697));
#12603=CARTESIAN_POINT('Ctrl Pts',(88.915345284881,-2.68884339937208,3.52742572663926));
#12604=CARTESIAN_POINT('Ctrl Pts',(88.9101630841282,-2.58681154263463,3.60327937580524));
#12605=CARTESIAN_POINT('Ctrl Pts',(88.904895067653,-2.48180444078077,3.67450512558962));
#12606=CARTESIAN_POINT('Ctrl Pts',(88.9000293782515,-2.38481690382521,3.74029124783699));
#12607=CARTESIAN_POINT('Ctrl Pts',(88.895090034108,-2.28529074647613,3.80212958643056));
#12608=CARTESIAN_POINT('Ctrl Pts',(88.8900061685127,-2.18357361175643,3.85979509254691));
#12609=CARTESIAN_POINT('Ctrl Pts',(88.8895779133094,-2.17500515309208,3.86465272550009));
#12610=CARTESIAN_POINT('Ctrl Pts',(88.8891486325734,-2.16642113361103,3.86948077528753));
#12611=CARTESIAN_POINT('Ctrl Pts',(88.8887182839436,-2.15782175335337,3.87427912243183));
#12612=CARTESIAN_POINT('Ctrl Pts',(88.8862969240186,-2.10943727320232,3.90127706009769));
#12613=CARTESIAN_POINT('Ctrl Pts',(88.8838416834989,-2.06056752652318,3.92733415410425));
#12614=CARTESIAN_POINT('Ctrl Pts',(88.8813448941584,-2.01125180454248,3.95242916661114));
#12615=CARTESIAN_POINT('Ctrl Pts',(88.8813428564613,-2.01121155665288,3.95244964732707));
#12616=CARTESIAN_POINT('Ctrl Pts',(88.8813408187366,-2.01117130846618,3.95247012740235));
#12617=CARTESIAN_POINT('Ctrl Pts',(88.8813387809842,-2.01113105998239,3.952490606837));
#12618=CARTESIAN_POINT('Ctrl Pts',(88.8761543330759,-1.90873090269395,4.00459436658136));
#12619=CARTESIAN_POINT('Ctrl Pts',(88.8707803904864,-1.80412184797462,4.05268645179417));
#12620=CARTESIAN_POINT('Ctrl Pts',(88.8652938432659,-1.6976623971288,4.09661557354543));
#12621=CARTESIAN_POINT('Ctrl Pts',(88.8647369133398,-1.68685588226361,4.10107474277323));
#12622=CARTESIAN_POINT('Ctrl Pts',(88.8641788231435,-1.67603034427544,4.10549102673119));
#12623=CARTESIAN_POINT('Ctrl Pts',(88.863619653099,-1.66518618723406,4.10986427424895));
#12624=CARTESIAN_POINT('Ctrl Pts',(88.8575592812349,-1.54765552752052,4.15726221065757));
#12625=CARTESIAN_POINT('Ctrl Pts',(88.8513726000233,-1.42793185514377,4.19960391981595));
#12626=CARTESIAN_POINT('Ctrl Pts',(88.8451512083656,-1.3065001605735,4.23673776581859));
#12627=CARTESIAN_POINT('Ctrl Pts',(88.8389358695328,-1.18518660753971,4.27383548410649));
#12628=CARTESIAN_POINT('Ctrl Pts',(88.8326862385821,-1.0621684332796,4.30573583380955));
#12629=CARTESIAN_POINT('Ctrl Pts',(88.8264762691896,-0.937931122903868,
4.33233007236424));
#12630=CARTESIAN_POINT('Ctrl Pts',(88.8217562731814,-0.843502379062377,
4.35254348919164));
#12631=CARTESIAN_POINT('Ctrl Pts',(88.817059309445,-0.74836641143597,4.36969206864705));
#12632=CARTESIAN_POINT('Ctrl Pts',(88.8125022748401,-0.652722061934351,
4.38358287260651));
#12633=CARTESIAN_POINT('Ctrl Pts',(88.8110680851599,-0.622620877519621,
4.38795458566464));
#12634=CARTESIAN_POINT('Ctrl Pts',(88.8096477552705,-0.592469722812713,
4.39200356834735));
#12635=CARTESIAN_POINT('Ctrl Pts',(88.8082449291489,-0.562275860701015,
4.39572370546327));
#12636=CARTESIAN_POINT('Ctrl Pts',(88.8033379360349,-0.456659725396665,
4.40873649937259));
#12637=CARTESIAN_POINT('Ctrl Pts',(88.7985549211245,-0.350544966988067,
4.41788031960409));
#12638=CARTESIAN_POINT('Ctrl Pts',(88.7937928824806,-0.244235520955601,
4.42334373127186));
#12639=CARTESIAN_POINT('Ctrl Pts',(88.7928699688644,-0.223632068817665,
4.42440257547628));
#12640=CARTESIAN_POINT('Ctrl Pts',(88.7919478431361,-0.203021146921662,
4.42532318213354));
#12641=CARTESIAN_POINT('Ctrl Pts',(88.7910257554883,-0.182404741442705,
4.42610692012007));
#12642=CARTESIAN_POINT('Ctrl Pts',(88.7834775121547,-0.0136380893970825,
4.43252262804751));
#12643=CARTESIAN_POINT('Ctrl Pts',(88.7759317389052,0.155498224570251,4.42977097023969));
#12644=CARTESIAN_POINT('Ctrl Pts',(88.7683830849804,0.323988656491828,4.41787215803026));
#12645=CARTESIAN_POINT('Ctrl Pts',(88.7645729185807,0.409033829944684,4.41186625884243));
#12646=CARTESIAN_POINT('Ctrl Pts',(88.7607620340732,0.493914102679781,4.403529109817));
#12647=CARTESIAN_POINT('Ctrl Pts',(88.7569498153798,0.57849664240472,4.39285864372773));
#12648=CARTESIAN_POINT('Ctrl Pts',(88.7516104338553,0.696962681795999,4.37791362244832));
#12649=CARTESIAN_POINT('Ctrl Pts',(88.7464282187022,0.814813527402178,4.35811550109011));
#12650=CARTESIAN_POINT('Ctrl Pts',(88.7414901855034,0.931554253797117,4.33332050942411));
#12651=CARTESIAN_POINT('Ctrl Pts',(88.741171223872,0.939094869877251,4.33171893027827));
#12652=CARTESIAN_POINT('Ctrl Pts',(88.7408532810254,0.946630837061738,4.33009650850236));
#12653=CARTESIAN_POINT('Ctrl Pts',(88.7405363804139,0.954162014877631,4.32845320779207));
#12654=CARTESIAN_POINT('Ctrl Pts',(88.7353078032711,1.07841972458532,4.3013402133026));
#12655=CARTESIAN_POINT('Ctrl Pts',(88.7301389971226,1.20145511200285,4.26892201973708));
#12656=CARTESIAN_POINT('Ctrl Pts',(88.724965633424,1.32277915137856,4.23131177478354));
#12657=CARTESIAN_POINT('Ctrl Pts',(88.7197891379548,1.44417663601871,4.19367876192349));
#12658=CARTESIAN_POINT('Ctrl Pts',(88.7146077169301,1.56386050606829,4.15084706101972));
#12659=CARTESIAN_POINT('Ctrl Pts',(88.7093408739182,1.68134408896872,4.10297497781955));
#12660=CARTESIAN_POINT('Ctrl Pts',(88.7044744759562,1.78989523946017,4.05874267250923));
#12661=CARTESIAN_POINT('Ctrl Pts',(88.6995347059271,1.89656841241729,4.010207035418));
#12662=CARTESIAN_POINT('Ctrl Pts',(88.6944506333384,2.00098330039062,3.95753266766142));
#12663=CARTESIAN_POINT('Ctrl Pts',(88.6940243924115,2.00973728606966,3.95311652864194));
#12664=CARTESIAN_POINT('Ctrl Pts',(88.6935971371976,2.01847542860371,3.94867130287051));
#12665=CARTESIAN_POINT('Ctrl Pts',(88.693168825898,2.02719752046672,3.94419708918269));
#12666=CARTESIAN_POINT('Ctrl Pts',(88.690736229254,2.07673469451726,3.91878576519375));
#12667=CARTESIAN_POINT('Ctrl Pts',(88.6882694915977,2.1257531106961,3.89243994260321));
#12668=CARTESIAN_POINT('Ctrl Pts',(88.6857608276608,2.17421273004713,3.86518085028478));
#12669=CARTESIAN_POINT('Ctrl Pts',(88.6857587910729,2.17425207061955,3.86515872076107));
#12670=CARTESIAN_POINT('Ctrl Pts',(88.6857567544573,2.17429141082386,3.8651365906355));
#12671=CARTESIAN_POINT('Ctrl Pts',(88.6857547178141,2.17433075066006,3.8651144599081));
#12672=CARTESIAN_POINT('Ctrl Pts',(88.6805696920064,2.27448480190595,3.80877253732366));
#12673=CARTESIAN_POINT('Ctrl Pts',(88.6751952198011,2.37252368917428,3.7483670152655));
#12674=CARTESIAN_POINT('Ctrl Pts',(88.6697081700516,2.4681226980108,3.68411251617214));
#12675=CARTESIAN_POINT('Ctrl Pts',(88.6691510908233,2.47782850067427,3.67758900200572));
#12676=CARTESIAN_POINT('Ctrl Pts',(88.6685928511944,2.48750913816589,3.67102585557611));
#12677=CARTESIAN_POINT('Ctrl Pts',(88.6680335316074,2.49716426042529,3.66442332963836));
#12678=CARTESIAN_POINT('Ctrl Pts',(88.6619724941223,2.60179148839528,3.59287540223691));
#12679=CARTESIAN_POINT('Ctrl Pts',(88.6557851745972,2.703425006078,3.51669775867505));
#12680=CARTESIAN_POINT('Ctrl Pts',(88.6495631532013,2.80166966427415,3.43621015540066));
#12681=CARTESIAN_POINT('Ctrl Pts',(88.6433471705941,2.89981897102572,3.35580066944464));
#12682=CARTESIAN_POINT('Ctrl Pts',(88.637096904447,2.9945862542781,3.27108985467447));
#12683=CARTESIAN_POINT('Ctrl Pts',(88.6308862907854,3.08561180252409,3.18242165144434));
#12684=CARTESIAN_POINT('Ctrl Pts',(88.6261587936146,3.15490012816381,3.1149277284998));
#12685=CARTESIAN_POINT('Ctrl Pts',(88.6214543919938,3.22202246743561,3.04513866982926));
#12686=CARTESIAN_POINT('Ctrl Pts',(88.6168898016557,3.28670769553783,2.97311411377379));
#12687=CARTESIAN_POINT('Ctrl Pts',(88.6154621219541,3.30693947546093,2.95058679169539));
#12688=CARTESIAN_POINT('Ctrl Pts',(88.6140481195462,3.32693258699011,2.92784106573228));
#12689=CARTESIAN_POINT('Ctrl Pts',(88.61265136565,3.34667807372635,2.90487957416858));
#12690=CARTESIAN_POINT('Ctrl Pts',(88.6077511753944,3.41595057903976,2.82432445453047));
#12691=CARTESIAN_POINT('Ctrl Pts',(88.6029753969762,3.48228774232787,2.74121671052258));
#12692=CARTESIAN_POINT('Ctrl Pts',(88.5982208451739,3.54567884503379,2.65591299564899));
#12693=CARTESIAN_POINT('Ctrl Pts',(88.5972892946892,3.55809894579443,2.63919959757321));
#12694=CARTESIAN_POINT('Ctrl Pts',(88.5963585590483,3.57040604445793,2.62240176864163));
#12695=CARTESIAN_POINT('Ctrl Pts',(88.5954278621686,3.5826001872094,2.605521994311));
#12696=CARTESIAN_POINT('Ctrl Pts',(88.5878790824142,3.68150553430708,2.46861200620224));
#12697=CARTESIAN_POINT('Ctrl Pts',(88.5803327708345,3.77298476484709,2.32631169387097));
#12698=CARTESIAN_POINT('Ctrl Pts',(88.5727835775853,3.85649165180118,2.17947751716839));
#12699=CARTESIAN_POINT('Ctrl Pts',(88.5689718689625,3.89865561694978,2.10533858881252));
#12700=CARTESIAN_POINT('Ctrl Pts',(88.5651594415353,3.93878622924592,2.03004362944537));
#12701=CARTESIAN_POINT('Ctrl Pts',(88.5613456788694,3.97680804529936,1.95370216437051));
#12702=CARTESIAN_POINT('Ctrl Pts',(88.5556603598935,4.03348859184737,1.83989708050399));
#12703=CARTESIAN_POINT('Ctrl Pts',(88.5501573255947,4.08519648762396,1.72361895994459));
#12704=CARTESIAN_POINT('Ctrl Pts',(88.5449329669845,4.13146929417268,1.60527672236151));
#12705=CARTESIAN_POINT('Ctrl Pts',(88.5397030542424,4.1777912943724,1.48680867251054));
#12706=CARTESIAN_POINT('Ctrl Pts',(88.5345327817112,4.2190184935044,1.36641641112919));
#12707=CARTESIAN_POINT('Ctrl Pts',(88.5293577937609,4.25497390592655,1.24456982842773));
#12708=CARTESIAN_POINT('Ctrl Pts',(88.5241796709027,4.29095109944351,1.1226494334184));
#12709=CARTESIAN_POINT('Ctrl Pts',(88.5189964640541,4.32164971921428,0.999272922515912));
#12710=CARTESIAN_POINT('Ctrl Pts',(88.5137276562027,4.34693167389145,0.874933274360714));
#12711=CARTESIAN_POINT('Ctrl Pts',(88.5088601667149,4.370287934376,0.76006441837417));
#12712=CARTESIAN_POINT('Ctrl Pts',(88.5039191737815,4.38902129238268,0.644373038264876));
#12713=CARTESIAN_POINT('Ctrl Pts',(88.4988337726266,4.40305791118607,0.528266872988238));
#12714=CARTESIAN_POINT('Ctrl Pts',(88.4984066063687,4.40423696663214,0.518514124950444));
#12715=CARTESIAN_POINT('Ctrl Pts',(88.4979784212019,4.40538290308052,0.508758427343947));
#12716=CARTESIAN_POINT('Ctrl Pts',(88.4975491751029,4.40649568756069,0.499000008966845));
#12717=CARTESIAN_POINT('Ctrl Pts',(88.4951269290217,4.41277515719891,0.443933018899884));
#12718=CARTESIAN_POINT('Ctrl Pts',(88.4926708248137,4.41799884925738,0.388780533792759));
#12719=CARTESIAN_POINT('Ctrl Pts',(88.4901731862196,4.42216229197357,0.333587031036786));
#12720=CARTESIAN_POINT('Ctrl Pts',(88.4901711523942,4.42216568226218,0.33354208700451));
#12721=CARTESIAN_POINT('Ctrl Pts',(88.4901691185412,4.42216907184788,0.333497142944872));
#12722=CARTESIAN_POINT('Ctrl Pts',(88.4901670846607,4.4221724607307,0.333452198857978));
#12723=CARTESIAN_POINT('Ctrl Pts',(88.4849814679223,4.43081281462189,0.21886198214381));
#12724=CARTESIAN_POINT('Ctrl Pts',(88.4796064741109,4.43489854926796,0.103778888302272));
#12725=CARTESIAN_POINT('Ctrl Pts',(88.4741189831289,4.43442821784785,-0.0114078262371407));
#12726=CARTESIAN_POINT('Ctrl Pts',(88.4735622701539,4.43438050212403,-0.0230936656757789));
#12727=CARTESIAN_POINT('Ctrl Pts',(88.4730043993173,4.43428591921341,-0.0347805354675403));
#12728=CARTESIAN_POINT('Ctrl Pts',(88.472445450895,4.43414448530773,-0.0464680050712581));
#12729=CARTESIAN_POINT('Ctrl Pts',(88.4663843784788,4.43261081760191,-0.173203490504955));
#12730=CARTESIAN_POINT('Ctrl Pts',(88.4601971327827,4.42556499904317,-0.300014605638085));
#12731=CARTESIAN_POINT('Ctrl Pts',(88.4539752809605,4.41305400745871,-0.426395274606113));
#12732=CARTESIAN_POINT('Ctrl Pts',(88.4477594703326,4.40055516359727,-0.552653232488251));
#12733=CARTESIAN_POINT('Ctrl Pts',(88.4415094715515,4.3826021227949,-0.678481647775574));
#12734=CARTESIAN_POINT('Ctrl Pts',(88.4352992044174,4.35928163403119,-0.803390517563371));
#12735=CARTESIAN_POINT('Ctrl Pts',(88.4305863657173,4.34158421464844,-0.898181183216139));
#12736=CARTESIAN_POINT('Ctrl Pts',(88.4258965276388,4.32079504824394,-0.992445189586246));
#12737=CARTESIAN_POINT('Ctrl Pts',(88.4213467444025,4.29681199588026,-1.08592553637779));
#12738=CARTESIAN_POINT('Ctrl Pts',(88.4199054548131,4.28921459576327,-1.11553843080342));
#12739=CARTESIAN_POINT('Ctrl Pts',(88.4184782198473,4.28129678745296,-1.14507230525));
#12740=CARTESIAN_POINT('Ctrl Pts',(88.4170687605823,4.27305564780333,-1.17451794685169));
#12741=CARTESIAN_POINT('Ctrl Pts',(88.4121482545705,4.24428533978623,-1.27731443067049));
#12742=CARTESIAN_POINT('Ctrl Pts',(88.4073509510985,4.21173177516902,-1.3790745538966));
#12743=CARTESIAN_POINT('Ctrl Pts',(88.4025741940027,4.17568645033873,-1.47958827496848));
#12744=CARTESIAN_POINT('Ctrl Pts',(88.4016654768837,4.1688292869794,-1.49870972854088));
#12745=CARTESIAN_POINT('Ctrl Pts',(88.4007575033423,4.16184569917836,-1.51778621507419));
#12746=CARTESIAN_POINT('Ctrl Pts',(88.3998495666191,4.15473760793157,-1.5368164839011));
#12747=CARTESIAN_POINT('Ctrl Pts',(88.3923010947199,4.0956418299334,-1.69503174912432));
#12748=CARTESIAN_POINT('Ctrl Pts',(88.3847550858854,4.02794349871041,-1.85005612301517));
#12749=CARTESIAN_POINT('Ctrl Pts',(88.3772061906082,3.95205236539545,-2.000960214394));
#12750=CARTESIAN_POINT('Ctrl Pts',(88.3733947719453,3.91373511879901,-2.07715131906201));
#12751=CARTESIAN_POINT('Ctrl Pts',(88.3695826333455,3.87332872318543,-2.152291432711));
#12752=CARTESIAN_POINT('Ctrl Pts',(88.3657691585757,3.83088247457447,-2.22625706203015));
#12753=CARTESIAN_POINT('Ctrl Pts',(88.3603973311197,3.771090831138,-2.33044828456525));
#12754=CARTESIAN_POINT('Ctrl Pts',(88.3551858219174,3.70700415987308,-2.43217120019112));
#12755=CARTESIAN_POINT('Ctrl Pts',(88.3502209500729,3.63868496442522,-2.5309062864685));
#12756=CARTESIAN_POINT('Ctrl Pts',(88.3499314769954,3.63470166568501,-2.53666296059508));
#12757=CARTESIAN_POINT('Ctrl Pts',(88.349642842333,3.63070398855769,-2.54240946675198));
#12758=CARTESIAN_POINT('Ctrl Pts',(88.3493550631941,3.6266919490924,-2.54814569788737));
#12759=CARTESIAN_POINT('Ctrl Pts',(88.344125910758,3.55379032730009,-2.65237711344623));
#12760=CARTESIAN_POINT('Ctrl Pts',(88.3389564100754,3.47646290549643,-2.75343582727919));
#12761=CARTESIAN_POINT('Ctrl Pts',(88.3337821996865,3.39500257058184,-2.85091405116349));
#12762=CARTESIAN_POINT('Ctrl Pts',(88.3286048543391,3.3134928803544,-2.94845133530382));
#12763=CARTESIAN_POINT('Ctrl Pts',(88.3234224307305,3.22784502012949,-3.04240347598096));
#12764=CARTESIAN_POINT('Ctrl Pts',(88.3181544088936,3.13839265625549,-3.13238225347051));
#12765=CARTESIAN_POINT('Ctrl Pts',(88.3132876826322,3.05575439432448,-3.21550682905898));
#12766=CARTESIAN_POINT('Ctrl Pts',(88.3083474564411,2.96986875590525,-3.29524064473898));
#12767=CARTESIAN_POINT('Ctrl Pts',(88.3032628268791,2.88103409455906,-3.37129621597049));
#12768=CARTESIAN_POINT('Ctrl Pts',(88.302835679954,2.87357131836818,-3.37768545298191));
#12769=CARTESIAN_POINT('Ctrl Pts',(88.3024075139372,2.86608772218063,-3.38404876108423));
#12770=CARTESIAN_POINT('Ctrl Pts',(88.3019782867927,2.85858347816145,-3.39038598595353));
#12771=CARTESIAN_POINT('Ctrl Pts',(88.2995531132985,2.81618379788861,-3.42619189892609));
#12772=CARTESIAN_POINT('Ctrl Pts',(88.2970939905493,2.77312586673181,-3.46116442599992));
#12773=CARTESIAN_POINT('Ctrl Pts',(88.2945932112675,2.72944435844312,-3.49527507400002));
#12774=CARTESIAN_POINT('Ctrl Pts',(88.294591175675,2.72940880242658,-3.4953028394965));
#12775=CARTESIAN_POINT('Ctrl Pts',(88.294589140055,2.72937324599686,-3.49533060442208));
#12776=CARTESIAN_POINT('Ctrl Pts',(88.2945871044073,2.72933768915397,-3.49535836877679));
#12777=CARTESIAN_POINT('Ctrl Pts',(88.2894019474456,2.6387680815256,-3.56607912201926));
#12778=CARTESIAN_POINT('Ctrl Pts',(88.2840273641573,2.54526323421544,-3.63328304472224));
#12779=CARTESIAN_POINT('Ctrl Pts',(88.2785402335313,2.44914625265982,-3.69675312843794));
#12780=CARTESIAN_POINT('Ctrl Pts',(88.2779833574119,2.43939156385309,-3.70319455954785));
#12781=CARTESIAN_POINT('Ctrl Pts',(88.2774253220833,2.42961001497231,-3.7095975342355));
#12782=CARTESIAN_POINT('Ctrl Pts',(88.2768662079069,2.41980197365509,-3.71596182704157));
#12783=CARTESIAN_POINT('Ctrl Pts',(88.2708053142631,2.31348112223194,-3.78495185348637));
#12784=CARTESIAN_POINT('Ctrl Pts',(88.264618181701,2.20404118108658,-3.84939661958584));
#12785=CARTESIAN_POINT('Ctrl Pts',(88.2583963889422,2.09192935522711,-3.90905462736617));
#12786=CARTESIAN_POINT('Ctrl Pts',(88.2521806394439,1.97992642418058,-3.96865468900613));
#12787=CARTESIAN_POINT('Ctrl Pts',(88.2459306479155,1.86525694388356,-4.02347763089949));
#12788=CARTESIAN_POINT('Ctrl Pts',(88.239720347209,1.74837679346202,-4.07332396730808));
#12789=CARTESIAN_POINT('Ctrl Pts',(88.2350013663689,1.65956383310872,-4.11120037902767));
#12790=CARTESIAN_POINT('Ctrl Pts',(88.2303054223472,1.56947167411519,-4.14620440265799));
#12791=CARTESIAN_POINT('Ctrl Pts',(88.2257494292195,1.47825849118211,-4.17810865159469));
#12792=CARTESIAN_POINT('Ctrl Pts',(88.2243139504936,1.44951951376367,-4.18816087716407));
#12793=CARTESIAN_POINT('Ctrl Pts',(88.2228923649931,1.42066961783144,-4.19790525660225));
#12794=CARTESIAN_POINT('Ctrl Pts',(88.2214883295742,1.39171478014474,-4.20733437422472));
#12795=CARTESIAN_POINT('Ctrl Pts',(88.2165772771388,1.29043619114185,-4.24031565834308));
#12796=CARTESIAN_POINT('Ctrl Pts',(88.2117899812828,1.18792712012537,-4.26958829497454));
#12797=CARTESIAN_POINT('Ctrl Pts',(88.2070235415891,1.08452252529479,-4.2952790429973));
#12798=CARTESIAN_POINT('Ctrl Pts',(88.2061044428004,1.06458331616579,-4.30023291567912));
#12799=CARTESIAN_POINT('Ctrl Pts',(88.2051861194916,1.04461065704532,-4.30505363710555));
#12800=CARTESIAN_POINT('Ctrl Pts',(88.2042678338922,1.02460673013011,-4.30974215488038));
#12801=CARTESIAN_POINT('Ctrl Pts',(88.1967193233434,0.860170030455247,-4.34828280704974));
#12802=CARTESIAN_POINT('Ctrl Pts',(88.1891732790936,0.693619179579493,-4.37789489650803));
#12803=CARTESIAN_POINT('Ctrl Pts',(88.1816243512325,0.525954872741697,-4.39840418586453));
#12804=CARTESIAN_POINT('Ctrl Pts',(88.1778131454757,0.441306670617002,-4.40875865249864));
#12805=CARTESIAN_POINT('Ctrl Pts',(88.1740012205647,0.356374844747491,-4.41679202056793));
#12806=CARTESIAN_POINT('Ctrl Pts',(88.1701879602425,0.271289481563919,-4.42247685680384));
#12807=CARTESIAN_POINT('Ctrl Pts',(88.1648020783348,0.151114177637051,-4.4305061687426));
#12808=CARTESIAN_POINT('Ctrl Pts',(88.1595777938041,0.0306099578475067,
-4.43356586781557));
#12809=CARTESIAN_POINT('Ctrl Pts',(88.1546011277753,-0.0897524081145261,
-4.431419783972));
#12810=CARTESIAN_POINT('Ctrl Pts',(88.1543247979209,-0.0964355399270603,
-4.43130062246256));
#12811=CARTESIAN_POINT('Ctrl Pts',(88.1540492314834,-0.103118221129596,
-4.43116541296832));
#12812=CARTESIAN_POINT('Ctrl Pts',(88.1537744431882,-0.109800366457727,
-4.43101411574125));
#12813=CARTESIAN_POINT('Ctrl Pts',(88.1485451983774,-0.236962164820039,
-4.42813491654148));
#12814=CARTESIAN_POINT('Ctrl Pts',(88.1433756304472,-0.363937474086309,
-4.41981354439092));
#12815=CARTESIAN_POINT('Ctrl Pts',(88.1382013876067,-0.490224550752052,
-4.40606764837524));
#12816=CARTESIAN_POINT('Ctrl Pts',(88.133024010588,-0.616588122899913,-4.39231342610028));
#12817=CARTESIAN_POINT('Ctrl Pts',(88.1278415902311,-0.742262504656591,
-4.37312772689429));
#12818=CARTESIAN_POINT('Ctrl Pts',(88.1225736131136,-0.866739629134219,
-4.34857298405046));
#12819=CARTESIAN_POINT('Ctrl Pts',(88.1177067342755,-0.981739195275547,
-4.32588781369805));
#12820=CARTESIAN_POINT('Ctrl Pts',(88.1127663851291,-1.0957173703205,-4.29861988600657));
#12821=CARTESIAN_POINT('Ctrl Pts',(88.1076816553335,-1.20826944966748,-4.26685810740331));
#12822=CARTESIAN_POINT('Ctrl Pts',(88.1072547200742,-1.21771979474282,-4.26419125513591));
#12823=CARTESIAN_POINT('Ctrl Pts',(88.1068267669332,-1.22716011473415,-4.26149273092718));
#12824=CARTESIAN_POINT('Ctrl Pts',(88.1063977539355,-1.23659018607998,-4.25876259240397));
#12825=CARTESIAN_POINT('Ctrl Pts',(88.1039716855763,-1.28991723640049,-4.24332365996438));
#12826=CARTESIAN_POINT('Ctrl Pts',(88.1015116496178,-1.34291544842791,-4.22687408587617));
#12827=CARTESIAN_POINT('Ctrl Pts',(88.0990099295383,-1.39554183572812,-4.20942694330022));
#12828=CARTESIAN_POINT('Ctrl Pts',(88.0990078942427,-1.39558465037319,-4.20941274902896));
#12829=CARTESIAN_POINT('Ctrl Pts',(88.0990058589194,-1.39562746477233,-4.2093985540975));
#12830=CARTESIAN_POINT('Ctrl Pts',(88.0990038235686,-1.39567027892551,-4.20938435850586));
#12831=CARTESIAN_POINT('Ctrl Pts',(88.0938185586643,-1.50474372313981,-4.17321963358952));
#12832=CARTESIAN_POINT('Ctrl Pts',(88.088443877551,-1.61251766299464,-4.1326620868654));
#12833=CARTESIAN_POINT('Ctrl Pts',(88.0829566570621,-1.7186323455401,-4.08786031364498));
#12834=CARTESIAN_POINT('Ctrl Pts',(88.0823997816709,-1.72940148730775,-4.08331356633651));
#12835=CARTESIAN_POINT('Ctrl Pts',(88.0818417471935,-1.74015351619585,-4.0787231435896));
#12836=CARTESIAN_POINT('Ctrl Pts',(88.0812826339848,-1.75088804074892,-4.0740892263663));
#12837=CARTESIAN_POINT('Ctrl Pts',(88.0752216516145,-1.86725403435956,-4.02385594595101));
#12838=CARTESIAN_POINT('Ctrl Pts',(88.0690344398818,-1.98156653853143,-3.96850663654002));
#12839=CARTESIAN_POINT('Ctrl Pts',(88.0628125743478,-2.09337661448109,-3.90827959845703));
#12840=CARTESIAN_POINT('Ctrl Pts',(88.056596750375,-2.20507812051486,-3.84811104208423));
#12841=CARTESIAN_POINT('Ctrl Pts',(88.0503466907482,-2.31428226052506,-3.78307453888872));
#12842=CARTESIAN_POINT('Ctrl Pts',(88.0441363251228,-2.4205702515934,-3.71343890046891));
#12843=CARTESIAN_POINT('Ctrl Pts',(88.0394171777067,-2.5013366232805,-3.66052400576866));
#12844=CARTESIAN_POINT('Ctrl Pts',(88.0347210700937,-2.58042157459384,-3.60495175543443));
#12845=CARTESIAN_POINT('Ctrl Pts',(88.0301649114412,-2.65754815888378,-3.54672774048508));
#12846=CARTESIAN_POINT('Ctrl Pts',(88.0287295278983,-2.68184630964094,-3.52838470214167));
#12847=CARTESIAN_POINT('Ctrl Pts',(88.027308034537,-2.70594978116437,-3.50977870841442));
#12848=CARTESIAN_POINT('Ctrl Pts',(88.0259040869341,-2.72984909076715,-3.4909106223017));
#12849=CARTESIAN_POINT('Ctrl Pts',(88.0209928096281,-2.81345344796704,-3.42490644740021));
#12850=CARTESIAN_POINT('Ctrl Pts',(88.0162052789899,-2.89465334862268,-3.3558217680881));
#12851=CARTESIAN_POINT('Ctrl Pts',(88.0114385997259,-2.97336854490301,-3.28400564154297));
#12852=CARTESIAN_POINT('Ctrl Pts',(88.0105196252819,-2.98854415243295,-3.270160114856));
#12853=CARTESIAN_POINT('Ctrl Pts',(88.0096014258522,-3.00362751794813,-3.25621295512458));
#12854=CARTESIAN_POINT('Ctrl Pts',(88.0086832641134,-3.01861822021235,-3.24216650263116));
#12855=CARTESIAN_POINT('Ctrl Pts',(88.0011347006088,-3.1418625934326,-3.12668517273712));
#12856=CARTESIAN_POINT('Ctrl Pts',(87.9935886028726,-3.25884839560788,-3.00449403319924));
#12857=CARTESIAN_POINT('Ctrl Pts',(87.9860396211324,-3.36887579490987,-2.87632928520553));
#12858=CARTESIAN_POINT('Ctrl Pts',(87.9822282302062,-3.42442731771977,-2.81162043116765));
#12859=CARTESIAN_POINT('Ctrl Pts',(87.9784161199724,-3.47820422621604,-2.74538850081591));
#12860=CARTESIAN_POINT('Ctrl Pts',(87.9746026741387,-3.53011155227134,-2.67772655760983));
#12861=CARTESIAN_POINT('Ctrl Pts',(87.9692069018449,-3.60355696725544,-2.58198940690191));
#12862=CARTESIAN_POINT('Ctrl Pts',(87.9639736672022,-3.67303384379134,-2.48321173699712));
#12863=CARTESIAN_POINT('Ctrl Pts',(87.9589887810297,-3.73808305226769,-2.38165655471672));
#12864=CARTESIAN_POINT('Ctrl Pts',(87.9587215274673,-3.74157052060685,-2.37621189995187));
#12865=CARTESIAN_POINT('Ctrl Pts',(87.9584549877401,-3.74504525679008,-2.37075927285087));
#12866=CARTESIAN_POINT('Ctrl Pts',(87.9581891750717,-3.74850718824951,-2.36529871778091));
#12867=CARTESIAN_POINT('Ctrl Pts',(87.9529597979794,-3.8166143449817,-2.25787230441816));
#12868=CARTESIAN_POINT('Ctrl Pts',(87.9477900813474,-3.8800887759405,-2.14758368696896));
#12869=CARTESIAN_POINT('Ctrl Pts',(87.9426156695314,-3.93866697693383,-2.03486023348492));
#12870=CARTESIAN_POINT('Ctrl Pts',(87.9374381231253,-3.99728066382439,-1.92206849362782));
#12871=CARTESIAN_POINT('Ctrl Pts',(87.9322555130345,-4.05099180229852,-1.80683885942346));
#12872=CARTESIAN_POINT('Ctrl Pts',(87.9269873229904,-4.0995706535505,-1.68962879293032));
#12873=CARTESIAN_POINT('Ctrl Pts',(87.9221203438699,-4.14444987255479,-1.58134512404803));
#12874=CARTESIAN_POINT('Ctrl Pts',(87.9171798775052,-4.18494888574857,-1.4713706791475));
#12875=CARTESIAN_POINT('Ctrl Pts',(87.9120950169835,-4.22091730478055,-1.36009155160004));
#12876=CARTESIAN_POINT('Ctrl Pts',(87.9116679621035,-4.22393813274828,-1.35074571128328));
#12877=CARTESIAN_POINT('Ctrl Pts',(87.9112398887284,-4.22692702787906,-1.34139064960208));
#12878=CARTESIAN_POINT('Ctrl Pts',(87.9108107548531,-4.22988391412598,-1.33202658472419));
#12879=CARTESIAN_POINT('Ctrl Pts',(87.9083858750644,-4.2465922052006,-1.27911365248534));
#12880=CARTESIAN_POINT('Ctrl Pts',(87.9059270595241,-4.26227814859569,-1.22591435830625));
#12881=CARTESIAN_POINT('Ctrl Pts',(87.9034266041876,-4.27692881094136,-1.17247165722849));
#12882=CARTESIAN_POINT('Ctrl Pts',(87.9034245691548,-4.27694073460114,-1.17242816209013));
#12883=CARTESIAN_POINT('Ctrl Pts',(87.9034225340943,-4.27695265757532,-1.17238466679047));
#12884=CARTESIAN_POINT('Ctrl Pts',(87.9034204990064,-4.27696457986393,-1.1723411713295));
#12885=CARTESIAN_POINT('Ctrl Pts',(87.8978635917896,-4.30951897158758,-1.05357468933986));
#12886=CARTESIAN_POINT('Ctrl Pts',(87.8920942735389,-4.33701541644651,-0.933385892211736));
#12887=CARTESIAN_POINT('Ctrl Pts',(87.8862035975494,-4.35940446872122,-0.812161221172599));
#12888=CARTESIAN_POINT('Ctrl Pts',(87.8845141711738,-4.36582557480534,-0.777394386774961));
#12889=CARTESIAN_POINT('Ctrl Pts',(87.8828147628401,-4.3718265554393,-0.742542676406213));
#12890=CARTESIAN_POINT('Ctrl Pts',(87.8811075204681,-4.37740620808549,-0.707615996194812));
#12891=CARTESIAN_POINT('Ctrl Pts',(87.8749624100512,-4.39748981317933,-0.581899630484627));
#12892=CARTESIAN_POINT('Ctrl Pts',(87.868716520935,-4.41211541244499,-0.455206027914046));
#12893=CARTESIAN_POINT('Ctrl Pts',(87.8624531612852,-4.42125080253421,-0.327948252047925));
#12894=CARTESIAN_POINT('Ctrl Pts',(87.8610232672522,-4.42333636691305,-0.29889593116357));
#12895=CARTESIAN_POINT('Ctrl Pts',(87.859592462679,-4.42513571081463,-0.269814406401312));
#12896=CARTESIAN_POINT('Ctrl Pts',(87.8581617388014,-4.42664832866523,-0.240708952987256));
#12897=CARTESIAN_POINT('Ctrl Pts',(87.8542856910892,-4.43074623955586,-0.161857870755987));
#12898=CARTESIAN_POINT('Ctrl Pts',(87.8504096358317,-4.43274097879134,-0.0828285532405415));
#12899=CARTESIAN_POINT('Ctrl Pts',(87.846549162128,-4.43262664155567,-0.00371887744496941));
#12900=CARTESIAN_POINT('',(86.595526637467,-4.43203607817194,0.00306014809319887));
#12901=CARTESIAN_POINT('Ctrl Pts',(87.8465491620889,-4.4326266415545,-0.00371887664439084));
#12902=CARTESIAN_POINT('Ctrl Pts',(87.8420321872549,-4.43249286043845,0.0888439646362164));
#12903=CARTESIAN_POINT('Ctrl Pts',(87.837539566186,-4.42947104529508,0.181459192850865));
#12904=CARTESIAN_POINT('Ctrl Pts',(87.8331922601159,-4.42339728692258,0.273914875587774));
#12905=CARTESIAN_POINT('Ctrl Pts',(87.8313277093922,-4.4207922643209,0.313568929702731));
#12906=CARTESIAN_POINT('Ctrl Pts',(87.8294898898659,-4.41762587274885,0.353192984278078));
#12907=CARTESIAN_POINT('Ctrl Pts',(87.8276883450477,-4.41388554911566,0.392767400535123));
#12908=CARTESIAN_POINT('Ctrl Pts',(87.8219800481264,-4.40203412157206,0.518161182690504));
#12909=CARTESIAN_POINT('Ctrl Pts',(87.8163477377429,-4.38491853543299,0.643096989781379));
#12910=CARTESIAN_POINT('Ctrl Pts',(87.8107160151864,-4.36277438570532,0.767152774573604));
#12911=CARTESIAN_POINT('Ctrl Pts',(87.8030492049417,-4.33262819290424,0.936037543346859));
#12912=CARTESIAN_POINT('Ctrl Pts',(87.7953833872014,-4.29316361199279,1.10330118214133));
#12913=CARTESIAN_POINT('Ctrl Pts',(87.787713556523,-4.2446084359225,1.26788955888696));
#12914=CARTESIAN_POINT('Ctrl Pts',(87.7841174992333,-4.22184297965912,1.34505804627621));
#12915=CARTESIAN_POINT('Ctrl Pts',(87.780520582148,-4.19707859508859,1.42163775930275));
#12916=CARTESIAN_POINT('Ctrl Pts',(87.7769223670011,-4.17033599426891,1.49751701101889));
#12917=CARTESIAN_POINT('Ctrl Pts',(87.7721906866967,-4.13516927065124,1.59729880454784));
#12918=CARTESIAN_POINT('Ctrl Pts',(87.7676894420486,-4.09620330819457,1.69572954157321));
#12919=CARTESIAN_POINT('Ctrl Pts',(87.7633106293043,-4.05368569554833,1.79254843599859));
#12920=CARTESIAN_POINT('Ctrl Pts',(87.7624719109063,-4.04554186614788,1.81109314041323));
#12921=CARTESIAN_POINT('Ctrl Pts',(87.761637684244,-4.03726769501056,1.82957885844103));
#12922=CARTESIAN_POINT('Ctrl Pts',(87.7608071903586,-4.02886485861313,1.84800396605026));
#12923=CARTESIAN_POINT('Ctrl Pts',(87.7556353717226,-3.97653702497376,1.96274450366897));
#12924=CARTESIAN_POINT('Ctrl Pts',(87.750515971314,-3.91936486516802,2.07519924701217));
#12925=CARTESIAN_POINT('Ctrl Pts',(87.7453844310164,-3.85756093535738,2.18492081907719));
#12926=CARTESIAN_POINT('Ctrl Pts',(87.7402497364616,-3.79571901588341,2.29470983484027));
#12927=CARTESIAN_POINT('Ctrl Pts',(87.7351025190936,-3.72923934908682,2.40176203210674));
#12928=CARTESIAN_POINT('Ctrl Pts',(87.7298632377616,-3.65837860760412,2.50564268836832));
#12929=CARTESIAN_POINT('Ctrl Pts',(87.7250410517259,-3.59315903713031,2.60125348272576));
#12930=CARTESIAN_POINT('Ctrl Pts',(87.7201404342511,-3.52422787649343,2.69417801339603));
#12931=CARTESIAN_POINT('Ctrl Pts',(87.7150929805591,-3.45182288569065,2.78408983865759));
#12932=CARTESIAN_POINT('Ctrl Pts',(87.7146486095049,-3.44544844739908,2.79200555517738));
#12933=CARTESIAN_POINT('Ctrl Pts',(87.7142031003518,-3.43904708269489,2.799897954217));
#12934=CARTESIAN_POINT('Ctrl Pts',(87.7137564064223,-3.43261895262095,2.80776683238764));
#12935=CARTESIAN_POINT('Ctrl Pts',(87.7118094788342,-3.40460177361932,2.84206355098437));
#12936=CARTESIAN_POINT('Ctrl Pts',(87.709840008583,-3.37607663711951,2.87591290488159));
#12937=CARTESIAN_POINT('Ctrl Pts',(87.7078440961899,-3.34705850668323,2.90929733663113));
#12938=CARTESIAN_POINT('Ctrl Pts',(87.707842060943,-3.3470289166769,2.90933137898782));
#12939=CARTESIAN_POINT('Ctrl Pts',(87.7078400256686,-3.34699932615796,2.9093654208612));
#12940=CARTESIAN_POINT('Ctrl Pts',(87.7078379903667,-3.34696973512643,2.90939946225126));
#12941=CARTESIAN_POINT('Ctrl Pts',(87.7026527277547,-3.27158176980333,2.99612543972864));
#12942=CARTESIAN_POINT('Ctrl Pts',(87.6972780493939,-3.19264053533738,3.07996015897756));
#12943=CARTESIAN_POINT('Ctrl Pts',(87.6917908332701,-3.11042172940336,3.16062886407172));
#12944=CARTESIAN_POINT('Ctrl Pts',(87.6912339754052,-3.10207793763384,3.16881534732183));
#12945=CARTESIAN_POINT('Ctrl Pts',(87.6906759585418,-3.09370043462526,3.17696921727969));
#12946=CARTESIAN_POINT('Ctrl Pts',(87.6901168630286,-3.08528953812638,3.18509018242693));
#12947=CARTESIAN_POINT('Ctrl Pts',(87.6840559043722,-2.99410995477915,3.27312672152846));
#12948=CARTESIAN_POINT('Ctrl Pts',(87.6778687188843,-2.89900014999921,3.35729765775097));
#12949=CARTESIAN_POINT('Ctrl Pts',(87.6716468824007,-2.80035295348696,3.43728048673872));
#12950=CARTESIAN_POINT('Ctrl Pts',(87.6654310880813,-2.70180155546905,3.51718564261601));
#12951=CARTESIAN_POINT('Ctrl Pts',(87.6591810609017,-2.59971984348263,3.59291113138957));
#12952=CARTESIAN_POINT('Ctrl Pts',(87.6529707306469,-2.49451718893161,3.66417402955279));
#12953=CARTESIAN_POINT('Ctrl Pts',(87.6482523398717,-2.41458790749374,3.71831707630076));
#12954=CARTESIAN_POINT('Ctrl Pts',(87.643556983457,-2.33285456524835,3.76988570281975));
#12955=CARTESIAN_POINT('Ctrl Pts',(87.6390015883502,-2.24942888367878,3.81862649461662));
#12956=CARTESIAN_POINT('Ctrl Pts',(87.6375655193732,-2.22312929157413,3.83399182240296));
#12957=CARTESIAN_POINT('Ctrl Pts',(87.6361433597352,-2.19666185259931,3.84907592724259));
#12958=CARTESIAN_POINT('Ctrl Pts',(87.6347387726507,-2.17003102095355,3.86387037446465));
#12959=CARTESIAN_POINT('Ctrl Pts',(87.6298265739827,-2.07689622198936,3.91561032333828));
#12960=CARTESIAN_POINT('Ctrl Pts',(87.6250380662065,-1.98184406908071,3.96394347591442));
#12961=CARTESIAN_POINT('Ctrl Pts',(87.6202703782167,-1.88522772634785,4.00893014210631));
#12962=CARTESIAN_POINT('Ctrl Pts',(87.6193524758796,-1.8666265999769,4.01759123027395));
#12963=CARTESIAN_POINT('Ctrl Pts',(87.6184353452515,-1.84796735203671,4.02612833703379));
#12964=CARTESIAN_POINT('Ctrl Pts',(87.6175182522254,-1.82925229586479,4.03454197231946));
#12965=CARTESIAN_POINT('Ctrl Pts',(87.6099697187913,-1.67520987790019,4.10379406065791));
#12966=CARTESIAN_POINT('Ctrl Pts',(87.6024236510301,-1.51738614938628,4.16468603921365));
#12967=CARTESIAN_POINT('Ctrl Pts',(87.5948746991461,-1.35673006542032,4.21685565374921));
#12968=CARTESIAN_POINT('Ctrl Pts',(87.591063375288,-1.27561782955352,4.24319511114682));
#12969=CARTESIAN_POINT('Ctrl Pts',(87.5872513321114,-1.19378362697453,4.26731029657811));
#12970=CARTESIAN_POINT('Ctrl Pts',(87.5834379533438,-1.11134991493068,4.28914941908763));
#12971=CARTESIAN_POINT('Ctrl Pts',(87.5780485769099,-0.994847901328057,
4.32001423985805));
#12972=CARTESIAN_POINT('Ctrl Pts',(87.5728211362164,-0.877071722791255,
4.3460573951986));
#12973=CARTESIAN_POINT('Ctrl Pts',(87.5678415778635,-0.758439264454936,
4.36695688964637));
#12974=CARTESIAN_POINT('Ctrl Pts',(87.5675684286752,-0.751931787807793,
4.36810331258967));
#12975=CARTESIAN_POINT('Ctrl Pts',(87.567296025358,-0.745421747656629,4.36923425749517));
#12976=CARTESIAN_POINT('Ctrl Pts',(87.5670243820978,-0.738909217522545,
4.37034967100128));
#12977=CARTESIAN_POINT('Ctrl Pts',(87.5617950797062,-0.613538945582386,
4.39182207753265));
#12978=CARTESIAN_POINT('Ctrl Pts',(87.5566254430359,-0.487311806443546,
4.40791682779094));
#12979=CARTESIAN_POINT('Ctrl Pts',(87.5514511172639,-0.36072368253644,4.4185553687992));
#12980=CARTESIAN_POINT('Ctrl Pts',(87.5462736570173,-0.23405887477288,4.42920035436423));
#12981=CARTESIAN_POINT('Ctrl Pts',(87.5410911391898,-0.107032693729212,
4.43438212200354));
#12982=CARTESIAN_POINT('Ctrl Pts',(87.5358230481848,0.0198442128251148,
4.43406487031915));
#12983=CARTESIAN_POINT('Ctrl Pts',(87.5309561347443,0.137059143472471,4.43377177809935));
#12984=CARTESIAN_POINT('Ctrl Pts',(87.5260157390795,0.254147184748634,4.42878522511559));
#12985=CARTESIAN_POINT('Ctrl Pts',(87.5209309533604,0.370694107711927,4.41911514676029));
#12986=CARTESIAN_POINT('Ctrl Pts',(87.5205039336699,0.380481704225322,4.418303054748));
#12987=CARTESIAN_POINT('Ctrl Pts',(87.5200758956512,0.390265510942247,4.41745794660317));
#12988=CARTESIAN_POINT('Ctrl Pts',(87.5196467973071,0.400045297283987,4.41657983617998));
#12989=CARTESIAN_POINT('Ctrl Pts',(87.5172214354079,0.455322884585387,4.41161655540042));
#12990=CARTESIAN_POINT('Ctrl Pts',(87.5147621242226,0.510470886944629,4.4055990652705));
#12991=CARTESIAN_POINT('Ctrl Pts',(87.512261154631,0.56544465342528,4.39853197945318));
#12992=CARTESIAN_POINT('Ctrl Pts',(87.5122591194373,0.565489388979495,4.39852622852831));
#12993=CARTESIAN_POINT('Ctrl Pts',(87.5122570842161,0.565534124418486,4.39852047690849));
#12994=CARTESIAN_POINT('Ctrl Pts',(87.5122550489673,0.565578859742214,4.39851472459374));
#12995=CARTESIAN_POINT('Ctrl Pts',(87.5070697694304,0.679552716391212,4.38385933726274));
#12996=CARTESIAN_POINT('Ctrl Pts',(87.5016950758124,0.793090461968622,4.36464378107407));
#12997=CARTESIAN_POINT('Ctrl Pts',(87.4962078458948,0.905810578361075,4.34094516434875));
#12998=CARTESIAN_POINT('Ctrl Pts',(87.4956509902613,0.917249652860444,4.3385401788774));
#12999=CARTESIAN_POINT('Ctrl Pts',(87.4950929756595,0.928680276631663,4.33608905636515));
#13000=CARTESIAN_POINT('Ctrl Pts',(87.4945338824363,0.940102030899779,4.33359189962059));
#13001=CARTESIAN_POINT('Ctrl Pts',(87.4884729125023,1.06392200643301,4.3065209366357));
#13002=CARTESIAN_POINT('Ctrl Pts',(87.4822857175649,1.18670399204952,4.27403588380812));
#13003=CARTESIAN_POINT('Ctrl Pts',(87.4760638729893,1.30796179006401,4.23628485623563));
#13004=CARTESIAN_POINT('Ctrl Pts',(87.4698480703799,1.42910183593701,4.19857048827936));
#13005=CARTESIAN_POINT('Ctrl Pts',(87.4635980362634,1.54872079402424,4.15560071509786));
#13006=CARTESIAN_POINT('Ctrl Pts',(87.4573876999309,1.66635623553417,4.10755936331984));
#13007=CARTESIAN_POINT('Ctrl Pts',(87.4526693738758,1.7557301983872,4.07105976817992));
#13008=CARTESIAN_POINT('Ctrl Pts',(87.4479740820003,1.84396193431663,4.03163150524466));
#13009=CARTESIAN_POINT('Ctrl Pts',(87.443418752614,1.93077860884527,3.98922704140366));
#13010=CARTESIAN_POINT('Ctrl Pts',(87.4419826161307,1.95814887849518,3.97585839285786));
#13011=CARTESIAN_POINT('Ctrl Pts',(87.4405603908129,1.98537815433257,3.96219410741805));
#13012=CARTESIAN_POINT('Ctrl Pts',(87.439155740593,2.01245694566142,3.94823321505794));
#13013=CARTESIAN_POINT('Ctrl Pts',(87.4342433948206,2.10715695298619,3.89940915224413));
#13014=CARTESIAN_POINT('Ctrl Pts',(87.4294547316289,2.20008468693029,3.84710035194527));
#13015=CARTESIAN_POINT('Ctrl Pts',(87.4246868836489,2.29109450842686,3.79163417302202));
#13016=CARTESIAN_POINT('Ctrl Pts',(87.4237691305853,2.30861279819681,3.78095760450633));
#13017=CARTESIAN_POINT('Ctrl Pts',(87.4228521487585,2.3260601554,3.77016396423666));
#13018=CARTESIAN_POINT('Ctrl Pts',(87.4219352045201,2.3434357221474,3.7592554589208));
#13019=CARTESIAN_POINT('Ctrl Pts',(87.4143866662749,2.48647618701755,3.66945363005947));
#13020=CARTESIAN_POINT('Ctrl Pts',(87.4068405936064,2.62465566138366,3.57186972469084));
#13021=CARTESIAN_POINT('Ctrl Pts',(87.3992916367383,2.75714652993736,3.46709263703067));
#13022=CARTESIAN_POINT('Ctrl Pts',(87.3954802914649,2.82403900984525,3.41419239335634));
#13023=CARTESIAN_POINT('Ctrl Pts',(87.3916682268472,2.88948066590474,3.35945806798491));
#13024=CARTESIAN_POINT('Ctrl Pts',(87.3878548266096,2.95336049953169,3.30296285886929));
#13025=CARTESIAN_POINT('Ctrl Pts',(87.3824646453376,3.04365363988452,3.22310776914367));
#13026=CARTESIAN_POINT('Ctrl Pts',(87.3772364770673,3.13063949483509,3.13951781825546));
#13027=CARTESIAN_POINT('Ctrl Pts',(87.3722562512605,3.21381824072451,3.0523624015897));
#13028=CARTESIAN_POINT('Ctrl Pts',(87.371983837485,3.21836804169512,3.04759508038163));
#13029=CARTESIAN_POINT('Ctrl Pts',(87.3717121655507,3.22290644391039,3.04281710161229));
#13030=CARTESIAN_POINT('Ctrl Pts',(87.3714412495208,3.2274333628932,3.03802849663882));
#13031=CARTESIAN_POINT('Ctrl Pts',(87.366211935062,3.31481351127428,2.94559719519307));
#13032=CARTESIAN_POINT('Ctrl Pts',(87.3610422843428,3.39819330392435,2.84947119216636));
#13033=CARTESIAN_POINT('Ctrl Pts',(87.3558679420249,3.47723242920269,2.75001962188339));
#13034=CARTESIAN_POINT('Ctrl Pts',(87.3506904651807,3.55631943500333,2.65050780557529));
#13035=CARTESIAN_POINT('Ctrl Pts',(87.3455079282499,3.63106015594755,2.54766621272678));
#13036=CARTESIAN_POINT('Ctrl Pts',(87.3402398152633,3.70114167286168,2.44189996909579));
#13037=CARTESIAN_POINT('Ctrl Pts',(87.335372893766,3.76588615387318,2.34418832051926));
#13038=CARTESIAN_POINT('Ctrl Pts',(87.3304324879514,3.82665427084412,2.24398003880654));
#13039=CARTESIAN_POINT('Ctrl Pts',(87.3253476904251,3.88322462821622,2.14162536304834));
#13040=CARTESIAN_POINT('Ctrl Pts',(87.3249206559189,3.88797555379467,2.13302935146696));
#13041=CARTESIAN_POINT('Ctrl Pts',(87.3244926030068,3.89269689942722,2.12441818745693));
#13042=CARTESIAN_POINT('Ctrl Pts',(87.3240634896879,3.89738854879096,2.11579207061174));
#13043=CARTESIAN_POINT('Ctrl Pts',(87.3216382590273,3.92390446285128,2.06703962659732));
#13044=CARTESIAN_POINT('Ctrl Pts',(87.3191790825226,3.94947129899816,2.01781058647708));
#13045=CARTESIAN_POINT('Ctrl Pts',(87.3166782524288,3.97406814418842,1.96814466095132));
#13046=CARTESIAN_POINT('Ctrl Pts',(87.3166762172577,3.97408816105828,1.96810424290746));
#13047=CARTESIAN_POINT('Ctrl Pts',(87.3166741820589,3.97410817728591,1.96806382457419));
#13048=CARTESIAN_POINT('Ctrl Pts',(87.3166721468325,3.97412819287132,1.96802340595155));
#13049=CARTESIAN_POINT('Ctrl Pts',(87.3114868635282,4.02512324822928,1.8650461581332));
#13050=CARTESIAN_POINT('Ctrl Pts',(87.3061121666443,4.0720814299214,1.759903512446));
#13051=CARTESIAN_POINT('Ctrl Pts',(87.3006249341305,4.11485538004488,1.65295572897146));
#13052=CARTESIAN_POINT('Ctrl Pts',(87.3000680823831,4.11919613812506,1.64210252383297));
#13053=CARTESIAN_POINT('Ctrl Pts',(87.2995100716915,4.12349381512763,1.63123077164528));
#13054=CARTESIAN_POINT('Ctrl Pts',(87.2989509824011,4.12774826442953,1.62034087791471));
#13055=CARTESIAN_POINT('Ctrl Pts',(87.2928900141741,4.17386984551746,1.50228585337636));
#13056=CARTESIAN_POINT('Ctrl Pts',(87.2867028218786,4.21491020159689,1.38209288317381));
#13057=CARTESIAN_POINT('Ctrl Pts',(87.280480980815,4.25072302986795,1.26024871219734));
#13058=CARTESIAN_POINT('Ctrl Pts',(87.274265181783,4.28650108029126,1.13852286413002));
#13059=CARTESIAN_POINT('Ctrl Pts',(87.2680151521108,4.31706211786227,1.01514909574692));
#13060=CARTESIAN_POINT('Ctrl Pts',(87.2618048209915,4.34230273810106,0.890614170921266));
#13061=CARTESIAN_POINT('Ctrl Pts',(87.2570866546338,4.36147875995381,0.796001423005591));
#13062=CARTESIAN_POINT('Ctrl Pts',(87.252391521378,4.37758438814031,0.700715537038209));
#13063=CARTESIAN_POINT('Ctrl Pts',(87.2478363532498,4.39042878644756,0.604957194971616));
#13064=CARTESIAN_POINT('Ctrl Pts',(87.2464000699041,4.39447873473821,0.574763773334275));
#13065=CARTESIAN_POINT('Ctrl Pts',(87.2449777018167,4.39820440517015,0.544523766430797));
#13066=CARTESIAN_POINT('Ctrl Pts',(87.2435729145498,4.40159972569208,0.514244537173169));
#13067=CARTESIAN_POINT('Ctrl Pts',(87.2386603570905,4.41347320116494,0.408357719240865));
#13068=CARTESIAN_POINT('Ctrl Pts',(87.2338714695506,4.42146363807649,0.302013713112158));
#13069=CARTESIAN_POINT('Ctrl Pts',(87.2291033900858,4.42576271697741,0.195515259139371));
#13070=CARTESIAN_POINT('Ctrl Pts',(87.2281858778846,4.4265899803178,0.175021970039555));
#13071=CARTESIAN_POINT('Ctrl Pts',(87.2272691361764,4.42728055817177,0.154522806978717));
#13072=CARTESIAN_POINT('Ctrl Pts',(87.2263524320363,4.42783581003968,0.134019705854794));
#13073=CARTESIAN_POINT('Ctrl Pts',(87.2188038983124,4.43240799125576,-0.0348115926004418));
#13074=CARTESIAN_POINT('Ctrl Pts',(87.2112578301234,4.42780862949383,-0.203912158104957));
#13075=CARTESIAN_POINT('Ctrl Pts',(87.2037088776929,4.41406895227369,-0.372266724295081));
#13076=CARTESIAN_POINT('Ctrl Pts',(87.1998975398427,4.40713202263717,-0.457266084974127));
#13077=CARTESIAN_POINT('Ctrl Pts',(87.1960854826396,4.39786434134989,-0.542074925775098));
#13078=CARTESIAN_POINT('Ctrl Pts',(87.1922720898112,4.38626528328757,-0.626560287858358));
#13079=CARTESIAN_POINT('Ctrl Pts',(87.1868829198374,4.36987324128047,-0.745956845476469));
#13080=CARTESIAN_POINT('Ctrl Pts',(87.18165566809,4.34854118073539,-0.864672026658181));
#13081=CARTESIAN_POINT('Ctrl Pts',(87.1766762855012,4.32213291004414,-0.982196215678846));
#13082=CARTESIAN_POINT('Ctrl Pts',(87.1764029378242,4.32068320431873,-0.988647811532593));
#13083=CARTESIAN_POINT('Ctrl Pts',(87.1761303371157,4.31921820531694,-0.995095805879495));
#13084=CARTESIAN_POINT('Ctrl Pts',(87.1758584975946,4.31773789206522,-1.00154011012351));
#13085=CARTESIAN_POINT('Ctrl Pts',(87.1706291943329,4.28926150685784,-1.12550744597788));
#13086=CARTESIAN_POINT('Ctrl Pts',(87.165459555318,4.25549235614025,-1.2481940859127));
#13087=CARTESIAN_POINT('Ctrl Pts',(87.1602852252395,4.21654895949107,-1.36911215257806));
#13088=CARTESIAN_POINT('Ctrl Pts',(87.155107760644,4.17758197162485,-1.49010346925755));
#13089=CARTESIAN_POINT('Ctrl Pts',(87.1499252364988,4.13343412021964,-1.60932387146666));
#13090=CARTESIAN_POINT('Ctrl Pts',(87.1446571368701,4.08426906522461,-1.72628832345511));
#13091=CARTESIAN_POINT('Ctrl Pts',(87.1397902258514,4.03884814216901,-1.83434542569051));
#13092=CARTESIAN_POINT('Ctrl Pts',(87.1348498309491,3.98914481113516,-1.94047754080729));
#13093=CARTESIAN_POINT('Ctrl Pts',(87.1297650447026,3.93532779867126,-2.04430623194306));
#13094=CARTESIAN_POINT('Ctrl Pts',(87.129338013202,3.93080812793682,-2.0530259931345));
#13095=CARTESIAN_POINT('Ctrl Pts',(87.128909963308,3.92625944699761,-2.06172953849333));
#13096=CARTESIAN_POINT('Ctrl Pts',(87.1284808530202,3.92168185746445,-2.07041666055344));
#13097=CARTESIAN_POINT('Ctrl Pts',(87.1260555633436,3.89580976594511,-2.11951543084519));
#13098=CARTESIAN_POINT('Ctrl Pts',(87.1235963261056,3.86901478499991,-2.168088573022));
#13099=CARTESIAN_POINT('Ctrl Pts',(87.1210954329384,3.84131836950711,-2.21609666245408));
#13100=CARTESIAN_POINT('Ctrl Pts',(87.1210933977422,3.84129583050394,-2.21613573084833));
#13101=CARTESIAN_POINT('Ctrl Pts',(87.1210913625185,3.84127329090383,-2.21617479886855));
#13102=CARTESIAN_POINT('Ctrl Pts',(87.1210893272671,3.84125075070682,-2.21621386651472));
#13103=CARTESIAN_POINT('Ctrl Pts',(87.1159040500741,3.78382434531974,-2.3157478006998));
#13104=CARTESIAN_POINT('Ctrl Pts',(87.1105293586286,3.72235764435729,-2.41312273717083));
#13105=CARTESIAN_POINT('Ctrl Pts',(87.1050421308377,3.65706876348978,-2.50801629903429));
#13106=CARTESIAN_POINT('Ctrl Pts',(87.1044852764418,3.65044312269184,-2.51764627961582));
#13107=CARTESIAN_POINT('Ctrl Pts',(87.1039272630813,3.64377816032576,-2.52725069005747));
#13108=CARTESIAN_POINT('Ctrl Pts',(87.103368171103,3.63707413257389,-2.53682918350185));
#13109=CARTESIAN_POINT('Ctrl Pts',(87.0973072046553,3.5643975626333,-2.6406670664137));
#13110=CARTESIAN_POINT('Ctrl Pts',(87.091120013192,3.4871245093646,-2.7414615945206));
#13111=CARTESIAN_POINT('Ctrl Pts',(87.0848981721618,3.405578937502,-2.83882114032578));
#13112=CARTESIAN_POINT('Ctrl Pts',(87.0786823731751,3.32411255472528,-2.93608614005987));
#13113=CARTESIAN_POINT('Ctrl Pts',(87.0724323427522,3.23838221335855,-3.02992308948798));
#13114=CARTESIAN_POINT('Ctrl Pts',(87.0662220102581,3.14873567846447,-3.11997605164627));
#13115=CARTESIAN_POINT('Ctrl Pts',(87.0615037416729,3.08062717867503,-3.18839333248644));
#13116=CARTESIAN_POINT('Ctrl Pts',(87.0568085068176,3.01025603180792,-3.25462847905602));
#13117=CARTESIAN_POINT('Ctrl Pts',(87.0522532353739,2.93768345794995,-3.31841140273829));
#13118=CARTESIAN_POINT('Ctrl Pts',(87.0508170479532,2.91480275392368,-3.33852090307874));
#13119=CARTESIAN_POINT('Ctrl Pts',(87.0493947731304,2.89170351892678,-3.35838639428964));
#13120=CARTESIAN_POINT('Ctrl Pts',(87.0479900754107,2.86838851367361,-3.37799874311116));
#13121=CARTESIAN_POINT('Ctrl Pts',(87.0430776682255,2.78685296497673,-3.44658562975487));
#13122=CARTESIAN_POINT('Ctrl Pts',(87.0382889398302,2.70278417717264,-3.51219462757426));
#13123=CARTESIAN_POINT('Ctrl Pts',(87.0335210244836,2.61654035549795,-3.57481742436555));
#13124=CARTESIAN_POINT('Ctrl Pts',(87.0326033456464,2.59994104023301,-3.58687041003486));
#13125=CARTESIAN_POINT('Ctrl Pts',(87.0316864378192,2.58326102286555,-3.5988128593167));
#13126=CARTESIAN_POINT('Ctrl Pts',(87.0307695675744,2.56650266965896,-3.6106448304546));
#13127=CARTESIAN_POINT('Ctrl Pts',(87.0232210325432,2.42853220222858,-3.7080567043061));
#13128=CARTESIAN_POINT('Ctrl Pts',(87.0156749630928,2.28525257417996,-3.79798508960943));
#13129=CARTESIAN_POINT('Ctrl Pts',(87.0081260094421,2.13752602929942,-3.87989307101794));
#13130=CARTESIAN_POINT('Ctrl Pts',(87.0043146727118,2.06294144014906,-3.92124700064805));
#13131=CARTESIAN_POINT('Ctrl Pts',(87.0005026166394,1.98722314558315,-3.96055559229602));
#13132=CARTESIAN_POINT('Ctrl Pts',(86.9966892249516,1.91048145048875,-3.99774460821275));
#13133=CARTESIAN_POINT('Ctrl Pts',(86.9912997004426,1.80202124486586,-4.05030441039433));
#13134=CARTESIAN_POINT('Ctrl Pts',(86.9860721269399,1.69138886072014,-4.09837461991389));
#13135=CARTESIAN_POINT('Ctrl Pts',(86.981092447861,1.57893298931347,-4.14155930441737));
#13136=CARTESIAN_POINT('Ctrl Pts',(86.980819429462,1.57276742693773,-4.14392696973046));
#13137=CARTESIAN_POINT('Ctrl Pts',(86.9805471562201,1.56659639585105,-4.14627994604861));
#13138=CARTESIAN_POINT('Ctrl Pts',(86.9802756422993,1.56041995793549,-4.14861816704189));
#13139=CARTESIAN_POINT('Ctrl Pts',(86.9750463358532,1.44146293902382,-4.19365185842192));
#13140=CARTESIAN_POINT('Ctrl Pts',(86.9698766938549,1.32063722601068,-4.23357071521643));
#13141=CARTESIAN_POINT('Ctrl Pts',(86.9647023611029,1.19841455402902,-4.26820287365268));
#13142=CARTESIAN_POINT('Ctrl Pts',(86.9595248938412,1.07611784194031,-4.30285601157396));
#13143=CARTESIAN_POINT('Ctrl Pts',(86.9543423673408,0.952422450226131,-4.33221564577044));
#13144=CARTESIAN_POINT('Ctrl Pts',(86.949074265738,0.827822776770507,-4.3561490548337));
#13145=CARTESIAN_POINT('Ctrl Pts',(86.944207350963,0.712711862548233,-4.37825983988892));
#13146=CARTESIAN_POINT('Ctrl Pts',(86.9392669525721,0.596828630513182,-4.39573940968646));
#13147=CARTESIAN_POINT('Ctrl Pts',(86.9341821630361,0.480581574012372,-4.4085183619281));
#13148=CARTESIAN_POINT('Ctrl Pts',(86.9337551334635,0.470818941653778,-4.40959156082378));
#13149=CARTESIAN_POINT('Ctrl Pts',(86.9333270855093,0.461053720111495,-4.4106316263472));
#13150=CARTESIAN_POINT('Ctrl Pts',(86.9328979771739,0.451286138377544,-4.41163852803421));
#13151=CARTESIAN_POINT('Ctrl Pts',(86.9304726880258,0.396080475787726,-4.41732946324301));
#13152=CARTESIAN_POINT('Ctrl Pts',(86.9280134514225,0.340800566886789,-4.42196091961307));
#13153=CARTESIAN_POINT('Ctrl Pts',(86.9255125590039,0.285491117169027,-4.42552889382131));
#13154=CARTESIAN_POINT('Ctrl Pts',(86.9255105238159,0.28544610718554,-4.42553179738411));
#13155=CARTESIAN_POINT('Ctrl Pts',(86.9255084886003,0.285401097182359,-4.42553470024274));
#13156=CARTESIAN_POINT('Ctrl Pts',(86.9255064533572,0.285356087159519,-4.42553760239722));
#13157=CARTESIAN_POINT('Ctrl Pts',(86.9203211737466,0.170682047092974,-4.43293155065508));
#13158=CARTESIAN_POINT('Ctrl Pts',(86.9149464801288,0.0555646764875576,
-4.43576603111863));
#13159=CARTESIAN_POINT('Ctrl Pts',(86.9094592503935,-0.0596068026293469,
-4.43404382642809));
#13160=CARTESIAN_POINT('Ctrl Pts',(86.9089023965005,-0.0712946104312107,
-4.43386905401418));
#13161=CARTESIAN_POINT('Ctrl Pts',(86.9083443836482,-0.0829829395834126,
-4.43364738023689));
#13162=CARTESIAN_POINT('Ctrl Pts',(86.907785292183,-0.0946713593865203,
-4.43337882598583));
#13163=CARTESIAN_POINT('Ctrl Pts',(86.9017243243539,-0.221382534226761,
-4.43046749791641));
#13164=CARTESIAN_POINT('Ctrl Pts',(86.895537131799,-0.348109428700612,-4.4220435073402));
#13165=CARTESIAN_POINT('Ctrl Pts',(86.8893152899021,-0.474346501949595,
-4.40815933176324));
#13166=CARTESIAN_POINT('Ctrl Pts',(86.8830994900267,-0.600460986564145,
-4.39428863908858));
#13167=CARTESIAN_POINT('Ctrl Pts',(86.8768494589391,-0.726086672918377,
-4.37496872859089));
#13168=CARTESIAN_POINT('Ctrl Pts',(86.8706391259347,-0.850734526830391,
-4.35029167322151));
#13169=CARTESIAN_POINT('Ctrl Pts',(86.8659208745263,-0.945434748517955,
-4.33154347547294));
#13170=CARTESIAN_POINT('Ctrl Pts',(86.8612256567654,-1.03957345093702,-4.3097024085963));
#13171=CARTESIAN_POINT('Ctrl Pts',(86.8566704027144,-1.13289191899611,-4.28466967187061));
#13172=CARTESIAN_POINT('Ctrl Pts',(86.8552341984528,-1.16231385243956,-4.27677722004228));
#13173=CARTESIAN_POINT('Ctrl Pts',(86.8538119072514,-1.19165387591231,-4.26856760529915));
#13174=CARTESIAN_POINT('Ctrl Pts',(86.852407193798,-1.22090285747926,-4.26003806115109));
#13175=CARTESIAN_POINT('Ctrl Pts',(86.8474947558015,-1.32318977447885,-4.23020930378668));
#13176=CARTESIAN_POINT('Ctrl Pts',(86.842705994816,-1.42440293531723,-4.19662121719783));
#13177=CARTESIAN_POINT('Ctrl Pts',(86.8379380458908,-1.52433681414696,-4.15956730069596));
#13178=CARTESIAN_POINT('Ctrl Pts',(86.8370203997396,-1.5435702289191,-4.1524358518484));
#13179=CARTESIAN_POINT('Ctrl Pts',(86.836103524496,-1.56275640043473,-4.1451759642625));
#13180=CARTESIAN_POINT('Ctrl Pts',(86.8351866868319,-1.5818940653392,-4.13778963924228));
#13181=CARTESIAN_POINT('Ctrl Pts',(86.8276381514256,-1.73945886310671,-4.07697632613084));
#13182=CARTESIAN_POINT('Ctrl Pts',(86.8200920815852,-1.89373933150401,-4.00759545907864));
#13183=CARTESIAN_POINT('Ctrl Pts',(86.8125431275321,-2.04381057454587,-3.93006693051597));
#13184=CARTESIAN_POINT('Ctrl Pts',(86.8087317883931,-2.11957900527457,-3.8909240885775));
#13185=CARTESIAN_POINT('Ctrl Pts',(86.8049197299082,-2.19427382669694,-3.8497037307355));
#13186=CARTESIAN_POINT('Ctrl Pts',(86.8011063358038,-2.26777209874956,-3.80645649505934));
#13187=CARTESIAN_POINT('Ctrl Pts',(86.7957167606299,-2.37164923589725,-3.74533398284062));
#13188=CARTESIAN_POINT('Ctrl Pts',(86.7904891414525,-2.47299431900228,-3.67991443977688));
#13189=CARTESIAN_POINT('Ctrl Pts',(86.7855094206065,-2.57128450374058,-3.61026854169116));
#13190=CARTESIAN_POINT('Ctrl Pts',(86.7852364479724,-2.57667246251633,-3.60645077261498));
#13191=CARTESIAN_POINT('Ctrl Pts',(86.7849642202449,-2.58205123188107,-3.60262031242433));
#13192=CARTESIAN_POINT('Ctrl Pts',(86.7846927515803,-2.58742072236894,-3.5987771758364));
#13193=CARTESIAN_POINT('Ctrl Pts',(86.7794634441658,-2.69085334677371,-3.52474674331534));
#13194=CARTESIAN_POINT('Ctrl Pts',(86.7742938009672,-2.79106535992229,-3.44632526980668));
#13195=CARTESIAN_POINT('Ctrl Pts',(86.7691194667172,-2.88765218381384,-3.36381005662206));
#13196=CARTESIAN_POINT('Ctrl Pts',(86.7639419979513,-2.98429751821472,-3.28124485724929));
#13197=CARTESIAN_POINT('Ctrl Pts',(86.7587594696479,-3.07731295376005,-3.19458071305253));
#13198=CARTESIAN_POINT('Ctrl Pts',(86.7534913658966,-3.16631392253261,-3.10415548793341));
#13199=CARTESIAN_POINT('Ctrl Pts',(86.748624450639,-3.24853708922042,-3.02061652807388));
#13200=CARTESIAN_POINT('Ctrl Pts',(86.7436840515152,-3.32733425175784,-2.93386709805201));
#13201=CARTESIAN_POINT('Ctrl Pts',(86.7385992610495,-3.40242116709039,-2.84420867629675));
#13202=CARTESIAN_POINT('Ctrl Pts',(86.7381722297014,-3.40872712343126,-2.83667897434168));
#13203=CARTESIAN_POINT('Ctrl Pts',(86.7377441799624,-3.41500694072864,-2.82912874699072));
#13204=CARTESIAN_POINT('Ctrl Pts',(86.737315069832,-3.42126046666564,-2.82155816792788));
#13205=CARTESIAN_POINT('Ctrl Pts',(86.7348897946573,-3.45660458962502,-2.77877023037616));
#13206=CARTESIAN_POINT('Ctrl Pts',(86.7324305723846,-3.49110816417236,-2.73533309406431));
#13207=CARTESIAN_POINT('Ctrl Pts',(86.7299296948,-3.52474307265858,-2.6912817437279));
#13208=CARTESIAN_POINT('Ctrl Pts',(86.7299276596136,-3.5247704443736,-2.69124589522818));
#13209=CARTESIAN_POINT('Ctrl Pts',(86.7299256243996,-3.52479781551352,-2.69121004632165));
#13210=CARTESIAN_POINT('Ctrl Pts',(86.729923589158,-3.52482518607833,-2.69117419700836));
#13211=CARTESIAN_POINT('Ctrl Pts',(86.7247422939637,-3.59450486297602,-2.59990941734138));
#13212=CARTESIAN_POINT('Ctrl Pts',(86.7193716830042,-3.66064459925158,-2.50574769312633));
#13213=CARTESIAN_POINT('Ctrl Pts',(86.7138884207033,-3.72303036313091,-2.40901285428436));
#13214=CARTESIAN_POINT('Ctrl Pts',(86.7133273451294,-3.72941399505467,-2.3991144485108));
#13215=CARTESIAN_POINT('Ctrl Pts',(86.7127650900471,-3.73575832287904,-2.38918914607351));
#13216=CARTESIAN_POINT('Ctrl Pts',(86.7122017375937,-3.74206311899499,-2.37923732457273));
#13217=CARTESIAN_POINT('Ctrl Pts',(86.7061401265042,-3.80990203906345,-2.27215680826239));
#13218=CARTESIAN_POINT('Ctrl Pts',(86.6999520037199,-3.8731643273773,-2.16200003631719));
#13219=CARTESIAN_POINT('Ctrl Pts',(86.6937289581471,-3.93161176112492,-2.04921595587832));
#13220=CARTESIAN_POINT('Ctrl Pts',(86.687511954482,-3.99000244870243,-1.93654137664771));
#13221=CARTESIAN_POINT('Ctrl Pts',(86.6812604481921,-4.04358797074338,-1.8212447305624));
#13222=CARTESIAN_POINT('Ctrl Pts',(86.6750484188064,-4.09217204731032,-1.70378344503025));
#13223=CARTESIAN_POINT('Ctrl Pts',(86.6703248143745,-4.12911520149415,-1.61446631298462));
#13224=CARTESIAN_POINT('Ctrl Pts',(86.6656241563928,-4.16316753521566,-1.52389481419493));
#13225=CARTESIAN_POINT('Ctrl Pts',(86.6610629657549,-4.19410319316702,-1.43223010271598));
#13226=CARTESIAN_POINT('Ctrl Pts',(86.659630195034,-4.2038207665952,-1.40343619227226));
#13227=CARTESIAN_POINT('Ctrl Pts',(86.6582111859304,-4.21323068902726,-1.37453477885787));
#13228=CARTESIAN_POINT('Ctrl Pts',(86.6568095500407,-4.22232567036051,-1.34553187995964));
#13229=CARTESIAN_POINT('Ctrl Pts',(86.6518979948167,-4.25419593239208,-1.24390110649319));
#13230=CARTESIAN_POINT('Ctrl Pts',(86.6471104298357,-4.28234537290711,-1.14107513937407));
#13231=CARTESIAN_POINT('Ctrl Pts',(86.6423435868528,-4.30690389679484,-1.0373873232451));
#13232=CARTESIAN_POINT('Ctrl Pts',(86.6414221494231,-4.31165109388304,-1.01734432306076));
#13233=CARTESIAN_POINT('Ctrl Pts',(86.6405014862797,-4.31626414482736,-0.997268966085684));
#13234=CARTESIAN_POINT('Ctrl Pts',(86.6395808515379,-4.32074402446021,-0.977163438477885));
#13235=CARTESIAN_POINT('Ctrl Pts',(86.6320580262991,-4.35735067206886,-0.812874210989112));
#13236=CARTESIAN_POINT('Ctrl Pts',(86.6245370168181,-4.38507002416069,-0.646569015077811));
#13237=CARTESIAN_POINT('Ctrl Pts',(86.6170124913105,-4.40373588982307,-0.479238878070492));
#13238=CARTESIAN_POINT('Ctrl Pts',(86.6131701100334,-4.41326757028192,-0.393792136626068));
#13239=CARTESIAN_POINT('Ctrl Pts',(86.6093268276084,-4.42043756843836,-0.308078337635977));
#13240=CARTESIAN_POINT('Ctrl Pts',(86.6054820079124,-4.42521857890916,-0.222230952065899));
#13241=CARTESIAN_POINT('Ctrl Pts',(86.6021218392718,-4.42939692866916,-0.14720488695166));
#13242=CARTESIAN_POINT('Ctrl Pts',(86.5987605042762,-4.4317505286615,-0.0720731711144324));
#13243=CARTESIAN_POINT('Ctrl Pts',(86.5955266375048,-4.43203607817087,0.00306014718217265));
#13244=CARTESIAN_POINT('',(85.3499542888372,-4.43459181384856,-0.00121389427323767));
#13245=CARTESIAN_POINT('Ctrl Pts',(86.595526637467,-4.43203607817194,0.00306014809321447));
#13246=CARTESIAN_POINT('Ctrl Pts',(86.5898840957589,-4.43219582861552,0.138943254598236));
#13247=CARTESIAN_POINT('Ctrl Pts',(86.5843386468504,-4.42615867458735,0.274609641975266));
#13248=CARTESIAN_POINT('Ctrl Pts',(86.5788171430829,-4.41396515084367,0.409536003282953));
#13249=CARTESIAN_POINT('Ctrl Pts',(86.578365432176,-4.41296760599,0.420574247860671));
#13250=CARTESIAN_POINT('Ctrl Pts',(86.5779138815287,-4.41192884278177,0.431607564185417));
#13251=CARTESIAN_POINT('Ctrl Pts',(86.5774624510902,-4.41084887490884,0.442635678585354));
#13252=CARTESIAN_POINT('Ctrl Pts',(86.5721566451797,-4.39815566808379,0.572252624123666));
#13253=CARTESIAN_POINT('Ctrl Pts',(86.5668669930949,-4.37977198140099,0.701148564835273));
#13254=CARTESIAN_POINT('Ctrl Pts',(86.5615075352585,-4.35575864894718,0.828850424506818));
#13255=CARTESIAN_POINT('Ctrl Pts',(86.5608048865756,-4.35261039460215,0.84559270446119));
#13256=CARTESIAN_POINT('Ctrl Pts',(86.5601010380454,-4.34936535441272,0.862314530342428));
#13257=CARTESIAN_POINT('Ctrl Pts',(86.5593957959606,-4.34602364389209,0.879014898987103));
#13258=CARTESIAN_POINT('Ctrl Pts',(86.5542953886152,-4.32185593573823,0.999794252247937));
#13259=CARTESIAN_POINT('Ctrl Pts',(86.5491214484734,-4.29263264903697,1.11944867369579));
#13260=CARTESIAN_POINT('Ctrl Pts',(86.5437895135129,-4.25843415252819,1.23756406555488));
#13261=CARTESIAN_POINT('Ctrl Pts',(86.5427220025229,-4.25158724401638,1.26121204322802));
#13262=CARTESIAN_POINT('Ctrl Pts',(86.5416481584107,-4.24454090257586,1.28479849707436));
#13263=CARTESIAN_POINT('Ctrl Pts',(86.5405673033412,-4.23729575710899,1.3083203545886));
#13264=CARTESIAN_POINT('Ctrl Pts',(86.5385206154844,-4.22357647904161,1.35286092390836));
#13265=CARTESIAN_POINT('Ctrl Pts',(86.5364487051521,-4.20914485426276,1.39716888383166));
#13266=CARTESIAN_POINT('Ctrl Pts',(86.5343468386373,-4.19400659716224,1.44122164868843));
#13267=CARTESIAN_POINT('Ctrl Pts',(86.5343448034482,-4.19399193913564,1.4412643039687));
#13268=CARTESIAN_POINT('Ctrl Pts',(86.5343427682311,-4.19397728044653,1.44130695900981));
#13269=CARTESIAN_POINT('Ctrl Pts',(86.5343407329859,-4.19396262109495,1.44134961381174));
#13270=CARTESIAN_POINT('Ctrl Pts',(86.5291554539045,-4.15661438039804,1.55002302960332));
#13271=CARTESIAN_POINT('Ctrl Pts',(86.5237807607676,-4.11488773180388,1.65734929203859));
#13272=CARTESIAN_POINT('Ctrl Pts',(86.518293531478,-4.0689351687674,1.76297028493064));
#13273=CARTESIAN_POINT('Ctrl Pts',(86.5177366776166,-4.06427182032342,1.77368889256226));
#13274=CARTESIAN_POINT('Ctrl Pts',(86.5171786647955,-4.05956498879926,1.78438991524111));
#13275=CARTESIAN_POINT('Ctrl Pts',(86.516619573361,-4.05481485937499,1.79507296354883));
#13276=CARTESIAN_POINT('Ctrl Pts',(86.5105586060111,-4.00331992031054,1.91088515991082));
#13277=CARTESIAN_POINT('Ctrl Pts',(86.5043714138943,-3.94673164378681,2.02458842439447));
#13278=CARTESIAN_POINT('Ctrl Pts',(86.4981495724106,-3.88529318864992,2.13573643973071));
#13279=CARTESIAN_POINT('Ctrl Pts',(86.4919337729579,-3.82391439640502,2.2467765192144));
#13280=CARTESIAN_POINT('Ctrl Pts',(86.4856837422683,-3.7576951524283,2.3552665180663));
#13281=CARTESIAN_POINT('Ctrl Pts',(86.4794734096533,-3.68690879741531,2.46079060385499));
#13282=CARTESIAN_POINT('Ctrl Pts',(86.4747551614893,-3.63312945735728,2.54096164378072));
#13283=CARTESIAN_POINT('Ctrl Pts',(86.4700599469391,-3.57671220342748,2.61942314447183));
#13284=CARTESIAN_POINT('Ctrl Pts',(86.4655046961467,-3.51766551356299,2.695898297196));
#13285=CARTESIAN_POINT('Ctrl Pts',(86.4640684891769,-3.49904891671944,2.72000984502505));
#13286=CARTESIAN_POINT('Ctrl Pts',(86.4626461953444,-3.48017118064383,2.74392363369086));
#13287=CARTESIAN_POINT('Ctrl Pts',(86.4612414793683,-3.46103326987111,2.76763017021447));
#13288=CARTESIAN_POINT('Ctrl Pts',(86.4563290396104,-3.39410597968449,2.85053442596512));
#13289=CARTESIAN_POINT('Ctrl Pts',(86.4515402767393,-3.3241230461927,2.93099971165257));
#13290=CARTESIAN_POINT('Ctrl Pts',(86.4467723258545,-3.2514344884534,3.00894941425027));
#13291=CARTESIAN_POINT('Ctrl Pts',(86.4458546824062,-3.23744479342866,3.02395167320996));
#13292=CARTESIAN_POINT('Ctrl Pts',(86.4449378098577,-3.22335476887946,3.03886086123303));
#13293=CARTESIAN_POINT('Ctrl Pts',(86.4440209748886,-3.20916674829457,3.05367658334066));
#13294=CARTESIAN_POINT('Ctrl Pts',(86.4364724397945,-3.09235317234639,3.17565818530495));
#13295=CARTESIAN_POINT('Ctrl Pts',(86.428926370269,-2.96889825024285,3.29130872838656));
#13296=CARTESIAN_POINT('Ctrl Pts',(86.4213774165328,-2.8395457373524,3.39993642494658));
#13297=CARTESIAN_POINT('Ctrl Pts',(86.4175660785136,-2.77423785926992,3.45478069665648));
#13298=CARTESIAN_POINT('Ctrl Pts',(86.4137540211494,-2.70742632237651,3.5078339594565));
#13299=CARTESIAN_POINT('Ctrl Pts',(86.4099406281668,-2.63920521289093,3.5590022653388));
#13300=CARTESIAN_POINT('Ctrl Pts',(86.4045511286379,-2.54278776021794,3.63131885104026));
#13301=CARTESIAN_POINT('Ctrl Pts',(86.3993235779102,-2.44338026879274,3.69964369565582));
#13302=CARTESIAN_POINT('Ctrl Pts',(86.3943439199277,-2.34124934016117,3.76352153528519));
#13303=CARTESIAN_POINT('Ctrl Pts',(86.3940708776871,-2.3356493456058,3.76702405463879));
#13304=CARTESIAN_POINT('Ctrl Pts',(86.3937985807351,-2.33004117476534,3.7705131983715));
#13305=CARTESIAN_POINT('Ctrl Pts',(86.3935270432396,-2.32442487571878,3.77398888953018));
#13306=CARTESIAN_POINT('Ctrl Pts',(86.3882977366634,-2.21626541332121,3.84092422970094));
#13307=CARTESIAN_POINT('Ctrl Pts',(86.3831280944019,-2.10529429770412,3.90319607655686));
#13308=CARTESIAN_POINT('Ctrl Pts',(86.3779537612096,-1.99194172975216,3.96054558939924));
#13309=CARTESIAN_POINT('Ctrl Pts',(86.3727762935036,-1.87852049494594,4.01792984349814));
#13310=CARTESIAN_POINT('Ctrl Pts',(86.3675937663811,-1.76271481841343,4.0703854124142));
#13311=CARTESIAN_POINT('Ctrl Pts',(86.3623256639482,-1.64498462590344,4.11768754589881));
#13312=CARTESIAN_POINT('Ctrl Pts',(86.3574587493474,-1.53622007544583,4.16138742589096));
#13313=CARTESIAN_POINT('Ctrl Pts',(86.3525183509811,-1.42581246032295,4.200689015183));
#13314=CARTESIAN_POINT('Ctrl Pts',(86.3474335613535,-1.31414948416729,4.23544613142731));
#13315=CARTESIAN_POINT('Ctrl Pts',(86.3470065307072,-1.30477180753288,4.23836510249637));
#13316=CARTESIAN_POINT('Ctrl Pts',(86.3465784816734,-1.29538525792704,4.24125204537026));
#13317=CARTESIAN_POINT('Ctrl Pts',(86.3461493722522,-1.28599005430222,4.24410688638762));
#13318=CARTESIAN_POINT('Ctrl Pts',(86.3437240899407,-1.23288932978963,4.26024215417355));
#13319=CARTESIAN_POINT('Ctrl Pts',(86.3412648603392,-1.17951327293067,4.27535166039204));
#13320=CARTESIAN_POINT('Ctrl Pts',(86.3387639751587,-1.12590500003043,4.28942293282578));
#13321=CARTESIAN_POINT('Ctrl Pts',(86.3387619399709,-1.12586137431477,4.28943438384438));
#13322=CARTESIAN_POINT('Ctrl Pts',(86.3387599047554,-1.12581774844521,4.28944583417556));
#13323=CARTESIAN_POINT('Ctrl Pts',(86.3387578695124,-1.12577412242181,4.28945728381933));
#13324=CARTESIAN_POINT('Ctrl Pts',(86.3335725900635,-1.01462615662874,4.31862805197162));
#13325=CARTESIAN_POINT('Ctrl Pts',(86.3281978965953,-0.902171760511038,
4.34340808868859));
#13326=CARTESIAN_POINT('Ctrl Pts',(86.3227106670089,-0.788793515388748,
4.36372574881666));
#13327=CARTESIAN_POINT('Ctrl Pts',(86.3221538132375,-0.777287690382657,
4.36578762093079));
#13328=CARTESIAN_POINT('Ctrl Pts',(86.3215958005074,-0.765772391249227,
4.36780355560554));
#13329=CARTESIAN_POINT('Ctrl Pts',(86.3210367091646,-0.754248044742652,
4.36977349104319));
#13330=CARTESIAN_POINT('Ctrl Pts',(86.3149757416187,-0.629315525087442,
4.39112906184654));
#13331=CARTESIAN_POINT('Ctrl Pts',(86.3087885493506,-0.503314160078422,
4.40707655958354));
#13332=CARTESIAN_POINT('Ctrl Pts',(86.3025667077508,-0.376750202562136,
4.4175708908222));
#13333=CARTESIAN_POINT('Ctrl Pts',(86.2963509081796,-0.250309151268211,
4.42805503101884));
#13334=CARTESIAN_POINT('Ctrl Pts',(86.2901008774065,-0.123306599074165,
4.43309696528657));
#13335=CARTESIAN_POINT('Ctrl Pts',(86.2838905447321,0.00375983736620393,
4.43269362025351));
#13336=CARTESIAN_POINT('Ctrl Pts',(86.2791722989182,0.100297448676526,4.43238718240008));
#13337=CARTESIAN_POINT('Ctrl Pts',(86.2744770867086,0.196874904896678,4.42893757612002));
#13338=CARTESIAN_POINT('Ctrl Pts',(86.2699218382983,0.293257138992177,4.42219838301227));
#13339=CARTESIAN_POINT('Ctrl Pts',(86.2684856290359,0.323645176014095,4.42007360502202));
#13340=CARTESIAN_POINT('Ctrl Pts',(86.2670633329739,0.354013419053023,4.41762185408007));
#13341=CARTESIAN_POINT('Ctrl Pts',(86.2656586148563,0.384353433004181,4.41483866957661));
#13342=CARTESIAN_POINT('Ctrl Pts',(86.2607461705137,0.490455595436704,4.40510558590888));
#13343=CARTESIAN_POINT('Ctrl Pts',(86.2559574027941,0.596222158195863,4.39147725368983));
#13344=CARTESIAN_POINT('Ctrl Pts',(86.251189446914,0.701395296850439,4.37420248981706));
#13345=CARTESIAN_POINT('Ctrl Pts',(86.2502718083016,0.72163687111139,4.37087779664689));
#13346=CARTESIAN_POINT('Ctrl Pts',(86.2493549405738,0.741856616416203,4.36741800606075));
#13347=CARTESIAN_POINT('Ctrl Pts',(86.2484381104248,0.762052910300203,4.36382484101895));
#13348=CARTESIAN_POINT('Ctrl Pts',(86.2408895753065,0.928335000633039,4.33424124526154));
#13349=CARTESIAN_POINT('Ctrl Pts',(86.2333435057538,1.09303045899132,4.29562037199433));
#13350=CARTESIAN_POINT('Ctrl Pts',(86.2257945519879,1.25515119566418,4.24819763754719));
#13351=CARTESIAN_POINT('Ctrl Pts',(86.2219832135279,1.33700320032816,4.22425470488596));
#13352=CARTESIAN_POINT('Ctrl Pts',(86.218171155722,1.41819837270992,4.19806738441553));
#13353=CARTESIAN_POINT('Ctrl Pts',(86.2143577622969,1.4986063618513,4.16966188842326));
#13354=CARTESIAN_POINT('Ctrl Pts',(86.2089682434684,1.6122480250964,4.12951602923274));
#13355=CARTESIAN_POINT('Ctrl Pts',(86.203740675327,1.72422545010329,4.08466857362693));
#13356=CARTESIAN_POINT('Ctrl Pts',(86.1987610014044,1.83401193600097,4.03508897922655));
#13357=CARTESIAN_POINT('Ctrl Pts',(86.1984879768791,1.84003128659781,4.03237063954472));
#13358=CARTESIAN_POINT('Ctrl Pts',(86.1982156975453,1.84604403978771,4.0296380812244));
#13359=CARTESIAN_POINT('Ctrl Pts',(86.197944177568,1.85205010488924,4.02689130161306));
#13360=CARTESIAN_POINT('Ctrl Pts',(86.1927148708447,1.96772320168933,3.97399002623559));
#13361=CARTESIAN_POINT('Ctrl Pts',(86.1875452283948,2.08107412016809,3.91616319949736));
#13362=CARTESIAN_POINT('Ctrl Pts',(86.182370894962,2.19164892640812,3.85362533328131));
#13363=CARTESIAN_POINT('Ctrl Pts',(86.1771934270152,2.30229071678806,3.791049582801));
#13364=CARTESIAN_POINT('Ctrl Pts',(86.1720108995998,2.41015276677152,3.72375678365849));
#13365=CARTESIAN_POINT('Ctrl Pts',(86.1667427968143,2.51479303267953,3.65200508658382));
#13366=CARTESIAN_POINT('Ctrl Pts',(86.1618758821495,2.61146450349588,3.58571758215531));
#13367=CARTESIAN_POINT('Ctrl Pts',(86.1569354836762,2.70538659224564,3.51562409301069));
#13368=CARTESIAN_POINT('Ctrl Pts',(86.1518506939089,2.79622268420564,3.44196622604107));
#13369=CARTESIAN_POINT('Ctrl Pts',(86.1514236629565,2.80385128334945,3.43578028905529));
#13370=CARTESIAN_POINT('Ctrl Pts',(86.150995613615,2.81145814736353,3.42956921003236));
#13371=CARTESIAN_POINT('Ctrl Pts',(86.1505665038843,2.81904309354882,3.42333313034923));
#13372=CARTESIAN_POINT('Ctrl Pts',(86.1481412239167,2.86191235687148,3.38808750888977));
#13373=CARTESIAN_POINT('Ctrl Pts',(86.1456819967187,2.90408061354856,3.35204402790925));
#13374=CARTESIAN_POINT('Ctrl Pts',(86.1431811140263,2.94551357861408,3.31523165464269));
#13375=CARTESIAN_POINT('Ctrl Pts',(86.1431790788384,2.94554729625724,3.31520169718095));
#13376=CARTESIAN_POINT('Ctrl Pts',(86.1431770436228,2.94558101341364,3.31517173921001));
#13377=CARTESIAN_POINT('Ctrl Pts',(86.1431750083797,2.94561473008326,3.3151417807299));
#13378=CARTESIAN_POINT('Ctrl Pts',(86.1379897289487,3.03151618984276,3.23881522763576));
#13379=CARTESIAN_POINT('Ctrl Pts',(86.1326150355066,3.11448791527129,3.15896703602293));
#13380=CARTESIAN_POINT('Ctrl Pts',(86.1271278059603,3.19425816325917,3.0758758762552));
#13381=CARTESIAN_POINT('Ctrl Pts',(86.1265709523188,3.20235338739831,3.0674436401864));
#13382=CARTESIAN_POINT('Ctrl Pts',(86.1260129397191,3.21041563415425,3.05897804999534));
#13383=CARTESIAN_POINT('Ctrl Pts',(86.1254538485075,3.21844461548815,3.05047942657368));
#13384=CARTESIAN_POINT('Ctrl Pts',(86.1193928811413,3.30548478502846,2.95834798514696));
#13385=CARTESIAN_POINT('Ctrl Pts',(86.1132056890736,3.38861683791079,2.86232857457603));
#13386=CARTESIAN_POINT('Ctrl Pts',(86.1069838476934,3.46752255960513,2.76281750892179));
#13387=CARTESIAN_POINT('Ctrl Pts',(86.1007680483423,3.54635165596562,2.66340307844765));
#13388=CARTESIAN_POINT('Ctrl Pts',(86.0945180178085,3.62096293755536,2.56050397832784));
#13389=CARTESIAN_POINT('Ctrl Pts',(86.0883076853898,3.69107794818618,2.45453263297218));
#13390=CARTESIAN_POINT('Ctrl Pts',(86.0835894400834,3.74434720939639,2.37402183755535));
#13391=CARTESIAN_POINT('Ctrl Pts',(86.0788942283879,3.79502274304321,2.29173518500281));
#13392=CARTESIAN_POINT('Ctrl Pts',(86.0743389805092,3.84285236572728,2.20778712345346));
#13393=CARTESIAN_POINT('Ctrl Pts',(86.0729027710171,3.85793241404427,2.18131940840073));
#13394=CARTESIAN_POINT('Ctrl Pts',(86.0714804747347,3.87272937300033,2.15468687949912));
#13395=CARTESIAN_POINT('Ctrl Pts',(86.0700757564095,3.88723485360502,2.1278940835062));
#13396=CARTESIAN_POINT('Ctrl Pts',(86.0651633114149,3.93796201670671,2.03419691004993));
#13397=CARTESIAN_POINT('Ctrl Pts',(86.0603745429983,3.98526139034097,1.93861934937803));
#13398=CARTESIAN_POINT('Ctrl Pts',(86.0556065863939,4.02919709767552,1.84151392321606));
#13399=CARTESIAN_POINT('Ctrl Pts',(86.0546889487526,4.03765293362169,1.82282507983735));
#13400=CARTESIAN_POINT('Ctrl Pts',(86.0537720819931,4.04598423569971,1.80407949977676));
#13401=CARTESIAN_POINT('Ctrl Pts',(86.0528552528123,4.0541915382368,1.78527948855819));
#13402=CARTESIAN_POINT('Ctrl Pts',(86.0453067179233,4.1217647687229,1.6304932496601));
#13403=CARTESIAN_POINT('Ctrl Pts',(86.0377606485988,4.18093727000537,1.47201681774839));
#13404=CARTESIAN_POINT('Ctrl Pts',(86.0302116950601,4.2313571249296,1.31080302876705));
#13405=CARTESIAN_POINT('Ctrl Pts',(86.0264003568354,4.25681325197743,1.22940892915413));
#13406=CARTESIAN_POINT('Ctrl Pts',(86.0225882992646,4.28003737230099,1.14731708322164));
#13407=CARTESIAN_POINT('Ctrl Pts',(86.0187749060743,4.30097902863963,1.06465050526195));
#13408=CARTESIAN_POINT('Ctrl Pts',(86.0133853695236,4.33057624472483,0.947816357507269));
#13409=CARTESIAN_POINT('Ctrl Pts',(86.0081577854476,4.35533792725017,0.829760468080612));
#13410=CARTESIAN_POINT('Ctrl Pts',(86.0031780969979,4.37494663312993,0.710904240823791));
#13411=CARTESIAN_POINT('Ctrl Pts',(86.0029050891604,4.37602166632583,0.704388033654169));
#13412=CARTESIAN_POINT('Ctrl Pts',(86.0026328264232,4.37708121044841,0.69786943392072));
#13413=CARTESIAN_POINT('Ctrl Pts',(86.0023613229485,4.37812521302266,0.691348515606644));
#13414=CARTESIAN_POINT('Ctrl Pts',(85.9971320165779,4.39823327727006,0.565752039462315));
#13415=CARTESIAN_POINT('Ctrl Pts',(85.9919623744859,4.41295467258498,0.439357213929078));
#13416=CARTESIAN_POINT('Ctrl Pts',(85.9867880414143,4.42221624186131,0.312660747524827));
#13417=CARTESIAN_POINT('Ctrl Pts',(85.9816105738279,4.43148342162433,0.185887530753862));
#13418=CARTESIAN_POINT('Ctrl Pts',(85.9764280467761,4.43528376276548,0.0588123608202801));
#13419=CARTESIAN_POINT('Ctrl Pts',(85.971159944355,4.43358701788811,-0.0680537539876058));
#13420=CARTESIAN_POINT('Ctrl Pts',(85.966293029979,4.43201948723363,-0.185258483248564));
#13421=CARTESIAN_POINT('Ctrl Pts',(85.9613526317935,4.42576015882048,-0.302285300534199));
#13422=CARTESIAN_POINT('Ctrl Pts',(85.9562678423078,4.41482347107894,-0.418720110591728));
#13423=CARTESIAN_POINT('Ctrl Pts',(85.9558408114293,4.41390498597982,-0.428498540824374));
#13424=CARTESIAN_POINT('Ctrl Pts',(85.9554127621619,4.412953526267,-0.438272822310485));
#13425=CARTESIAN_POINT('Ctrl Pts',(85.9549836525054,4.41196910830211,-0.448042724618684));
#13426=CARTESIAN_POINT('Ctrl Pts',(85.9525583701489,4.40640528216577,-0.503261178314962));
#13427=CARTESIAN_POINT('Ctrl Pts',(85.95009914049,4.39978879021105,-0.558338602336901));
#13428=CARTESIAN_POINT('Ctrl Pts',(85.9475982552398,4.39212473073041,-0.613230403193613));
#13429=CARTESIAN_POINT('Ctrl Pts',(85.9475962200502,4.39211849381327,-0.613275073464575));
#13430=CARTESIAN_POINT('Ctrl Pts',(85.947594184833,4.39211225620248,-0.61331974361277));
#13431=CARTESIAN_POINT('Ctrl Pts',(85.9475921495882,4.39210601789805,-0.613364413638149));
#13432=CARTESIAN_POINT('Ctrl Pts',(85.9424068704086,4.37621242585401,-0.727172126655377));
#13433=CARTESIAN_POINT('Ctrl Pts',(85.93703217718,4.35576368154846,-0.840494181412317));
#13434=CARTESIAN_POINT('Ctrl Pts',(85.9315449478011,4.33084103589823,-0.952949920937747));
#13435=CARTESIAN_POINT('Ctrl Pts',(85.9309880938758,4.32831184090763,-0.964362132027367));
#13436=CARTESIAN_POINT('Ctrl Pts',(85.9304300809907,4.32573660380383,-0.975765391395718));
#13437=CARTESIAN_POINT('Ctrl Pts',(85.9298709894921,4.32311543194047,-0.987159281414365));
#13438=CARTESIAN_POINT('Ctrl Pts',(85.9238100219872,4.29469998021658,-1.11067752006864));
#13439=CARTESIAN_POINT('Ctrl Pts',(85.9176228297165,4.26088205263452,-1.23309897558197));
#13440=CARTESIAN_POINT('Ctrl Pts',(85.9114009880802,4.22181504041481,-1.35393908995992));
#13441=CARTESIAN_POINT('Ctrl Pts',(85.9051851884749,4.18278596617458,-1.47466185649065));
#13442=CARTESIAN_POINT('Ctrl Pts',(85.8989351576339,4.13851834258754,-1.59380649644786));
#13443=CARTESIAN_POINT('Ctrl Pts',(85.8927248248716,4.08920101189957,-1.71091260746274));
#13444=CARTESIAN_POINT('Ctrl Pts',(85.8880065829692,4.05173263378374,-1.79988287381678));
#13445=CARTESIAN_POINT('Ctrl Pts',(85.8833113746208,4.01134828387334,-1.88767918590884));
#13446=CARTESIAN_POINT('Ctrl Pts',(85.8787561301198,3.96800338770175,-1.97402821645276));
#13447=CARTESIAN_POINT('Ctrl Pts',(85.8773199170399,3.95433727014978,-2.00125301351398));
#13448=CARTESIAN_POINT('Ctrl Pts',(85.875897617263,3.9403770330886,-2.0283335954952));
#13449=CARTESIAN_POINT('Ctrl Pts',(85.8744928955748,3.92612180922687,-2.05526045989324));
#13450=CARTESIAN_POINT('Ctrl Pts',(85.8695804485481,3.87626991851789,-2.14942629791357));
#13451=CARTESIAN_POINT('Ctrl Pts',(85.8647916779767,3.82295261903395,-2.24178200764895));
#13452=CARTESIAN_POINT('Ctrl Pts',(85.8600237191508,3.76649884035913,-2.33218550156041));
#13453=CARTESIAN_POINT('Ctrl Pts',(85.8591060838274,3.75563381753786,-2.34958444362464));
#13454=CARTESIAN_POINT('Ctrl Pts',(85.8581892193786,3.74465253116239,-2.36691120306815));
#13455=CARTESIAN_POINT('Ctrl Pts',(85.8572723925084,3.73355719617822,-2.38416494630189));
#13456=CARTESIAN_POINT('Ctrl Pts',(85.8497238572283,3.64220567682109,-2.52622065361032));
#13457=CARTESIAN_POINT('Ctrl Pts',(85.8421777875189,3.5431253917475,-2.66333106288721));
#13458=CARTESIAN_POINT('Ctrl Pts',(85.8346288336008,3.43691419708384,-2.79467501010445));
#13459=CARTESIAN_POINT('Ctrl Pts',(85.8308174959047,3.38328998181449,-2.86098832220123));
#13460=CARTESIAN_POINT('Ctrl Pts',(85.8270054388642,3.32784757267642,-2.92583096377285));
#13461=CARTESIAN_POINT('Ctrl Pts',(85.823192046206,3.27066136956487,-2.98909273912823));
#13462=CARTESIAN_POINT('Ctrl Pts',(85.8178026498303,3.18984118045341,-3.07849942062754));
#13463=CARTESIAN_POINT('Ctrl Pts',(85.8125751922913,3.10532341564083,-3.16455941835129));
#13464=CARTESIAN_POINT('Ctrl Pts',(85.8075956197331,3.01728274818844,-3.24677493312333));
#13465=CARTESIAN_POINT('Ctrl Pts',(85.8073224817074,3.01245356781049,-3.25128459396744));
#13466=CARTESIAN_POINT('Ctrl Pts',(85.8070500894955,3.00761379846055,-3.25578268002325));
#13467=CARTESIAN_POINT('Ctrl Pts',(85.8067784572813,3.00276347265943,-3.26026910647789));
#13468=CARTESIAN_POINT('Ctrl Pts',(85.8015491507576,2.90938780132206,-3.3466391977428));
#13469=CARTESIAN_POINT('Ctrl Pts',(85.7963795085898,2.81236114119968,-3.42896901143191));
#13470=CARTESIAN_POINT('Ctrl Pts',(85.7912051755409,2.71205630374664,-3.50692226952133));
#13471=CARTESIAN_POINT('Ctrl Pts',(85.7860277079776,2.61169070349584,-3.58492275023904));
#13472=CARTESIAN_POINT('Ctrl Pts',(85.7808451810478,2.50804277796375,-3.6585410124661));
#13473=CARTESIAN_POINT('Ctrl Pts',(85.7755770788642,2.40152103005734,-3.72746856029959));
#13474=CARTESIAN_POINT('Ctrl Pts',(85.7707101643231,2.30311135124782,-3.79114699195077));
#13475=CARTESIAN_POINT('Ctrl Pts',(85.7657697660599,2.20224841543128,-3.85082215564701));
#13476=CARTESIAN_POINT('Ctrl Pts',(85.7606849765742,2.099284847855,-3.90627647648126));
#13477=CARTESIAN_POINT('Ctrl Pts',(85.7602579461313,2.0906377685623,-3.91093363746222));
#13478=CARTESIAN_POINT('Ctrl Pts',(85.7598298973021,2.08197585954655,-3.91556105601013));
#13479=CARTESIAN_POINT('Ctrl Pts',(85.7594007880867,2.07329932164923,-3.92015861798155));
#13480=CARTESIAN_POINT('Ctrl Pts',(85.7569755051691,2.02426038612856,-3.94614358430527));
#13481=CARTESIAN_POINT('Ctrl Pts',(85.7545162749515,1.97475517878424,-3.97117430399793));
#13482=CARTESIAN_POINT('Ctrl Pts',(85.7520153891379,1.92482363811476,-3.99523029555697));
#13483=CARTESIAN_POINT('Ctrl Pts',(85.7520133539521,1.9247830045265,-3.99524987198587));
#13484=CARTESIAN_POINT('Ctrl Pts',(85.7520113187387,1.92474237065582,-3.99526944776944));
#13485=CARTESIAN_POINT('Ctrl Pts',(85.7520092834976,1.92470173650278,-3.99528902290766));
#13486=CARTESIAN_POINT('Ctrl Pts',(85.7468240038619,1.82117618607677,-4.04516152687214));
#13487=CARTESIAN_POINT('Ctrl Pts',(85.7414493102135,1.71552925404483,-4.09097385477383));
#13488=CARTESIAN_POINT('Ctrl Pts',(85.7359620804535,1.60812278109484,-4.13258257419633));
#13489=CARTESIAN_POINT('Ctrl Pts',(85.7354052266776,1.59722298235525,-4.13680510059591));
#13490=CARTESIAN_POINT('Ctrl Pts',(85.734847213943,1.58630510588221,-4.14098434647469));
#13491=CARTESIAN_POINT('Ctrl Pts',(85.7342881225959,1.57536955875698,-4.14512016962523));
#13492=CARTESIAN_POINT('Ctrl Pts',(85.7282271548735,1.45682006142753,-4.18995558114381));
#13493=CARTESIAN_POINT('Ctrl Pts',(85.7220399624372,1.3361879854999,-4.22968682176168));
#13494=CARTESIAN_POINT('Ctrl Pts',(85.7158181206739,1.21396163801592,-4.26417288909974));
#13495=CARTESIAN_POINT('Ctrl Pts',(85.7096023209395,1.09185398450512,-4.29862546702709));
#13496=CARTESIAN_POINT('Ctrl Pts',(85.7033522900078,0.968155225385933,-4.32784342167491));
#13497=CARTESIAN_POINT('Ctrl Pts',(85.6971419571728,0.843353220264177,-4.35172864669007));
#13498=CARTESIAN_POINT('Ctrl Pts',(85.6924237080598,0.748535926953768,-4.36987524925338));
#13499=CARTESIAN_POINT('Ctrl Pts',(85.687728492581,0.653078893740779,-4.38494421345017));
#13500=CARTESIAN_POINT('Ctrl Pts',(85.6831732408483,0.557184877352213,-4.39674690018236));
#13501=CARTESIAN_POINT('Ctrl Pts',(85.6817370345738,0.526950853830489,-4.4004681199385));
#13502=CARTESIAN_POINT('Ctrl Pts',(85.6803147414161,0.496673778449594,-4.40386461098195));
#13503=CARTESIAN_POINT('Ctrl Pts',(85.6789100260858,0.466361078450329,-4.40693038309136));
#13504=CARTESIAN_POINT('Ctrl Pts',(85.6739975838905,0.360354271715672,-4.41765172139186));
#13505=CARTESIAN_POINT('Ctrl Pts',(85.6692088184592,0.253932537364538,-4.42448546452957));
#13506=CARTESIAN_POINT('Ctrl Pts',(85.6644408649485,0.147396494829036,-4.42762657668275));
#13507=CARTESIAN_POINT('Ctrl Pts',(85.6635232234467,0.126892541960029,-4.42823111589795));
#13508=CARTESIAN_POINT('Ctrl Pts',(85.6626063528382,0.106384199984283,-4.42869887504062));
#13509=CARTESIAN_POINT('Ctrl Pts',(85.6616895198087,0.0858733907272211,
-4.42903123529975));
#13510=CARTESIAN_POINT('Ctrl Pts',(85.6541409846172,-0.0829976692238332,
-4.43176764752723));
#13511=CARTESIAN_POINT('Ctrl Pts',(85.6465949149874,-0.252038268960491,
-4.42533012680183));
#13512=CARTESIAN_POINT('Ctrl Pts',(85.6390459611412,-0.420233541092514,
-4.40976093706903));
#13513=CARTESIAN_POINT('Ctrl Pts',(85.6352346217969,-0.505152494272502,
-4.40190031603486));
#13514=CARTESIAN_POINT('Ctrl Pts',(85.6314225631056,-0.589855599106871,
-4.39171115039403));
#13515=CARTESIAN_POINT('Ctrl Pts',(85.6276091687937,-0.674209897682507,
-4.37919426061962));
#13516=CARTESIAN_POINT('Ctrl Pts',(85.6222195647431,-0.793430789127758,
-4.36150370089445));
#13517=CARTESIAN_POINT('Ctrl Pts',(85.6169919195691,-0.911916514284298,
-4.33888000264703));
#13518=CARTESIAN_POINT('Ctrl Pts',(85.6120121749869,-1.02915589167847,-4.31119254294835));
#13519=CARTESIAN_POINT('Ctrl Pts',(85.611739229202,-1.03558192284624,-4.30967496000878));
#13520=CARTESIAN_POINT('Ctrl Pts',(85.6114670281768,-1.04200419735488,-4.30814216848057));
#13521=CARTESIAN_POINT('Ctrl Pts',(85.6111955860632,-1.04842262677744,-4.30659414845052));
#13522=CARTESIAN_POINT('Ctrl Pts',(85.6059662788624,-1.17207307566988,-4.27677168581844));
#13523=CARTESIAN_POINT('Ctrl Pts',(85.6007966358639,-1.29438536193029,-4.2416706913012));
#13524=CARTESIAN_POINT('Ctrl Pts',(85.5956223017994,-1.4148729253243,-4.20141498159159));
#13525=CARTESIAN_POINT('Ctrl Pts',(85.5904448332242,-1.53543347773565,-4.16113488575772));
#13526=CARTESIAN_POINT('Ctrl Pts',(85.5852623050967,-1.65416689427829,-4.11569348298227));
#13527=CARTESIAN_POINT('Ctrl Pts',(85.57999420151,-1.77058994689207,-4.06525969676661));
#13528=CARTESIAN_POINT('Ctrl Pts',(85.575127286506,-1.87814688692753,-4.01866665872152));
#13529=CARTESIAN_POINT('Ctrl Pts',(85.5701868876291,-1.98373239500671,-3.96781239106193));
#13530=CARTESIAN_POINT('Ctrl Pts',(85.5651020974149,-2.08696989070404,-3.91286972470537));
#13531=CARTESIAN_POINT('Ctrl Pts',(85.5646750659807,-2.09563999389301,-3.90825552340602));
#13532=CARTESIAN_POINT('Ctrl Pts',(85.564247016155,-2.10429356683553,-3.90361248994626));
#13533=CARTESIAN_POINT('Ctrl Pts',(85.5638179059376,-2.11293040318291,-3.89894072818614));
#13534=CARTESIAN_POINT('Ctrl Pts',(85.5613926308205,-2.16174467847522,-3.87253653856314));
#13535=CARTESIAN_POINT('Ctrl Pts',(85.5589334086046,-2.21002333018883,-3.84521524038816));
#13536=CARTESIAN_POINT('Ctrl Pts',(85.5564325310774,-2.2577271700392,-3.81699871544304));
#13537=CARTESIAN_POINT('Ctrl Pts',(85.556430495889,-2.25776599093189,-3.81697575312616));
#13538=CARTESIAN_POINT('Ctrl Pts',(85.5564284606731,-2.25780481144409,-3.81695279021645));
#13539=CARTESIAN_POINT('Ctrl Pts',(85.5564264254296,-2.25784363157577,-3.81692982671393));
#13540=CARTESIAN_POINT('Ctrl Pts',(85.551241145975,-2.35674738960827,-3.75842470068692));
#13541=CARTESIAN_POINT('Ctrl Pts',(85.5458664525601,-2.45344835146911,-3.69590298795353));
#13542=CARTESIAN_POINT('Ctrl Pts',(85.5403792231113,-2.54762653041449,-3.62958629625731));
#13543=CARTESIAN_POINT('Ctrl Pts',(85.5398223700601,-2.55718388659679,-3.62285636953257));
#13544=CARTESIAN_POINT('Ctrl Pts',(85.539264358054,-2.56671524678532,-3.61608740174902));
#13545=CARTESIAN_POINT('Ctrl Pts',(85.5387052674388,-2.57622026693092,-3.60927965284289));
#13546=CARTESIAN_POINT('Ctrl Pts',(85.5326443008004,-2.67926189996543,-3.53547848737126));
#13547=CARTESIAN_POINT('Ctrl Pts',(85.5264571095619,-2.77921038643425,-3.45711419679469));
#13548=CARTESIAN_POINT('Ctrl Pts',(85.5202352690982,-2.87567764407725,-3.37451498435399));
#13549=CARTESIAN_POINT('Ctrl Pts',(85.5140194706598,-2.97205122242823,-3.2919959839555));
#13550=CARTESIAN_POINT('Ctrl Pts',(85.5077694411254,-3.06495059658092,-3.20525054580355));
#13551=CARTESIAN_POINT('Ctrl Pts',(85.501559109773,-3.1540236314308,-3.11463028404254));
#13552=CARTESIAN_POINT('Ctrl Pts',(85.4968408579376,-3.22169618967374,-3.04578223196543));
#13553=CARTESIAN_POINT('Ctrl Pts',(85.4921456398231,-3.28716215867454,-2.97469540514654));
#13554=CARTESIAN_POINT('Ctrl Pts',(85.4875903854759,-3.35015213193905,-2.90143395399441));
#13555=CARTESIAN_POINT('Ctrl Pts',(85.4861541832599,-3.37001190974662,-2.87833573587593));
#13556=CARTESIAN_POINT('Ctrl Pts',(85.4847318940682,-3.38962531165613,-2.85502164769157));
#13557=CARTESIAN_POINT('Ctrl Pts',(85.483327182572,-3.40898323459362,-2.83149454933526));
#13558=CARTESIAN_POINT('Ctrl Pts',(85.4784147446847,-3.47668012062022,-2.74921757669169));
#13559=CARTESIAN_POINT('Ctrl Pts',(85.4736259837766,-3.54137171508201,-2.66443985809102));
#13560=CARTESIAN_POINT('Ctrl Pts',(85.468858034897,-3.60305359689301,-2.57751967162226));
#13561=CARTESIAN_POINT('Ctrl Pts',(85.4679403901104,-3.61492496101744,-2.56079091508893));
#13562=CARTESIAN_POINT('Ctrl Pts',(85.4670235162279,-3.62668492620405,-2.54398266893432));
#13563=CARTESIAN_POINT('Ctrl Pts',(85.4661066799248,-3.63833357637928,-2.52709729836248));
#13564=CARTESIAN_POINT('Ctrl Pts',(85.4585581460186,-3.73423971633857,-2.3880759792425));
#13565=CARTESIAN_POINT('Ctrl Pts',(85.4510120776706,-3.82260509299389,-2.24382717287147));
#13566=CARTESIAN_POINT('Ctrl Pts',(85.4434631251022,-3.9029021966404,-2.09521890865093));
#13567=CARTESIAN_POINT('Ctrl Pts',(85.4396517872357,-3.94344283971919,-2.02018912146399));
#13568=CARTESIAN_POINT('Ctrl Pts',(85.4358397300216,-3.98192593919025,-1.94404793137696));
#13569=CARTESIAN_POINT('Ctrl Pts',(85.4320263371865,-4.01827846077401,-1.86690644393239));
#13570=CARTESIAN_POINT('Ctrl Pts',(85.4266365949618,-4.06965809277716,-1.75787683430971));
#13571=CARTESIAN_POINT('Ctrl Pts',(85.4214088253351,-4.11652440392096,-1.64672380638182));
#13572=CARTESIAN_POINT('Ctrl Pts',(85.4164289670649,-4.15848525213285,-1.5338003894688));
#13573=CARTESIAN_POINT('Ctrl Pts',(85.4161561509682,-4.16078403137511,-1.52761400340116));
#13574=CARTESIAN_POINT('Ctrl Pts',(85.4158840789221,-4.16306808473654,-1.52142231651565));
#13575=CARTESIAN_POINT('Ctrl Pts',(85.4156127650568,-4.16533734671304,-1.51522539127473));
#13576=CARTESIAN_POINT('Ctrl Pts',(85.4103834597761,-4.20907511743536,-1.39578581216136));
#13577=CARTESIAN_POINT('Ctrl Pts',(85.4052138187203,-4.24767803984522,-1.27453325637026));
#13578=CARTESIAN_POINT('Ctrl Pts',(85.4000394866055,-4.28097938890212,-1.1519412996419));
#13579=CARTESIAN_POINT('Ctrl Pts',(85.3948620199694,-4.31430091134194,-1.02927507882045));
#13580=CARTESIAN_POINT('Ctrl Pts',(85.3896794937884,-4.34231403673318,-0.905267810486362));
#13581=CARTESIAN_POINT('Ctrl Pts',(85.3844113921312,-4.36489142648191,-0.780415306259535));
#13582=CARTESIAN_POINT('Ctrl Pts',(85.3795444786099,-4.38574945288143,-0.665070846240425));
#13583=CARTESIAN_POINT('Ctrl Pts',(85.3746040811925,-4.40196814370703,-0.549004463717536));
#13584=CARTESIAN_POINT('Ctrl Pts',(85.3695192923719,-4.41348254186089,-0.432625382137005));
#13585=CARTESIAN_POINT('Ctrl Pts',(85.3690922613637,-4.414449544666,-0.422851627847718));
#13586=CARTESIAN_POINT('Ctrl Pts',(85.368664211965,-4.41538338769334,-0.413075644729704));
#13587=CARTESIAN_POINT('Ctrl Pts',(85.3682351021756,-4.41628404296986,-0.403297662094833));
#13588=CARTESIAN_POINT('Ctrl Pts',(85.3658098126881,-4.42137446464771,-0.34803339388098));
#13589=CARTESIAN_POINT('Ctrl Pts',(85.363350575666,-4.42540466293366,-0.292706402114392));
#13590=CARTESIAN_POINT('Ctrl Pts',(85.3608496827478,-4.42837112077165,-0.237361433173412));
#13591=CARTESIAN_POINT('Ctrl Pts',(85.36084764755,-4.42837353484072,-0.237316394077848));
#13592=CARTESIAN_POINT('Ctrl Pts',(85.3608456123247,-4.42837594820546,-0.237271354970261));
#13593=CARTESIAN_POINT('Ctrl Pts',(85.3608435770718,-4.42837836086587,-0.237226315850657));
#13594=CARTESIAN_POINT('Ctrl Pts',(85.3572923046138,-4.43258816420395,-0.158638448753409));
#13595=CARTESIAN_POINT('Ctrl Pts',(85.3536546163276,-4.4346561875942,-0.0799395109034866));
#13596=CARTESIAN_POINT('Ctrl Pts',(85.3499542888701,-4.43459181384913,-0.00121389497252961));
#13597=CARTESIAN_POINT('',(84.0953986853364,-4.42975181744819,-0.00129412797191142));
#13598=CARTESIAN_POINT('Ctrl Pts',(85.3499542888372,-4.43459181384856,-0.00121389427323007));
#13599=CARTESIAN_POINT('Ctrl Pts',(85.3443627450434,-4.43449453902907,0.117747936589198));
#13600=CARTESIAN_POINT('Ctrl Pts',(85.3386250062462,-4.42952256215798,0.236873214595778));
#13601=CARTESIAN_POINT('Ctrl Pts',(85.3328212751709,-4.41970267314065,0.355734616697525));
#13602=CARTESIAN_POINT('Ctrl Pts',(85.3324982112812,-4.41915605037309,0.362351020249405));
#13603=CARTESIAN_POINT('Ctrl Pts',(85.3321749429093,-4.41859441338435,0.368966594981758));
#13604=CARTESIAN_POINT('Ctrl Pts',(85.3318514838888,-4.41801776948587,0.375581263292163));
#13605=CARTESIAN_POINT('Ctrl Pts',(85.325724481569,-4.40709490668166,0.500877160188369));
#13606=CARTESIAN_POINT('Ctrl Pts',(85.3195294832927,-4.39078493141124,0.625852307579887));
#13607=CARTESIAN_POINT('Ctrl Pts',(85.3133461040938,-4.36916256993669,0.750018636766457));
#13608=CARTESIAN_POINT('Ctrl Pts',(85.307168464745,-4.34756027986803,0.874069705980425));
#13609=CARTESIAN_POINT('Ctrl Pts',(85.3010026794321,-4.32065571810597,0.997313514097945));
#13610=CARTESIAN_POINT('Ctrl Pts',(85.2949088018228,-4.28856072520909,1.11927693375167));
#13611=CARTESIAN_POINT('Ctrl Pts',(85.2908108730481,-4.26697791647055,1.2012932522454));
#13612=CARTESIAN_POINT('Ctrl Pts',(85.2869118605903,-4.24277054945837,1.28265283961973));
#13613=CARTESIAN_POINT('Ctrl Pts',(85.2830812618982,-4.21622777153665,1.36325866850456));
#13614=CARTESIAN_POINT('Ctrl Pts',(85.2812191292538,-4.20332478241829,1.40244281629966));
#13615=CARTESIAN_POINT('Ctrl Pts',(85.2793731636828,-4.18986972440365,1.44144960587744));
#13616=CARTESIAN_POINT('Ctrl Pts',(85.2775283734857,-4.17589453858595,1.48027215448857));
#13617=CARTESIAN_POINT('Ctrl Pts',(85.2697398901285,-4.11689297714989,1.64417630695318));
#13618=CARTESIAN_POINT('Ctrl Pts',(85.2619544711741,-4.04865181528642,1.80481341257982));
#13619=CARTESIAN_POINT('Ctrl Pts',(85.2541669226034,-3.97165771867034,1.96116259370312));
#13620=CARTESIAN_POINT('Ctrl Pts',(85.2506806541404,-3.9371896073732,2.0311557647776));
#13621=CARTESIAN_POINT('Ctrl Pts',(85.2471939527207,-3.90096660633359,2.10028946703939));
#13622=CARTESIAN_POINT('Ctrl Pts',(85.2437063512401,-3.86302935653635,2.16847054002379));
#13623=CARTESIAN_POINT('Ctrl Pts',(85.2393355443983,-3.81548482144543,2.25391788885295));
#13624=CARTESIAN_POINT('Ctrl Pts',(85.2349632968975,-3.7652452621893,2.33787320140798));
#13625=CARTESIAN_POINT('Ctrl Pts',(85.2307004097096,-3.71223605028654,2.42002879416054));
#13626=CARTESIAN_POINT('Ctrl Pts',(85.2294629596189,-3.69684829753027,2.44387728960959));
#13627=CARTESIAN_POINT('Ctrl Pts',(85.2282347247852,-3.6812273272569,2.46757384101803));
#13628=CARTESIAN_POINT('Ctrl Pts',(85.2270184154944,-3.6653717509357,2.49111022443572));
#13629=CARTESIAN_POINT('Ctrl Pts',(85.2226810167006,-3.60883024612882,2.57504173907688));
#13630=CARTESIAN_POINT('Ctrl Pts',(85.2185002056003,-3.54930026576319,2.65692809285175));
#13631=CARTESIAN_POINT('Ctrl Pts',(85.2143637396925,-3.48705788915787,2.73662776750612));
#13632=CARTESIAN_POINT('Ctrl Pts',(85.2133392630817,-3.47164234834229,2.75636694930846));
#13633=CARTESIAN_POINT('Ctrl Pts',(85.2123175066139,-3.45606029811023,2.7759722134224));
#13634=CARTESIAN_POINT('Ctrl Pts',(85.2112967650899,-3.44031566070746,2.79544182210765));
#13635=CARTESIAN_POINT('Ctrl Pts',(85.2061521108481,-3.36096088410859,2.8935708807936));
#13636=CARTESIAN_POINT('Ctrl Pts',(85.2010329451672,-3.27747677113758,2.98825187445984));
#13637=CARTESIAN_POINT('Ctrl Pts',(85.1958670671956,-3.19018387642686,3.07910075506622));
#13638=CARTESIAN_POINT('Ctrl Pts',(85.1906931541495,-3.10275520520107,3.17009094321484));
#13639=CARTESIAN_POINT('Ctrl Pts',(85.1854719470249,-3.01150566656215,3.25723667246366));
#13640=CARTESIAN_POINT('Ctrl Pts',(85.1801186357432,-2.91679888704007,3.34017703779908));
#13641=CARTESIAN_POINT('Ctrl Pts',(85.1752973944057,-2.83150509104349,3.41487389304535));
#13642=CARTESIAN_POINT('Ctrl Pts',(85.1703685282327,-2.74340758943231,3.48615979009815));
#13643=CARTESIAN_POINT('Ctrl Pts',(85.1652667799706,-2.65280287863538,3.55379345323013));
#13644=CARTESIAN_POINT('Ctrl Pts',(85.1652647448044,-2.6527667350155,3.55382043334396));
#13645=CARTESIAN_POINT('Ctrl Pts',(85.1652627096106,-2.65273059099647,3.5538474128773));
#13646=CARTESIAN_POINT('Ctrl Pts',(85.1652606743893,-2.65269444657834,3.55387439183014));
#13647=CARTESIAN_POINT('Ctrl Pts',(85.1600753925247,-2.56060667334183,3.62261063990077));
#13648=CARTESIAN_POINT('Ctrl Pts',(85.1547006967979,-2.46566074711065,3.6877668987319));
#13649=CARTESIAN_POINT('Ctrl Pts',(85.149213465117,-2.36818443293561,3.74913323468465));
#13650=CARTESIAN_POINT('Ctrl Pts',(85.1486566118364,-2.35829237652487,3.75536079121572));
#13651=CARTESIAN_POINT('Ctrl Pts',(85.1480985996017,-2.34837430506267,3.76154931927579));
#13652=CARTESIAN_POINT('Ctrl Pts',(85.1475395087587,-2.33843059095367,3.76769860148941));
#13653=CARTESIAN_POINT('Ctrl Pts',(85.141478539663,-2.23063318259331,3.83436148807664));
#13654=CARTESIAN_POINT('Ctrl Pts',(85.1352913460616,-2.11981621289668,3.8964122132986));
#13655=CARTESIAN_POINT('Ctrl Pts',(85.1290695032808,-2.00643204719541,3.9536190623625));
#13656=CARTESIAN_POINT('Ctrl Pts',(85.12285370252,-1.89315798864708,4.01077035796142));
#13657=CARTESIAN_POINT('Ctrl Pts',(85.116603670709,-1.77732185769731,4.06308752801176));
#13658=CARTESIAN_POINT('Ctrl Pts',(85.1103933370457,-1.65938377745455,4.11038104877906));
#13659=CARTESIAN_POINT('Ctrl Pts',(85.1056750483368,-1.56978055441894,4.14631220757636));
#13660=CARTESIAN_POINT('Ctrl Pts',(85.1009797936717,-1.47896125316684,4.17934463667908));
#13661=CARTESIAN_POINT('Ctrl Pts',(85.0964245021716,-1.38708885330889,4.20925442909443));
#13662=CARTESIAN_POINT('Ctrl Pts',(85.0949883328377,-1.35812378635327,4.21868423762538));
#13663=CARTESIAN_POINT('Ctrl Pts',(85.0935660756043,-1.3290544141682,4.22780354442039));
#13664=CARTESIAN_POINT('Ctrl Pts',(85.0921613947722,-1.29988688200897,4.23660505115098));
#13665=CARTESIAN_POINT('Ctrl Pts',(85.0872489806352,-1.19788292919405,4.2673854569922));
#13666=CARTESIAN_POINT('Ctrl Pts',(85.0824602450516,-1.09472882755048,4.29442923830735));
#13667=CARTESIAN_POINT('Ctrl Pts',(85.077692322407,-0.990756907868159,4.31787032279431));
#13668=CARTESIAN_POINT('Ctrl Pts',(85.0767746450963,-0.970745536303325,
4.32238200491949));
#13669=CARTESIAN_POINT('Ctrl Pts',(85.0758577387868,-0.950703716756279,
4.32676025572996));
#13670=CARTESIAN_POINT('Ctrl Pts',(85.0749408700586,-0.930633599828038,
4.33100606386856));
#13671=CARTESIAN_POINT('Ctrl Pts',(85.0673923349243,-0.765397314496613,
4.36596159340343));
#13672=CARTESIAN_POINT('Ctrl Pts',(85.0598462653068,-0.598241567400583,
4.39194463939876));
#13673=CARTESIAN_POINT('Ctrl Pts',(85.0522973114357,-0.4301706000107,4.40880275502221));
#13674=CARTESIAN_POINT('Ctrl Pts',(85.04848596313,-0.345314206962011,4.41731415296094));
#13675=CARTESIAN_POINT('Ctrl Pts',(85.044673895465,-0.260224722043043,4.42349865776892));
#13676=CARTESIAN_POINT('Ctrl Pts',(85.0408604921652,-0.175032810746617,
4.42733166758056));
#13677=CARTESIAN_POINT('Ctrl Pts',(85.0354698342498,-0.0546048321555523,
4.43275004142041));
#13678=CARTESIAN_POINT('Ctrl Pts',(85.0302412367628,0.0660442875316501,
4.43318368293072));
#13679=CARTESIAN_POINT('Ctrl Pts',(85.0252606189512,0.18643746193737,4.42840668878626));
#13680=CARTESIAN_POINT('Ctrl Pts',(85.0249886482198,0.19301163022839,4.42814583709275));
#13681=CARTESIAN_POINT('Ctrl Pts',(85.0247174169133,0.199585022546118,4.42786945021315));
#13682=CARTESIAN_POINT('Ctrl Pts',(85.0244469390212,0.206157556782235,4.42757749211126));
#13683=CARTESIAN_POINT('Ctrl Pts',(85.0192176276754,0.33322830397975,4.42193289098418));
#13684=CARTESIAN_POINT('Ctrl Pts',(85.0140479797323,0.459994220768434,4.41085131019553));
#13685=CARTESIAN_POINT('Ctrl Pts',(85.0088736397687,0.585954052039474,4.39436130789153));
#13686=CARTESIAN_POINT('Ctrl Pts',(85.0036961653171,0.711990186679063,4.3778613163496));
#13687=CARTESIAN_POINT('Ctrl Pts',(84.9985136303553,0.837219126886628,4.35594597195404));
#13688=CARTESIAN_POINT('Ctrl Pts',(84.9932455188829,0.961134268792317,4.32868874528195));
#13689=CARTESIAN_POINT('Ctrl Pts',(84.9883786009584,1.0756126408649,4.30350729539096));
#13690=CARTESIAN_POINT('Ctrl Pts',(84.9834381983927,1.18897018723484,4.27376641965414));
#13691=CARTESIAN_POINT('Ctrl Pts',(84.9783534039193,1.30080424095069,4.23956380318721));
#13692=CARTESIAN_POINT('Ctrl Pts',(84.9779263672656,1.31019640818819,4.23669136243107));
#13693=CARTESIAN_POINT('Ctrl Pts',(84.9774983121933,1.31957785908119,4.23378746134294));
#13694=CARTESIAN_POINT('Ctrl Pts',(84.9770691967007,1.32894837122947,4.23085216243986));
#13695=CARTESIAN_POINT('Ctrl Pts',(84.9746439662741,1.38190765973384,4.21426274459428));
#13696=CARTESIAN_POINT('Ctrl Pts',(84.9721847899234,1.43451645852858,4.19667080485617));
#13697=CARTESIAN_POINT('Ctrl Pts',(84.9696839599123,1.48673212258517,4.17809033243677));
#13698=CARTESIAN_POINT('Ctrl Pts',(84.9696819247138,1.48677461617353,4.17807521147717));
#13699=CARTESIAN_POINT('Ctrl Pts',(84.9696798894877,1.48681710950168,4.17806008986295));
#13700=CARTESIAN_POINT('Ctrl Pts',(84.9696778542341,1.48685960256962,4.17804496759413));
#13701=CARTESIAN_POINT('Ctrl Pts',(84.9644925752988,1.59512051017262,4.13951749412701));
#13702=CARTESIAN_POINT('Ctrl Pts',(84.9591178827597,1.70198674692963,4.0966265206881));
#13703=CARTESIAN_POINT('Ctrl Pts',(84.9536306546941,1.80710187557081,4.04952842474458));
#13704=CARTESIAN_POINT('Ctrl Pts',(84.9530738061195,1.81776904829537,4.0447488698801));
#13705=CARTESIAN_POINT('Ctrl Pts',(84.9525157986131,1.82841816474237,4.03992602651722));
#13706=CARTESIAN_POINT('Ctrl Pts',(84.9519567125193,1.83904883754031,4.03506008405304));
#13707=CARTESIAN_POINT('Ctrl Pts',(84.9458957520418,1.9542942145772,3.98230920133997));
#13708=CARTESIAN_POINT('Ctrl Pts',(84.9397085677023,2.06737541948516,3.92448822190028));
#13709=CARTESIAN_POINT('Ctrl Pts',(84.9334867347874,2.17784880585476,3.86184514143038));
#13710=CARTESIAN_POINT('Ctrl Pts',(84.9272709438731,2.28821491189869,3.79926289344054));
#13711=CARTESIAN_POINT('Ctrl Pts',(84.9210209225093,2.39597847332284,3.73186821447881));
#13712=CARTESIAN_POINT('Ctrl Pts',(84.9148105998528,2.50072665476181,3.65993894890574));
#13713=CARTESIAN_POINT('Ctrl Pts',(84.9100923213472,2.58030884723625,3.60529085307492));
#13714=CARTESIAN_POINT('Ctrl Pts',(84.9053970771899,2.65815290072415,3.54802354859147));
#13715=CARTESIAN_POINT('Ctrl Pts',(84.9008417967757,2.73398211261954,3.48814852671847));
#13716=CARTESIAN_POINT('Ctrl Pts',(84.8994056285702,2.75788920357092,3.46927140063666));
#13717=CARTESIAN_POINT('Ctrl Pts',(84.8979833725685,2.7815957190102,3.45013531491955));
#13718=CARTESIAN_POINT('Ctrl Pts',(84.896578693098,2.80509217788893,3.43074133727564));
#13719=CARTESIAN_POINT('Ctrl Pts',(84.891666288651,2.88726331480333,3.36291727916896));
#13720=CARTESIAN_POINT('Ctrl Pts',(84.8868775629567,2.96696244339537,3.2920643159296));
#13721=CARTESIAN_POINT('Ctrl Pts',(84.8821096502108,3.04411676486044,3.21853327559953));
#13722=CARTESIAN_POINT('Ctrl Pts',(84.8811919761277,3.05896655867597,3.2043808500813));
#13723=CARTESIAN_POINT('Ctrl Pts',(84.8802750730439,3.07372219006676,3.19012910601789));
#13724=CARTESIAN_POINT('Ctrl Pts',(84.8793582075413,3.08838328943348,3.17578038132092));
#13725=CARTESIAN_POINT('Ctrl Pts',(84.8718096813903,3.20908768027593,3.05764776175447));
#13726=CARTESIAN_POINT('Ctrl Pts',(84.8642636207654,3.32338920208233,2.93294302913735));
#13727=CARTESIAN_POINT('Ctrl Pts',(84.8567146758861,3.43060419465878,2.8024174136542));
#13728=CARTESIAN_POINT('Ctrl Pts',(84.8529033446259,3.48473518373024,2.73651729562523));
#13729=CARTESIAN_POINT('Ctrl Pts',(84.8490912940106,3.53705892944319,2.66913308306512));
#13730=CARTESIAN_POINT('Ctrl Pts',(84.8452779077678,3.5874825124696,2.60035987757172));
#13731=CARTESIAN_POINT('Ctrl Pts',(84.8398870676215,3.65876442791117,2.5031377936897));
#13732=CARTESIAN_POINT('Ctrl Pts',(84.834658308312,3.72602025675175,2.40296772540271));
#13733=CARTESIAN_POINT('Ctrl Pts',(84.8296775451296,3.78879745195251,2.30012150739739));
#13734=CARTESIAN_POINT('Ctrl Pts',(84.8294057559354,3.79222306418852,2.29450941750232));
#13735=CARTESIAN_POINT('Ctrl Pts',(84.829134705185,3.79563533511922,2.28888937065754));
#13736=CARTESIAN_POINT('Ctrl Pts',(84.8288644068382,3.79903418938342,2.28326141512133));
#13737=CARTESIAN_POINT('Ctrl Pts',(84.8236351120371,3.86478971895968,2.17438084303772));
#13738=CARTESIAN_POINT('Ctrl Pts',(84.8184654813944,3.92585147626731,2.06273948891568));
#13739=CARTESIAN_POINT('Ctrl Pts',(84.8132911594918,3.981965313625,1.94877034131851));
#13740=CARTESIAN_POINT('Ctrl Pts',(84.8081137030104,4.03811314446976,1.83473215177149));
#13741=CARTESIAN_POINT('Ctrl Pts',(84.8029311867842,4.08930667195149,1.71836324852354));
#13742=CARTESIAN_POINT('Ctrl Pts',(84.7976630947116,4.13532615997803,1.60012597256214));
#13743=CARTESIAN_POINT('Ctrl Pts',(84.7927961893516,4.17784107616579,1.49089294774299));
#13744=CARTESIAN_POINT('Ctrl Pts',(84.78785579976,4.21594011018023,1.38006477453644));
#13745=CARTESIAN_POINT('Ctrl Pts',(84.7827710182219,4.24948130381418,1.2680307221417));
#13746=CARTESIAN_POINT('Ctrl Pts',(84.7823439884463,4.25229815804497,1.25862188601248));
#13747=CARTESIAN_POINT('Ctrl Pts',(84.7819159402795,4.25508288962256,1.24920452565539));
#13748=CARTESIAN_POINT('Ctrl Pts',(84.7814868317212,4.25783542727072,1.23977886080998));
#13749=CARTESIAN_POINT('Ctrl Pts',(84.7790614671213,4.27339304606401,1.18650405796183));
#13750=CARTESIAN_POINT('Ctrl Pts',(84.7766021526623,4.28792190026075,1.1329650723735));
#13751=CARTESIAN_POINT('Ctrl Pts',(84.7741011792086,4.3014099859364,1.07920515793332));
#13752=CARTESIAN_POINT('Ctrl Pts',(84.7740991439519,4.30142096234921,1.07916140887747));
#13753=CARTESIAN_POINT('Ctrl Pts',(84.7740971086676,4.30143193807291,1.07911765967523));
#13754=CARTESIAN_POINT('Ctrl Pts',(84.7740950733557,4.30144291310753,1.07907391032659));
#13755=CARTESIAN_POINT('Ctrl Pts',(84.768909803381,4.32940350105146,0.967615718873223));
#13756=CARTESIAN_POINT('Ctrl Pts',(84.763535117755,4.35295944008393,0.854898914033085));
#13757=CARTESIAN_POINT('Ctrl Pts',(84.7580478939663,4.37204324863032,0.741306830386417));
#13758=CARTESIAN_POINT('Ctrl Pts',(84.7574910265083,4.37397995694803,0.729779009160925));
#13759=CARTESIAN_POINT('Ctrl Pts',(84.7569330000111,4.37587062545103,0.718242213346182));
#13760=CARTESIAN_POINT('Ctrl Pts',(84.7563738948267,4.37771519698071,0.706696870372616));
#13761=CARTESIAN_POINT('Ctrl Pts',(84.7503129183795,4.39771126374356,0.581539648120451));
#13762=CARTESIAN_POINT('Ctrl Pts',(84.7441257143383,4.4122879629984,0.455372437180053));
#13763=CARTESIAN_POINT('Ctrl Pts',(84.7379038586095,4.42140570754389,0.328701950375454));
#13764=CARTESIAN_POINT('Ctrl Pts',(84.7316880450157,4.43051459771433,0.202154475132937));
#13765=CARTESIAN_POINT('Ctrl Pts',(84.7254379978752,4.43417550512059,0.075104696430171));
#13766=CARTESIAN_POINT('Ctrl Pts',(84.7192276472584,4.43239076643115,-0.0519497654959621));
#13767=CARTESIAN_POINT('Ctrl Pts',(84.7145096587603,4.43103490472084,-0.148472736096043));
#13768=CARTESIAN_POINT('Ctrl Pts',(84.7098147003148,4.4265359915693,-0.245001378756047));
#13769=CARTESIAN_POINT('Ctrl Pts',(84.7052597085182,4.41875015260918,-0.341299084631016));
#13770=CARTESIAN_POINT('Ctrl Pts',(84.7038232361851,4.41629479313635,-0.371667743107352));
#13771=CARTESIAN_POINT('Ctrl Pts',(84.7024006840014,4.41351257292165,-0.402013046553423));
#13772=CARTESIAN_POINT('Ctrl Pts',(84.700995719546,4.4103991195604,-0.432326506843429));
#13773=CARTESIAN_POINT('Ctrl Pts',(84.6960830564247,4.39951247581047,-0.538321941723752));
#13774=CARTESIAN_POINT('Ctrl Pts',(84.6912940568784,4.38473411194135,-0.643939410514095));
#13775=CARTESIAN_POINT('Ctrl Pts',(84.6865258619715,4.3663156351685,-0.748923772186185));
#13776=CARTESIAN_POINT('Ctrl Pts',(84.6856084689167,4.36277194976964,-0.769122595039711));
#13777=CARTESIAN_POINT('Ctrl Pts',(84.6846918459903,4.35909348503392,-0.789298133509308));
#13778=CARTESIAN_POINT('Ctrl Pts',(84.6837752606268,4.35528197981159,-0.80944878521036));
#13779=CARTESIAN_POINT('Ctrl Pts',(84.6762267057085,4.32389226136465,-0.975399832506024));
#13780=CARTESIAN_POINT('Ctrl Pts',(84.6686806166527,4.28348300576916,-1.13966608036638));
#13781=CARTESIAN_POINT('Ctrl Pts',(84.6611316436492,4.23430036531949,-1.30126205165788));
#13782=CARTESIAN_POINT('Ctrl Pts',(84.6573203316184,4.20946912149827,-1.38284833752986));
#13783=CARTESIAN_POINT('Ctrl Pts',(84.6535083003208,4.18240079675737,-1.46375343855993));
#13784=CARTESIAN_POINT('Ctrl Pts',(84.6496949334886,4.15312301906299,-1.54384729969441));
#13785=CARTESIAN_POINT('Ctrl Pts',(84.6443132190019,4.11180398334093,-1.65688187301069));
#13786=CARTESIAN_POINT('Ctrl Pts',(84.639092697203,4.06581574754515,-1.76820634527985));
#13787=CARTESIAN_POINT('Ctrl Pts',(84.6341194783051,4.01513272168606,-1.87729568176754));
#13788=CARTESIAN_POINT('Ctrl Pts',(84.6338392039288,4.0122763918614,-1.88344360052497));
#13789=CARTESIAN_POINT('Ctrl Pts',(84.6335597150067,4.00940515807036,-1.88958440849035));
#13790=CARTESIAN_POINT('Ctrl Pts',(84.6332810269519,4.00651901836426,-1.8957180075007));
#13791=CARTESIAN_POINT('Ctrl Pts',(84.6280517137449,3.95236338369587,-2.01080909145097));
#13792=CARTESIAN_POINT('Ctrl Pts',(84.6228820688287,3.89330774160362,-2.12352459141227));
#13793=CARTESIAN_POINT('Ctrl Pts',(84.6177077380327,3.8295715259579,-2.23341293355516));
#13794=CARTESIAN_POINT('Ctrl Pts',(84.6125302727593,3.76579670054097,-2.34336784324847));
#13795=CARTESIAN_POINT('Ctrl Pts',(84.6073477531349,3.6973353322639,-2.45049190190229));
#13796=CARTESIAN_POINT('Ctrl Pts',(84.6020796641393,3.62445036165115,-2.55434589972039));
#13797=CARTESIAN_POINT('Ctrl Pts',(84.5972127429459,3.55711562063874,-2.65029135990778));
#13798=CARTESIAN_POINT('Ctrl Pts',(84.5922723424912,3.48600498536139,-2.74344620822685));
#13799=CARTESIAN_POINT('Ctrl Pts',(84.5871875548635,3.41136371001468,-2.83347647361782));
#13800=CARTESIAN_POINT('Ctrl Pts',(84.5867605459365,3.40509550508114,-2.8410370110158));
#13801=CARTESIAN_POINT('Ctrl Pts',(84.5863325187537,3.39880239828021,-2.84857554335884));
#13802=CARTESIAN_POINT('Ctrl Pts',(84.5859034313212,3.39248453294577,-2.85609188952173));
#13803=CARTESIAN_POINT('Ctrl Pts',(84.5834781257411,3.35677443544996,-2.89857608949763));
#13804=CARTESIAN_POINT('Ctrl Pts',(84.5810188731415,3.32027412338363,-2.94035063029836));
#13805=CARTESIAN_POINT('Ctrl Pts',(84.5785179649191,3.28301293624369,-2.98138154243981));
#13806=CARTESIAN_POINT('Ctrl Pts',(84.5785159299288,3.28298261679641,-2.98141492931428));
#13807=CARTESIAN_POINT('Ctrl Pts',(84.5785138949109,3.28295229684535,-2.98144831569655));
#13808=CARTESIAN_POINT('Ctrl Pts',(84.5785118598654,3.28292197639053,-2.98148170158665));
#13809=CARTESIAN_POINT('Ctrl Pts',(84.5733265574052,3.20566535957455,-3.06654905737755));
#13810=CARTESIAN_POINT('Ctrl Pts',(84.5679518428513,3.12491911275222,-3.14864850413186));
#13811=CARTESIAN_POINT('Ctrl Pts',(84.5624645943197,3.04096485078219,-3.22751134131508));
#13812=CARTESIAN_POINT('Ctrl Pts',(84.5619077499984,3.03244519766962,-3.23551431818019));
#13813=CARTESIAN_POINT('Ctrl Pts',(84.5613497467876,3.02389255180424,-3.24348395767438));
#13814=CARTESIAN_POINT('Ctrl Pts',(84.560790665029,3.01530723717742,-3.25141997527823));
#13815=CARTESIAN_POINT('Ctrl Pts',(84.5547296888236,2.92223428878533,-3.33745392848651));
#13816=CARTESIAN_POINT('Ctrl Pts',(84.5485424907892,2.82531604959927,-3.41953766354237));
#13817=CARTESIAN_POINT('Ctrl Pts',(84.5423206455941,2.72495227604094,-3.49735729128607));
#13818=CARTESIAN_POINT('Ctrl Pts',(84.5361048423106,2.6246859637701,-3.5751013499191));
#13819=CARTESIAN_POINT('Ctrl Pts',(84.529854809988,2.52098100948511,-3.64858989306717));
#13820=CARTESIAN_POINT('Ctrl Pts',(84.5236444767993,2.41425284641874,-3.717548962688));
#13821=CARTESIAN_POINT('Ctrl Pts',(84.5189257891911,2.33315947425737,-3.7699449126978));
#13822=CARTESIAN_POINT('Ctrl Pts',(84.5142301400925,2.25031820586455,-3.81972745306807));
#13823=CARTESIAN_POINT('Ctrl Pts',(84.5096744486561,2.16584629455141,-3.86664565444101));
#13824=CARTESIAN_POINT('Ctrl Pts',(84.5082386601763,2.13922381609311,-3.88143256746258));
#13825=CARTESIAN_POINT('Ctrl Pts',(84.5068167734316,2.11243971047828,-3.8959347854256));
#13826=CARTESIAN_POINT('Ctrl Pts',(84.505412448532,2.08549861207607,-3.91014397891237));
#13827=CARTESIAN_POINT('Ctrl Pts',(84.500500330476,1.99126268708196,-3.95984560843227));
#13828=CARTESIAN_POINT('Ctrl Pts',(84.4957119095192,1.89518400202996,-4.0060996746415));
#13829=CARTESIAN_POINT('Ctrl Pts',(84.4909443119702,1.79761431116414,-4.04897415816643));
#13830=CARTESIAN_POINT('Ctrl Pts',(84.4900262694309,1.77882641519906,-4.05723001435369));
#13831=CARTESIAN_POINT('Ctrl Pts',(84.489108999,1.75998309001578,-4.06536061625154));
#13832=CARTESIAN_POINT('Ctrl Pts',(84.4881917661738,1.74108663839054,-4.07336652430806));
#13833=CARTESIAN_POINT('Ctrl Pts',(84.4806432389444,1.5855749999614,-4.13925253844839));
#13834=CARTESIAN_POINT('Ctrl Pts',(84.4730971767776,1.42646473439164,-4.19669820861065));
#13835=CARTESIAN_POINT('Ctrl Pts',(84.4655482299722,1.26471243690291,-4.24536198986576));
#13836=CARTESIAN_POINT('Ctrl Pts',(84.4617368033983,1.18304448759641,-4.26993209664203));
#13837=CARTESIAN_POINT('Ctrl Pts',(84.4579246573404,1.10070306845423,-4.29226263505166));
#13838=CARTESIAN_POINT('Ctrl Pts',(84.4541111755068,1.01781174310843,-4.31230448362946));
#13839=CARTESIAN_POINT('Ctrl Pts',(84.4484261205266,0.894239175431847,-4.3421824314052));
#13840=CARTESIAN_POINT('Ctrl Pts',(84.4429217562405,0.76936510175984,-4.36666473639337));
#13841=CARTESIAN_POINT('Ctrl Pts',(84.4376979694913,0.643690135002427,-4.38538581583833));
#13842=CARTESIAN_POINT('Ctrl Pts',(84.4324686290142,0.517881555483126,-4.40412679881058));
#13843=CARTESIAN_POINT('Ctrl Pts',(84.4272989443257,0.391333239082584,-4.41747267370568));
#13844=CARTESIAN_POINT('Ctrl Pts',(84.4221245584116,0.264542667669082,-4.42535568566965));
#13845=CARTESIAN_POINT('Ctrl Pts',(84.4169470381692,0.13767529424048,-4.43324347268272));
#13846=CARTESIAN_POINT('Ctrl Pts',(84.4117644481786,0.0105654297978427,
-4.43566138153736));
#13847=CARTESIAN_POINT('Ctrl Pts',(84.4064962713937,-0.116275610554298,
-4.4325847207063));
#13848=CARTESIAN_POINT('Ctrl Pts',(84.4016293336883,-0.233456082488926,
-4.4297423869698));
#13849=CARTESIAN_POINT('Ctrl Pts',(84.3966889037664,-0.350407633567806,
-4.42221048502865));
#13850=CARTESIAN_POINT('Ctrl Pts',(84.3916040760287,-0.466716354271229,
-4.41000795340358));
#13851=CARTESIAN_POINT('Ctrl Pts',(84.391176991259,-0.476485354472302,-4.40898303856334));
#13852=CARTESIAN_POINT('Ctrl Pts',(84.3907488878128,-0.486249846560294,
-4.40792518846741));
#13853=CARTESIAN_POINT('Ctrl Pts',(84.390319723676,-0.496009600215878,-4.40683442198824));
#13854=CARTESIAN_POINT('Ctrl Pts',(84.387894843512,-0.551154545982175,-4.40067133012542));
#13855=CARTESIAN_POINT('Ctrl Pts',(84.3854360262954,-0.606147076768305,
-4.39345753784936));
#13856=CARTESIAN_POINT('Ctrl Pts',(84.3829355680468,-0.66094268088986,-4.38519862474495));
#13857=CARTESIAN_POINT('Ctrl Pts',(84.382933532696,-0.660987284023301,-4.38519190206328));
#13858=CARTESIAN_POINT('Ctrl Pts',(84.3829314973177,-0.6610318870264,-4.38518517868924));
#13859=CARTESIAN_POINT('Ctrl Pts',(84.3829294619118,-0.661076489899159,
-4.38517845462283));
#13860=CARTESIAN_POINT('Ctrl Pts',(84.3777441956494,-0.774703835395292,
-4.36804866522549));
#13861=CARTESIAN_POINT('Ctrl Pts',(84.3723695177718,-0.88779606058497,-4.34636933738174));
#13862=CARTESIAN_POINT('Ctrl Pts',(84.3668823074273,-0.999973416805149,
-4.32022585152307));
#13863=CARTESIAN_POINT('Ctrl Pts',(84.3663254894094,-1.01135668247584,-4.31757292534336));
#13864=CARTESIAN_POINT('Ctrl Pts',(84.365767512611,-1.02273049790092,-4.31487406332162));
#13865=CARTESIAN_POINT('Ctrl Pts',(84.365208457365,-1.03409444672231,-4.31212937732032));
#13866=CARTESIAN_POINT('Ctrl Pts',(84.3591475471469,-1.1572949247151,-4.28237329229963));
#13867=CARTESIAN_POINT('Ctrl Pts',(84.3529604176001,-1.2793400076234,-4.24722710726337));
#13868=CARTESIAN_POINT('Ctrl Pts',(84.346738643613,-1.39974684446633,-4.20684946448488));
#13869=CARTESIAN_POINT('Ctrl Pts',(84.3405229114828,-1.52003675631752,-4.16651103173526));
#13870=CARTESIAN_POINT('Ctrl Pts',(84.3342729530153,-1.63869175079973,-4.12095164052296));
#13871=CARTESIAN_POINT('Ctrl Pts',(84.3280626968707,-1.75525351555293,-4.07036511954236));
#13872=CARTESIAN_POINT('Ctrl Pts',(84.323344383073,-1.84381266192753,-4.03193142625033));
#13873=CARTESIAN_POINT('Ctrl Pts',(84.3186491065442,-1.93116619998183,-3.99059460369246));
#13874=CARTESIAN_POINT('Ctrl Pts',(84.3140937959104,-2.01704032526029,-3.94631306123798));
#13875=CARTESIAN_POINT('Ctrl Pts',(84.3126577269723,-2.04411228012874,-3.93235323439904));
#13876=CARTESIAN_POINT('Ctrl Pts',(84.3112355683443,-2.07103686167745,-3.91810093225873));
#13877=CARTESIAN_POINT('Ctrl Pts',(84.3098309834969,-2.09780456156354,-3.90355539143292));
#13878=CARTESIAN_POINT('Ctrl Pts',(84.3049187094006,-2.19141961017728,-3.8526850694659));
#13879=CARTESIAN_POINT('Ctrl Pts',(84.3001301197621,-2.28318710933881,-3.7983694526866));
#13880=CARTESIAN_POINT('Ctrl Pts',(84.2953623456716,-2.37296857833148,-3.74093898603706));
#13881=CARTESIAN_POINT('Ctrl Pts',(84.2944446023704,-2.39025050909643,-3.72988426216618));
#13882=CARTESIAN_POINT('Ctrl Pts',(84.293527630326,-2.40745898081416,-3.7187140383902));
#13883=CARTESIAN_POINT('Ctrl Pts',(84.2926106958682,-2.4245931838124,-3.70743053955982));
#13884=CARTESIAN_POINT('Ctrl Pts',(84.2850622258382,-2.56564690550592,-3.61454150912677));
#13885=CARTESIAN_POINT('Ctrl Pts',(84.2775162212794,-2.70167171791562,-3.51397803803153));
#13886=CARTESIAN_POINT('Ctrl Pts',(84.2699673323685,-2.83185301388745,-3.4063468653672));
#13887=CARTESIAN_POINT('Ctrl Pts',(84.2661560849157,-2.89757833300751,-3.35200654621597));
#13888=CARTESIAN_POINT('Ctrl Pts',(84.2623441181025,-2.96181337970296,-3.29586420792149));
#13889=CARTESIAN_POINT('Ctrl Pts',(84.2585308156723,-3.02444877978825,-3.23799543932097));
#13890=CARTESIAN_POINT('Ctrl Pts',(84.2531361978723,-3.11305807590203,-3.15612942033363));
#13891=CARTESIAN_POINT('Ctrl Pts',(84.2479040427514,-3.19827388489918,-3.07059505341164));
#13892=CARTESIAN_POINT('Ctrl Pts',(84.2429201846493,-3.27959931121367,-2.98157340683114));
#13893=CARTESIAN_POINT('Ctrl Pts',(84.2426519708598,-3.28397596085487,-2.97678257356753));
#13894=CARTESIAN_POINT('Ctrl Pts',(84.2423844761919,-3.28834133566107,-2.97198165050621));
#13895=CARTESIAN_POINT('Ctrl Pts',(84.2421177140242,-3.29269535571472,-2.96717066938321));
#13896=CARTESIAN_POINT('Ctrl Pts',(84.236888511953,-3.37804497961775,-2.87286347180652));
#13897=CARTESIAN_POINT('Ctrl Pts',(84.2317189767506,-3.45931499008182,-2.7749495005523));
#13898=CARTESIAN_POINT('Ctrl Pts',(84.2265447526407,-3.5361731913615,-2.67380519287902));
#13899=CARTESIAN_POINT('Ctrl Pts',(84.2213673934426,-3.61307796140822,-2.57259960136585));
#13900=CARTESIAN_POINT('Ctrl Pts',(84.2161849768733,-3.68556521370341,-2.4681595865901));
#13901=CARTESIAN_POINT('Ctrl Pts',(84.2109169859668,-3.75333092100466,-2.36089697216956));
#13902=CARTESIAN_POINT('Ctrl Pts',(84.2060501515979,-3.81593628217304,-2.26180238608621));
#13903=CARTESIAN_POINT('Ctrl Pts',(84.2011098336268,-3.8745120190635,-2.16029823643245));
#13904=CARTESIAN_POINT('Ctrl Pts',(84.1960251220409,-3.92884440752957,-2.05673948987575));
#13905=CARTESIAN_POINT('Ctrl Pts',(84.1955981220718,-3.93340709074217,-2.0480429137124));
#13906=CARTESIAN_POINT('Ctrl Pts',(84.1951701038138,-3.93793987598769,-2.03933183384053));
#13907=CARTESIAN_POINT('Ctrl Pts',(84.1947410252724,-3.94244265133404,-2.03060645229457));
#13908=CARTESIAN_POINT('Ctrl Pts',(84.1923149363545,-3.96790217054373,-1.98127154171295));
#13909=CARTESIAN_POINT('Ctrl Pts',(84.1898548759893,-3.99240178177722,-1.9314804486622));
#13910=CARTESIAN_POINT('Ctrl Pts',(84.1873531275102,-4.01592141876326,-1.88127337373804));
#13911=CARTESIAN_POINT('Ctrl Pts',(84.1873510918653,-4.01594055643057,-1.88123252079897));
#13912=CARTESIAN_POINT('Ctrl Pts',(84.1873490561927,-4.01595969344922,-1.88119166758441));
#13913=CARTESIAN_POINT('Ctrl Pts',(84.1873470204926,-4.01597882981921,-1.88115081409439));
#13914=CARTESIAN_POINT('Ctrl Pts',(84.1819697230983,-4.06652750835006,-1.7732364115609));
#13915=CARTESIAN_POINT('Ctrl Pts',(84.1763910602686,-4.11265933192718,-1.66314804805023));
#13916=CARTESIAN_POINT('Ctrl Pts',(84.1706955902453,-4.15424332898281,-1.5512634750962));
#13917=CARTESIAN_POINT('Ctrl Pts',(84.1698688634138,-4.16027946050242,-1.53502285261677));
#13918=CARTESIAN_POINT('Ctrl Pts',(84.1690396754526,-4.16621977557407,-1.51874447338153));
#13919=CARTESIAN_POINT('Ctrl Pts',(84.1682082849763,-4.1720638824027,-1.50242958347748));
#13920=CARTESIAN_POINT('Ctrl Pts',(84.1621129362214,-4.21491001824171,-1.38281678215043));
#13921=CARTESIAN_POINT('Ctrl Pts',(84.1558997937435,-4.25258494005077,-1.26123583913524));
#13922=CARTESIAN_POINT('Ctrl Pts',(84.1496578445298,-4.28497060102772,-1.13814119430532));
#13923=CARTESIAN_POINT('Ctrl Pts',(84.1492041116699,-4.2873247436316,-1.12919333469826));
#13924=CARTESIAN_POINT('Ctrl Pts',(84.1487502265962,-4.28965093504631,-1.1202374993918));
#13925=CARTESIAN_POINT('Ctrl Pts',(84.1482962234882,-4.2919491288373,-1.11127387361339));
#13926=CARTESIAN_POINT('Ctrl Pts',(84.1416095743663,-4.32579738939976,-0.979255789620047));
#13927=CARTESIAN_POINT('Ctrl Pts',(84.134897742431,-4.35357361761577,-0.845541944315518));
#13928=CARTESIAN_POINT('Ctrl Pts',(84.1282458234568,-4.37517089418641,-0.710689438469849));
#13929=CARTESIAN_POINT('Ctrl Pts',(84.1237021614488,-4.38992313717226,-0.618577040548796));
#13930=CARTESIAN_POINT('Ctrl Pts',(84.1191966943683,-4.40177509059477,-0.525927551545028));
#13931=CARTESIAN_POINT('Ctrl Pts',(84.1148472705922,-4.41053065276273,-0.432914202617163));
#13932=CARTESIAN_POINT('Ctrl Pts',(84.1128481987243,-4.41455486353612,-0.390163627195017));
#13933=CARTESIAN_POINT('Ctrl Pts',(84.1108820907501,-4.41792484474684,-0.347336899647861));
#13934=CARTESIAN_POINT('Ctrl Pts',(84.1089603889782,-4.42062115446675,-0.304454516660194));
#13935=CARTESIAN_POINT('Ctrl Pts',(84.1044418844722,-4.42696099751471,-0.20362501044392));
#13936=CARTESIAN_POINT('Ctrl Pts',(84.0999225009031,-4.43000245478287,-0.102516986223067));
#13937=CARTESIAN_POINT('Ctrl Pts',(84.0954003870484,-4.42975191188515,-0.00133220471272644));
#13938=CARTESIAN_POINT('Ctrl Pts',(84.0953986853364,-4.42975181744819,-0.00129412797191142));
#13939=CARTESIAN_POINT('Ctrl Pts',(84.0921041236228,-4.42956868394745,0.0724235029283445));
#13940=CARTESIAN_POINT('Ctrl Pts',(84.0888129452018,-4.4276388654098,0.146073633444381));
#13941=CARTESIAN_POINT('Ctrl Pts',(84.0855227855576,-4.42397300444274,0.219615246120854));
#13942=CARTESIAN_POINT('Ctrl Pts',(84.0832767518464,-4.42147049751198,0.26981856727126));
#13943=CARTESIAN_POINT('Ctrl Pts',(84.081031192899,-4.41815876163643,0.319971342296661));
#13944=CARTESIAN_POINT('Ctrl Pts',(84.0787853565039,-4.41403849979053,0.370060518426921));
#13945=CARTESIAN_POINT('Ctrl Pts',(84.0766447228571,-4.41011124526732,0.417803344217714));
#13946=CARTESIAN_POINT('Ctrl Pts',(84.0745040431029,-4.40544960649604,0.465483779962639));
#13947=CARTESIAN_POINT('Ctrl Pts',(84.0723635194703,-4.40005552138737,0.513071474916498));
#13948=CARTESIAN_POINT('Ctrl Pts',(84.0683690128851,-4.38998942907243,0.601876549513941));
#13949=CARTESIAN_POINT('Ctrl Pts',(84.0643746841183,-4.37737225064415,0.690366878393935));
#13950=CARTESIAN_POINT('Ctrl Pts',(84.0603796133334,-4.36220899928437,0.778394604056078));
#13951=CARTESIAN_POINT('Ctrl Pts',(84.05617274016,-4.34624185406891,0.871089201361364));
#13952=CARTESIAN_POINT('Ctrl Pts',(84.0521774134784,-4.32708977131361,0.963202639840204));
#13953=CARTESIAN_POINT('Ctrl Pts',(84.0482733884729,-4.30496998710146,1.05454490782526));
#13954=CARTESIAN_POINT('Ctrl Pts',(84.0465086388677,-4.29497110635664,1.09583466163947));
#13955=CARTESIAN_POINT('Ctrl Pts',(84.044762545315,-4.2843657224338,1.13696754074424));
#13956=CARTESIAN_POINT('Ctrl Pts',(84.0430240012982,-4.27317320049019,1.17792941784365));
#13957=CARTESIAN_POINT('Ctrl Pts',(84.0376734094523,-4.23872678091809,1.30399484010832));
#13958=CARTESIAN_POINT('Ctrl Pts',(84.032373050424,-4.19875456442782,1.42844930968254));
#13959=CARTESIAN_POINT('Ctrl Pts',(84.0270479533909,-4.15340577613371,1.55078471097965));
#13960=CARTESIAN_POINT('Ctrl Pts',(84.0217176986437,-4.10801306449197,1.67323860233045));
#13961=CARTESIAN_POINT('Ctrl Pts',(84.0163622131321,-4.05723291931334,1.79356913068581));
#13962=CARTESIAN_POINT('Ctrl Pts',(84.0108900377808,-4.0012607786246,1.91127096742671));
#13963=CARTESIAN_POINT('Ctrl Pts',(84.0060032934323,-3.95127671842411,2.01638068131246));
#13964=CARTESIAN_POINT('Ctrl Pts',(84.0010229837432,-3.89715180930192,2.11939486055675));
#13965=CARTESIAN_POINT('Ctrl Pts',(83.9958781590854,-3.83906274531618,2.219956617997));
#13966=CARTESIAN_POINT('Ctrl Pts',(83.9952521771515,-3.83199492337375,2.23219218433321));
#13967=CARTESIAN_POINT('Ctrl Pts',(83.9946237597193,-3.82486842011884,2.24439150798265));
#13968=CARTESIAN_POINT('Ctrl Pts',(83.9939927789906,-3.81768355643046,2.25655399880712));
#13969=CARTESIAN_POINT('Ctrl Pts',(83.9932545591512,-3.80927758034196,2.27078358081195));
#13970=CARTESIAN_POINT('Ctrl Pts',(83.9925128278645,-3.80079179029708,2.28496265396045));
#13971=CARTESIAN_POINT('Ctrl Pts',(83.9917673800263,-3.79222676466892,2.29909021385551));
#13972=CARTESIAN_POINT('Ctrl Pts',(83.9917653465489,-3.79220340047755,2.29912875186197));
#13973=CARTESIAN_POINT('Ctrl Pts',(83.9917633130438,-3.79218003569659,2.2991672894851));
#13974=CARTESIAN_POINT('Ctrl Pts',(83.9917612795111,-3.79215667032603,2.29920582672493));
#13975=CARTESIAN_POINT('Ctrl Pts',(83.9865757948938,-3.73257524862255,2.39747533769407));
#13976=CARTESIAN_POINT('Ctrl Pts',(83.9812009167659,-3.66900089073088,2.49349808630057));
#13977=CARTESIAN_POINT('Ctrl Pts',(83.9757135262295,-3.60165872173485,2.58695647398915));
#13978=CARTESIAN_POINT('Ctrl Pts',(83.9751567956568,-3.59482643158448,2.59643842016334));
#13979=CARTESIAN_POINT('Ctrl Pts',(83.97459890695,-3.58795539964775,2.6058939557739));
#13980=CARTESIAN_POINT('Ctrl Pts',(83.9740399403985,-3.58104588944113,2.61532273982873));
#13981=CARTESIAN_POINT('Ctrl Pts',(83.9679789452048,-3.50612457610737,2.71756108428501));
#13982=CARTESIAN_POINT('Ctrl Pts',(83.9617917577651,-3.4266736543611,2.81665643569426));
#13983=CARTESIAN_POINT('Ctrl Pts',(83.9555699461621,-3.34302557056066,2.91222427944364));
#13984=CARTESIAN_POINT('Ctrl Pts',(83.94935417531,-3.25945870060518,3.00769933646447));
#13985=CARTESIAN_POINT('Ctrl Pts',(83.9431041983205,-3.17170307474004,3.09965400179128));
#13986=CARTESIAN_POINT('Ctrl Pts',(83.9368939332264,-3.08011415524685,3.18773995994843));
#13987=CARTESIAN_POINT('Ctrl Pts',(83.9321714407092,-3.01046688892119,3.25472345774784));
#13988=CARTESIAN_POINT('Ctrl Pts',(83.9274720317323,-2.93860077278703,3.31947182220502));
#13989=CARTESIAN_POINT('Ctrl Pts',(83.9229125305786,-2.86458353598871,3.38171618169541));
#13990=CARTESIAN_POINT('Ctrl Pts',(83.921480437798,-2.84133547728902,3.40126649978011));
#13991=CARTESIAN_POINT('Ctrl Pts',(83.9200621472598,-2.81787550339761,3.42056954585345));
#13992=CARTESIAN_POINT('Ctrl Pts',(83.9186612788476,-2.79420655895491,3.43961634624809));
#13993=CARTESIAN_POINT('Ctrl Pts',(83.9137520717548,-2.71126104535474,3.50636400561238));
#13994=CARTESIAN_POINT('Ctrl Pts',(83.9089667419841,-2.62585089380582,3.57008342169783));
#13995=CARTESIAN_POINT('Ctrl Pts',(83.9042023368082,-2.53833398823929,3.63077443813605));
#13996=CARTESIAN_POINT('Ctrl Pts',(83.903280789688,-2.52140617683094,3.64251349670761));
#13997=CARTESIAN_POINT('Ctrl Pts',(83.902360025411,-2.50439941431259,3.65413933914884));
#13998=CARTESIAN_POINT('Ctrl Pts',(83.9014392989632,-2.48731609731623,3.6656520795929));
#13999=CARTESIAN_POINT('Ctrl Pts',(83.893890900357,-2.34726181028116,3.76003706671547));
#14000=CARTESIAN_POINT('Ctrl Pts',(83.8863449624767,-2.20206255364273,3.84682508637063));
#14001=CARTESIAN_POINT('Ctrl Pts',(83.8787961362334,-2.05259191981534,3.92549805073244));
#14002=CARTESIAN_POINT('Ctrl Pts',(83.8749840512519,-1.97711068074216,3.96522714453188));
#14003=CARTESIAN_POINT('Ctrl Pts',(83.8711712456039,-1.90054003840731,4.00288588696796));
#14004=CARTESIAN_POINT('Ctrl Pts',(83.8673571028617,-1.82299194579675,4.0384024029594));
#14005=CARTESIAN_POINT('Ctrl Pts',(83.861671776735,-1.70739947147196,4.09134299536656));
#14006=CARTESIAN_POINT('Ctrl Pts',(83.8561715279256,-1.58949550822084,4.13922841460962));
#14007=CARTESIAN_POINT('Ctrl Pts',(83.8509475525488,-1.46970726301584,4.18161804952431));
#14008=CARTESIAN_POINT('Ctrl Pts',(83.8457180259812,-1.34979172635732,4.2240527292448));
#14009=CARTESIAN_POINT('Ctrl Pts',(83.8405480859766,-1.2281190573001,4.26133255678184));
#14010=CARTESIAN_POINT('Ctrl Pts',(83.835373360171,-1.10516466997342,4.29329593792215));
#14011=CARTESIAN_POINT('Ctrl Pts',(83.830195501057,-0.982135833481593,4.32527867296346));
#14012=CARTESIAN_POINT('Ctrl Pts',(83.8250124873297,-0.857823707063181,
4.35193812240549));
#14013=CARTESIAN_POINT('Ctrl Pts',(83.8197437912569,-0.732725519128845,
4.37315232248143));
#14014=CARTESIAN_POINT('Ctrl Pts',(83.8148767348689,-0.617163731868134,
4.3927493359679));
#14015=CARTESIAN_POINT('Ctrl Pts',(83.809936115427,-0.500930638268043,4.40769966463376));
#14016=CARTESIAN_POINT('Ctrl Pts',(83.8048510408623,-0.384436097958309,
4.41794280566729));
#14017=CARTESIAN_POINT('Ctrl Pts',(83.8044235307491,-0.374642221096632,
4.41880396243646));
#14018=CARTESIAN_POINT('Ctrl Pts',(83.8039949996233,-0.36484647269912,4.41963186800146));
#14019=CARTESIAN_POINT('Ctrl Pts',(83.8035654053595,-0.355049083076931,
4.42042649680689));
#14020=CARTESIAN_POINT('Ctrl Pts',(83.8011431360686,-0.299806455297337,
4.42490701508921));
#14021=CARTESIAN_POINT('Ctrl Pts',(83.7986869927428,-0.244512795542103,
4.42832951566351));
#14022=CARTESIAN_POINT('Ctrl Pts',(83.7961892995956,-0.189212704827418,
4.43069097878495));
#14023=CARTESIAN_POINT('Ctrl Pts',(83.7961872624375,-0.189167601199163,
4.43069290483161));
#14024=CARTESIAN_POINT('Ctrl Pts',(83.7961852252519,-0.189122497566507,
4.43069483017255));
#14025=CARTESIAN_POINT('Ctrl Pts',(83.7961831880386,-0.189077393929466,
4.43069675480781));
#14026=CARTESIAN_POINT('Ctrl Pts',(83.7909980958776,-0.074280129178877,
4.43559531459573));
#14027=CARTESIAN_POINT('Ctrl Pts',(83.785623599497,0.0408613960656662,4.43592667179727));
#14028=CARTESIAN_POINT('Ctrl Pts',(83.7801365849949,0.155958163511104,4.43170203503521));
#14029=CARTESIAN_POINT('Ctrl Pts',(83.7795799531664,0.167634189533694,4.43127346549442));
#14030=CARTESIAN_POINT('Ctrl Pts',(83.7790221633972,0.179309719652794,4.43079803619748));
#14031=CARTESIAN_POINT('Ctrl Pts',(83.7784632959555,0.190984324241664,4.43027577732082));
#14032=CARTESIAN_POINT('Ctrl Pts',(83.77240277904,0.317587044874403,4.42461225405919));
#14033=CARTESIAN_POINT('Ctrl Pts',(83.7662160650533,0.444085919803523,4.41343834714048));
#14034=CARTESIAN_POINT('Ctrl Pts',(83.7599947286139,0.569976779683552,4.39681746005267));
#14035=CARTESIAN_POINT('Ctrl Pts',(83.7537794334196,0.695745392914888,4.38021271272073));
#14036=CARTESIAN_POINT('Ctrl Pts',(83.7475299337402,0.820907251237237,4.35817192446295));
#14037=CARTESIAN_POINT('Ctrl Pts',(83.7413201587169,0.944975540862707,4.33079772638433));
#14038=CARTESIAN_POINT('Ctrl Pts',(83.7366031774661,1.03921853578525,4.31000412619592));
#14039=CARTESIAN_POINT('Ctrl Pts',(83.7319092369034,1.13283341894311,4.28613239844926));
#14040=CARTESIAN_POINT('Ctrl Pts',(83.7273552997934,1.2255595276426,4.25908925970827));
#14041=CARTESIAN_POINT('Ctrl Pts',(83.7259184348083,1.25481660686286,4.25055656849965));
#14042=CARTESIAN_POINT('Ctrl Pts',(83.7244955076997,1.28398483229506,4.2417082638057));
#14043=CARTESIAN_POINT('Ctrl Pts',(83.7230901924276,1.31305499752794,4.23254176849106));
#14044=CARTESIAN_POINT('Ctrl Pts',(83.7181776848939,1.41467447647992,4.20049879693493));
#14045=CARTESIAN_POINT('Ctrl Pts',(83.7133888293406,1.51513881220252,4.16472052270079));
#14046=CARTESIAN_POINT('Ctrl Pts',(83.7086207664946,1.61424885826624,4.12550486535286));
#14047=CARTESIAN_POINT('Ctrl Pts',(83.7077039761991,1.6333054712653,4.11796458426871));
#14048=CARTESIAN_POINT('Ctrl Pts',(83.7067879546218,1.65231215695153,4.11029715863561));
#14049=CARTESIAN_POINT('Ctrl Pts',(83.7058719705771,1.67126769888763,4.10250461110111));
#14050=CARTESIAN_POINT('Ctrl Pts',(83.6983238768225,1.82746933638149,4.03829074218398));
#14051=CARTESIAN_POINT('Ctrl Pts',(83.6907782499507,1.98020189059388,3.96558359210025));
#14052=CARTESIAN_POINT('Ctrl Pts',(83.6832297395517,2.12854987973628,3.88482306144842));
#14053=CARTESIAN_POINT('Ctrl Pts',(83.679419412548,2.20343277968634,3.84405686858208));
#14054=CARTESIAN_POINT('Ctrl Pts',(83.6756083666427,2.27719782470252,3.80123805572656));
#14055=CARTESIAN_POINT('Ctrl Pts',(83.6717959857574,2.34972329100296,3.75641988700811));
#14056=CARTESIAN_POINT('Ctrl Pts',(83.6664177671139,2.45203673415599,3.69319380393264));
#14057=CARTESIAN_POINT('Ctrl Pts',(83.6612005502138,2.551736824447,3.62574492221054));
#14058=CARTESIAN_POINT('Ctrl Pts',(83.6562305162575,2.64830487667778,3.55415362758043));
#14059=CARTESIAN_POINT('Ctrl Pts',(83.6559476717751,2.65380056161585,3.55007936916362));
#14060=CARTESIAN_POINT('Ctrl Pts',(83.6556656278551,2.65928609232917,3.54599170401589));
#14061=CARTESIAN_POINT('Ctrl Pts',(83.6553844003821,2.66476136953762,3.54189065047767));
#14062=CARTESIAN_POINT('Ctrl Pts',(83.6501559879268,2.76655443852363,3.46564632350785));
#14063=CARTESIAN_POINT('Ctrl Pts',(83.6449872923774,2.86503315524786,3.38508292429783));
#14064=CARTESIAN_POINT('Ctrl Pts',(83.6398139617035,2.95979960583976,3.30050642057553));
#14065=CARTESIAN_POINT('Ctrl Pts',(83.6346374916142,3.05462356508098,3.21587859193324));
#14066=CARTESIAN_POINT('Ctrl Pts',(83.6294560182221,3.1457304301424,3.12723254995599));
#14067=CARTESIAN_POINT('Ctrl Pts',(83.6241890224578,3.23274317603943,3.03491436927644));
#14068=CARTESIAN_POINT('Ctrl Pts',(83.6193227826456,3.31313528326577,2.94962050797348));
#14069=CARTESIAN_POINT('Ctrl Pts',(83.6143830940161,3.39003289396152,2.86119163286796));
#14070=CARTESIAN_POINT('Ctrl Pts',(83.6092990232269,3.46315841226844,2.76993532987214));
#14071=CARTESIAN_POINT('Ctrl Pts',(83.6088724314768,3.46929419285222,2.76227824018534));
#14072=CARTESIAN_POINT('Ctrl Pts',(83.6084448232082,3.47540344518774,2.75460123514701));
#14073=CARTESIAN_POINT('Ctrl Pts',(83.6080161565174,3.48148602117807,2.74690449123667));
#14074=CARTESIAN_POINT('Ctrl Pts',(83.6055834116648,3.51600551091099,2.70322436741865));
#14075=CARTESIAN_POINT('Ctrl Pts',(83.6031165029076,3.54966513737925,2.65890943823865));
#14076=CARTESIAN_POINT('Ctrl Pts',(83.6006076436536,3.58243728965208,2.61399563943773));
#14077=CARTESIAN_POINT('Ctrl Pts',(83.6006056057948,3.58246390932781,2.6139591575262));
#14078=CARTESIAN_POINT('Ctrl Pts',(83.6006035679082,3.58249052841819,2.61392267521949));
#14079=CARTESIAN_POINT('Ctrl Pts',(83.6006015299941,3.58251714692321,2.61388619251767));
#14080=CARTESIAN_POINT('Ctrl Pts',(83.5954166817284,3.65023977746171,2.52106713544909));
#14081=CARTESIAN_POINT('Ctrl Pts',(83.5900423118012,3.71435230953212,2.42542966378751));
#14082=CARTESIAN_POINT('Ctrl Pts',(83.584555266241,3.77464845947616,2.32730368333586));
#14083=CARTESIAN_POINT('Ctrl Pts',(83.5839973965675,3.78077878828693,2.31732718358245));
#14084=CARTESIAN_POINT('Ctrl Pts',(83.5834383621824,3.78686967036942,2.30732500482146));
#14085=CARTESIAN_POINT('Ctrl Pts',(83.5828782438472,3.79292089131384,2.29729752376806));
#14086=CARTESIAN_POINT('Ctrl Pts',(83.5768163714489,3.85841014048677,2.1887752583749));
#14087=CARTESIAN_POINT('Ctrl Pts',(83.5706280763583,3.91925405413166,2.07728344318731));
#14088=CARTESIAN_POINT('Ctrl Pts',(83.5644049661865,3.97522582996733,1.96327700683015));
#14089=CARTESIAN_POINT('Ctrl Pts',(83.5581879051488,4.03114319880001,1.84938138969269));
#14090=CARTESIAN_POINT('Ctrl Pts',(83.5519364479608,4.0821982463679,1.73297617410154));
#14091=CARTESIAN_POINT('Ctrl Pts',(83.5457245712611,4.12820645876471,1.61452358162241));
#14092=CARTESIAN_POINT('Ctrl Pts',(83.5410209908633,4.16304348732034,1.52483228235841));
#14093=CARTESIAN_POINT('Ctrl Pts',(83.5363402224714,4.19498794677658,1.43396432677261));
#14094=CARTESIAN_POINT('Ctrl Pts',(83.5317995616617,4.22381742177296,1.34208276760707));
#14095=CARTESIAN_POINT('Ctrl Pts',(83.5303478472981,4.23303461827788,1.31270691577096));
#14096=CARTESIAN_POINT('Ctrl Pts',(83.5289104543474,4.24193329377069,1.28322783771989));
#14097=CARTESIAN_POINT('Ctrl Pts',(83.5274912160669,4.25050589703514,1.25365195119791));
#14098=CARTESIAN_POINT('Ctrl Pts',(83.5225652846931,4.28025992492025,1.15099914840792));
#14099=CARTESIAN_POINT('Ctrl Pts',(83.5177622460202,4.30624407429985,1.04723109347148));
#14100=CARTESIAN_POINT('Ctrl Pts',(83.5129795917191,4.3285951463578,0.942680774685479));
#14101=CARTESIAN_POINT('Ctrl Pts',(83.5120764624614,4.33281579578061,0.922938086661672));
#14102=CARTESIAN_POINT('Ctrl Pts',(83.5111740600778,4.33690692070658,0.903167357049539));
#14103=CARTESIAN_POINT('Ctrl Pts',(83.5102716943254,4.34086947147152,0.883370621573313));
#14104=CARTESIAN_POINT('Ctrl Pts',(83.5027215983376,4.37402414135265,0.71773129772002));
#14105=CARTESIAN_POINT('Ctrl Pts',(83.4951739851061,4.39818241547758,0.55026993718802));
#14106=CARTESIAN_POINT('Ctrl Pts',(83.4876235034185,4.41320306700913,0.381992895145997));
#14107=CARTESIAN_POINT('Ctrl Pts',(83.4838129798435,4.42078358294728,0.297068030432569));
#14108=CARTESIAN_POINT('Ctrl Pts',(83.4800017414153,4.42603592339558,0.211935627319798));
#14109=CARTESIAN_POINT('Ctrl Pts',(83.4761891720582,4.42893697379109,0.126726501352696));
#14110=CARTESIAN_POINT('Ctrl Pts',(83.4711900572098,4.43274088730706,0.014998643590784));
#14111=CARTESIAN_POINT('Ctrl Pts',(83.4663151445685,4.43228269129631,-0.0968724714744418));
#14112=CARTESIAN_POINT('Ctrl Pts',(83.4616590637086,4.42734101575312,-0.20850640372019));
#14113=CARTESIAN_POINT('Ctrl Pts',(83.4610199200294,4.42666266827954,-0.223830476545876));
#14114=CARTESIAN_POINT('Ctrl Pts',(83.4603848998537,4.42589984630004,-0.239150000201453));
#14115=CARTESIAN_POINT('Ctrl Pts',(83.4597542479529,4.42505198770308,-0.254463914514458));
#14116=CARTESIAN_POINT('Ctrl Pts',(83.4545238336106,4.41802013421873,-0.381472359208858));
#14117=CARTESIAN_POINT('Ctrl Pts',(83.4493532883236,4.40555445277623,-0.508116824523829));
#14118=CARTESIAN_POINT('Ctrl Pts',(83.4441783208528,4.38768895006725,-0.633896375290781));
#14119=CARTESIAN_POINT('Ctrl Pts',(83.4390002249744,4.36981264717916,-0.759751963194735));
#14120=CARTESIAN_POINT('Ctrl Pts',(83.4338173390892,4.34652961734655,-0.884741454493317));
#14121=CARTESIAN_POINT('Ctrl Pts',(83.4285492038077,4.31791882352173,-1.00835906006262));
#14122=CARTESIAN_POINT('Ctrl Pts',(83.4236813525029,4.29148193786622,-1.12258394048542));
#14123=CARTESIAN_POINT('Ctrl Pts',(83.4187402686918,4.2604959670513,-1.23563797592087));
#14124=CARTESIAN_POINT('Ctrl Pts',(83.4136550391749,4.22506300672305,-1.34711935625403));
#14125=CARTESIAN_POINT('Ctrl Pts',(83.413229011399,4.22209452216738,-1.35645898671952));
#14126=CARTESIAN_POINT('Ctrl Pts',(83.4128019719122,4.21909483432159,-1.36578760828526));
#14127=CARTESIAN_POINT('Ctrl Pts',(83.4123738790171,4.21606400765798,-1.37510500073172));
#14128=CARTESIAN_POINT('Ctrl Pts',(83.4099529500042,4.19892423195254,-1.42779624124671));
#14129=CARTESIAN_POINT('Ctrl Pts',(83.4074982579746,4.18078900305616,-1.48012728715261));
#14130=CARTESIAN_POINT('Ctrl Pts',(83.4050021356873,4.16167269623072,-1.53205585686474));
#14131=CARTESIAN_POINT('Ctrl Pts',(83.4050001147405,4.16165721900856,-1.53209790002805));
#14132=CARTESIAN_POINT('Ctrl Pts',(83.4049980937665,4.16164174114336,-1.5321399429277));
#14133=CARTESIAN_POINT('Ctrl Pts',(83.4049960727654,4.16162626263514,-1.53218198556367));
#14134=CARTESIAN_POINT('Ctrl Pts',(83.3998090342966,4.12189960606499,-1.6400873041627));
#14135=CARTESIAN_POINT('Ctrl Pts',(83.39443278481,4.07781980193203,-1.74654803110892));
#14136=CARTESIAN_POINT('Ctrl Pts',(83.3889442402674,4.0295474499751,-1.85120901823054));
#14137=CARTESIAN_POINT('Ctrl Pts',(83.3883887623086,4.02466196033003,-1.86180142046694));
#14138=CARTESIAN_POINT('Ctrl Pts',(83.3878321341325,4.01973356519352,-1.87237536606769));
#14139=CARTESIAN_POINT('Ctrl Pts',(83.3872744354734,4.01476245694717,-1.88293047238602));
#14140=CARTESIAN_POINT('Ctrl Pts',(83.3812136369893,3.96073886404263,-1.99763824750323));
#14141=CARTESIAN_POINT('Ctrl Pts',(83.3750269467086,3.90166577113011,-2.11012439295221));
#14142=CARTESIAN_POINT('Ctrl Pts',(83.3688058702781,3.83779625481318,-2.21994776795051));
#14143=CARTESIAN_POINT('Ctrl Pts',(83.3625908230251,3.77398863785629,-2.32966470724957));
#14144=CARTESIAN_POINT('Ctrl Pts',(83.3563418066165,3.70539419617667,-2.43672425023083));
#14145=CARTESIAN_POINT('Ctrl Pts',(83.3501326438124,3.6322954950446,-2.54071638406537));
#14146=CARTESIAN_POINT('Ctrl Pts',(83.3453747546907,3.57628222467187,-2.6204023349633));
#14147=CARTESIAN_POINT('Ctrl Pts',(83.3406403877156,3.51762241240995,-2.69828955358027));
#14148=CARTESIAN_POINT('Ctrl Pts',(83.3360454945849,3.45633625635999,-2.77409862803806));
#14149=CARTESIAN_POINT('Ctrl Pts',(83.3346482625727,3.43770013649747,-2.79715093037385));
#14150=CARTESIAN_POINT('Ctrl Pts',(83.3332639272723,3.41882139867615,-2.82001079176768));
#14151=CARTESIAN_POINT('Ctrl Pts',(83.3318957489754,3.39970124785076,-2.84266964208191));
#14152=CARTESIAN_POINT('Ctrl Pts',(83.3270132673139,3.33146906935275,-2.92353002510502));
#14153=CARTESIAN_POINT('Ctrl Pts',(83.3222563202797,3.26027188291528,-3.00191668634912));
#14154=CARTESIAN_POINT('Ctrl Pts',(83.3175212277932,3.18645817129212,-3.07776470819284));
#14155=CARTESIAN_POINT('Ctrl Pts',(83.3165680478573,3.17159938044212,-3.09303300818994));
#14156=CARTESIAN_POINT('Ctrl Pts',(83.3156157535154,3.15663444020069,-3.10819855383837));
#14157=CARTESIAN_POINT('Ctrl Pts',(83.314663499032,3.14156600359999,-3.12326098650216));
#14158=CARTESIAN_POINT('Ctrl Pts',(83.3071167037327,3.02214581867496,-3.24263358910162));
#14159=CARTESIAN_POINT('Ctrl Pts',(83.2995723295983,2.89622647997022,-3.35553454280886));
#14160=CARTESIAN_POINT('Ctrl Pts',(83.2920250328264,2.76456537085735,-3.46128825066738));
#14161=CARTESIAN_POINT('Ctrl Pts',(83.2882075858386,2.69797075830039,-3.51477881632305));
#14162=CARTESIAN_POINT('Ctrl Pts',(83.2843894074362,2.62990689191812,-3.56644000015238));
#14163=CARTESIAN_POINT('Ctrl Pts',(83.2805698800677,2.56047027845926,-3.61617938269018));
#14164=CARTESIAN_POINT('Ctrl Pts',(83.274882611746,2.45707930517862,-3.69024122002343));
#14165=CARTESIAN_POINT('Ctrl Pts',(83.2694212546832,2.35041368498791,-3.75971890711027));
#14166=CARTESIAN_POINT('Ctrl Pts',(83.2641962605888,2.24088491821295,-3.82421505258511));
#14167=CARTESIAN_POINT('Ctrl Pts',(83.2589657305283,2.13124010393381,-3.88877953277175));
#14168=CARTESIAN_POINT('Ctrl Pts',(83.2537941812851,2.0188842603045,-3.94861631443767));
#14169=CARTESIAN_POINT('Ctrl Pts',(83.2486170992431,1.90425347118074,-4.00347568986756));
#14170=CARTESIAN_POINT('Ctrl Pts',(83.2434368894082,1.78955342656573,-4.05836820921127));
#14171=CARTESIAN_POINT('Ctrl Pts',(83.2382507755029,1.67257559122187,-4.10827691655245));
#14172=CARTESIAN_POINT('Ctrl Pts',(83.232978127041,1.55378509690204,-4.15298685851507));
#14173=CARTESIAN_POINT('Ctrl Pts',(83.2281105165493,1.44411993324624,-4.19426224111572));
#14174=CARTESIAN_POINT('Ctrl Pts',(83.2231687085409,1.33290939295841,-4.23110701948943));
#14175=CARTESIAN_POINT('Ctrl Pts',(83.2180819163818,1.22054383348356,-4.2633835944284));
#14176=CARTESIAN_POINT('Ctrl Pts',(83.2176507811159,1.21102019779215,-4.26611922216453));
#14177=CARTESIAN_POINT('Ctrl Pts',(83.2172186043491,1.20148824518652,-4.26882205787307));
#14178=CARTESIAN_POINT('Ctrl Pts',(83.2167853429832,1.19194820207161,-4.27149203085028));
#14179=CARTESIAN_POINT('Ctrl Pts',(83.2143813551094,1.13901445406698,-4.28630660506678));
#14180=CARTESIAN_POINT('Ctrl Pts',(83.2119439043162,1.08583272356488,-4.3001091693648));
#14181=CARTESIAN_POINT('Ctrl Pts',(83.2094655122813,1.032445146656,-4.31288851184167));
#14182=CARTESIAN_POINT('Ctrl Pts',(83.2094634559398,1.03240085056045,-4.31289911496338));
#14183=CARTESIAN_POINT('Ctrl Pts',(83.2094613995701,1.03235655432311,-4.31290971738082));
#14184=CARTESIAN_POINT('Ctrl Pts',(83.2094593431722,1.03231225794397,-4.31292031909402));
#14185=CARTESIAN_POINT('Ctrl Pts',(83.2042762343558,0.920664139950302,-4.33964172047668));
#14186=CARTESIAN_POINT('Ctrl Pts',(83.1989037007853,0.807805603682432,-4.36195383867267));
#14187=CARTESIAN_POINT('Ctrl Pts',(83.1934186670854,0.694120027050924,-4.37979314581744));
#14188=CARTESIAN_POINT('Ctrl Pts',(83.1928629297045,0.682601533626714,-4.38160060414353));
#14189=CARTESIAN_POINT('Ctrl Pts',(83.1923060374522,0.671074589850501,-4.3833621661427));
#14190=CARTESIAN_POINT('Ctrl Pts',(83.1917480703369,0.659539620962272,-4.38507777932936));
#14191=CARTESIAN_POINT('Ctrl Pts',(83.1856904731488,0.534309668887365,-4.40370341752789));
#14192=CARTESIAN_POINT('Ctrl Pts',(83.1795067222463,0.408128309738017,-4.4169110341505));
#14193=CARTESIAN_POINT('Ctrl Pts',(83.1732884166176,0.281501608649066,-4.42466627281055));
#14194=CARTESIAN_POINT('Ctrl Pts',(83.1670761523311,0.154997930659677,-4.43241397693414));
#14195=CARTESIAN_POINT('Ctrl Pts',(83.1608297506867,0.0280497684847077,
-4.43472026555932));
#14196=CARTESIAN_POINT('Ctrl Pts',(83.1546231847352,-0.0988462957672127,
-4.43159260547438));
#14197=CARTESIAN_POINT('Ctrl Pts',(83.1499306446216,-0.194787413032101,
-4.42922790484522));
#14198=CARTESIAN_POINT('Ctrl Pts',(83.1452609940217,-0.290701728684633,
-4.42375682800405));
#14199=CARTESIAN_POINT('Ctrl Pts',(83.1407318165524,-0.386354485368013,
-4.41503603971653));
#14200=CARTESIAN_POINT('Ctrl Pts',(83.1392748197715,-0.417125140640413,
-4.41223063839405));
#14201=CARTESIAN_POINT('Ctrl Pts',(83.1378323598895,-0.447868327306429,
-4.40908898022418));
#14202=CARTESIAN_POINT('Ctrl Pts',(83.1364083513007,-0.478575093763186,
-4.40560645526888));
#14203=CARTESIAN_POINT('Ctrl Pts',(83.1314823913209,-0.584796575758634,
-4.39355963287357));
#14204=CARTESIAN_POINT('Ctrl Pts',(83.1266791266776,-0.690596500927511,
-4.37760349242614));
#14205=CARTESIAN_POINT('Ctrl Pts',(83.1218960858815,-0.795719867644331,
-4.35799264321106));
#14206=CARTESIAN_POINT('Ctrl Pts',(83.1210003234424,-0.815407252174682,
-4.35431994567937));
#14207=CARTESIAN_POINT('Ctrl Pts',(83.1201052703218,-0.835071050871667,
-4.35051903223484));
#14208=CARTESIAN_POINT('Ctrl Pts',(83.1192102534356,-0.854709785325135,
-4.34659152404242));
#14209=CARTESIAN_POINT('Ctrl Pts',(83.1116643988368,-1.02028323648516,-4.31347884626688));
#14210=CARTESIAN_POINT('Ctrl Pts',(83.1041210386046,-1.18407820825324,-4.2713714180056));
#14211=CARTESIAN_POINT('Ctrl Pts',(83.0965748157052,-1.34511223604663,-4.22052663331527));
#14212=CARTESIAN_POINT('Ctrl Pts',(83.0927737523542,-1.42622573474487,-4.19491590722648));
#14213=CARTESIAN_POINT('Ctrl Pts',(83.0889719781047,-1.50663820973591,-4.16708763564311));
#14214=CARTESIAN_POINT('Ctrl Pts',(83.0851688787083,-1.58622088491304,-4.13707070931025));
#14215=CARTESIAN_POINT('Ctrl Pts',(83.0802290600159,-1.68959025432714,-4.09808193769794));
#14216=CARTESIAN_POINT('Ctrl Pts',(83.0754089626005,-1.79148850189328,-4.05520097269121));
#14217=CARTESIAN_POINT('Ctrl Pts',(83.0708045781324,-1.89149125190055,-4.00836457291793));
#14218=CARTESIAN_POINT('Ctrl Pts',(83.0701160143723,-1.9064461867097,-4.00136041247981));
#14219=CARTESIAN_POINT('Ctrl Pts',(83.0694322747687,-1.92135864759915,-3.99426783906397));
#14220=CARTESIAN_POINT('Ctrl Pts',(83.0687536803555,-1.93622712847732,-3.98708669161156));
#14221=CARTESIAN_POINT('Ctrl Pts',(83.0635317258871,-2.05064382372104,-3.93182595809779));
#14222=CARTESIAN_POINT('Ctrl Pts',(83.0583701263716,-2.16263885447323,-3.8717010322688));
#14223=CARTESIAN_POINT('Ctrl Pts',(83.0532046183295,-2.27176411047279,-3.80693589126885));
#14224=CARTESIAN_POINT('Ctrl Pts',(83.0480359361002,-2.38095642357315,-3.74213095230876));
#14225=CARTESIAN_POINT('Ctrl Pts',(83.0428629803953,-2.48727516552271,-3.67267980234581));
#14226=CARTESIAN_POINT('Ctrl Pts',(83.0376052600746,-2.5902850983655,-3.5988496773313));
#14227=CARTESIAN_POINT('Ctrl Pts',(83.0327438048167,-2.68553135512561,-3.53058399799632));
#14228=CARTESIAN_POINT('Ctrl Pts',(83.0278094365958,-2.77794913347238,-3.45857417713402));
#14229=CARTESIAN_POINT('Ctrl Pts',(83.022730999609,-2.86720719965072,-3.38306923522428));
#14230=CARTESIAN_POINT('Ctrl Pts',(83.0223090528177,-2.87462329139591,-3.37679583495479));
#14231=CARTESIAN_POINT('Ctrl Pts',(83.02188611148,-2.88201760041316,-3.37049830368306));
#14232=CARTESIAN_POINT('Ctrl Pts',(83.0214621347834,-2.88938995281641,-3.3641767821702));
#14233=CARTESIAN_POINT('Ctrl Pts',(83.0189708446667,-2.932709948522,-3.32703147632875));
#14234=CARTESIAN_POINT('Ctrl Pts',(83.0164437251978,-2.97527093498445,-3.2890586609128));
#14235=CARTESIAN_POINT('Ctrl Pts',(83.0138723507173,-3.01703632090005,-3.2502907069457));
#14236=CARTESIAN_POINT('Ctrl Pts',(83.0138703039779,-3.01706956493473,-3.25025984877983));
#14237=CARTESIAN_POINT('Ctrl Pts',(83.0138682572104,-3.01710280846552,-3.25022899011018));
#14238=CARTESIAN_POINT('Ctrl Pts',(83.0138662104149,-3.01713605149244,-3.25019813093678));
#14239=CARTESIAN_POINT('Ctrl Pts',(83.0087347594115,-3.1004785067607,-3.17283215325411));
#14240=CARTESIAN_POINT('Ctrl Pts',(83.0034159680191,-3.18089387926395,-3.09206394837344));
#14241=CARTESIAN_POINT('Ctrl Pts',(82.9979843348117,-3.25811675623012,-3.00817024856034));
#14242=CARTESIAN_POINT('Ctrl Pts',(82.9974493435073,-3.26572286034265,-2.99990709856862));
#14243=CARTESIAN_POINT('Ctrl Pts',(82.996913257484,-3.27329798884271,-2.99161366854329));
#14244=CARTESIAN_POINT('Ctrl Pts',(82.996376147928,-3.28084188596267,-2.98329025010284));
#14245=CARTESIAN_POINT('Ctrl Pts',(82.99039332449,-3.3648727954933,-2.8905763104994));
#14246=CARTESIAN_POINT('Ctrl Pts',(82.9842840229385,-3.44502954170072,-2.79413572203119));
#14247=CARTESIAN_POINT('Ctrl Pts',(82.9781369279056,-3.5210052932334,-2.6943596675154));
#14248=CARTESIAN_POINT('Ctrl Pts',(82.9719965698146,-3.59689777873267,-2.59469296310303));
#14249=CARTESIAN_POINT('Ctrl Pts',(82.9658188451291,-3.66861870715653,-2.4916983245184));
#14250=CARTESIAN_POINT('Ctrl Pts',(82.9596760395827,-3.73590152906811,-2.3857833174973));
#14251=CARTESIAN_POINT('Ctrl Pts',(82.9549408128507,-3.787766986067,-2.30413795711975));
#14252=CARTESIAN_POINT('Ctrl Pts',(82.9502264590364,-3.83699676504752,-2.22075475036848));
#14253=CARTESIAN_POINT('Ctrl Pts',(82.9456496772315,-3.88334000890611,-2.13575781248512));
#14254=CARTESIAN_POINT('Ctrl Pts',(82.944292813768,-3.8970792381408,-2.11055904958906));
#14255=CARTESIAN_POINT('Ctrl Pts',(82.942948041854,-3.91056460553878,-2.08521876279161));
#14256=CARTESIAN_POINT('Ctrl Pts',(82.9416184023416,-3.92378920759747,-2.05974098750738));
#14257=CARTESIAN_POINT('Ctrl Pts',(82.9368771085923,-3.97094614186146,-1.9688910875301));
#14258=CARTESIAN_POINT('Ctrl Pts',(82.9322682646822,-4.01487748023783,-1.87634492024307));
#14259=CARTESIAN_POINT('Ctrl Pts',(82.9276849638517,-4.05566876559709,-1.78243544837345));
#14260=CARTESIAN_POINT('Ctrl Pts',(82.9266495030548,-4.06488434589737,-1.76121939030247));
#14261=CARTESIAN_POINT('Ctrl Pts',(82.9256153459765,-4.07393974301493,-1.73993355659287));
#14262=CARTESIAN_POINT('Ctrl Pts',(82.924581259878,-4.08283608159913,-1.71858144525149));
#14263=CARTESIAN_POINT('Ctrl Pts',(82.9166349033586,-4.15119932350881,-1.55450275837398));
#14264=CARTESIAN_POINT('Ctrl Pts',(82.9086926499015,-4.21017510191321,-1.38650973643088));
#14265=CARTESIAN_POINT('Ctrl Pts',(82.900749320533,-4.25938512909566,-1.21574718217419));
#14266=CARTESIAN_POINT('Ctrl Pts',(82.8974727757882,-4.27968377824818,-1.14530931867953));
#14267=CARTESIAN_POINT('Ctrl Pts',(82.8941960587482,-4.29832015049098,-1.07440021001745));
#14268=CARTESIAN_POINT('Ctrl Pts',(82.890918840253,-4.31526507376258,-1.00310021346923));
#14269=CARTESIAN_POINT('Ctrl Pts',(82.8870928818563,-4.33504726758591,-0.919861692484912));
#14270=CARTESIAN_POINT('Ctrl Pts',(82.8832662196026,-4.35252498261166,-0.836085699931758));
#14271=CARTESIAN_POINT('Ctrl Pts',(82.8795678067457,-4.36742592605661,-0.75188043808983));
#14272=CARTESIAN_POINT('Ctrl Pts',(82.8778392658581,-4.37439023507361,-0.712525113610447));
#14273=CARTESIAN_POINT('Ctrl Pts',(82.8761387395344,-4.38079153195561,-0.67307674815633));
#14274=CARTESIAN_POINT('Ctrl Pts',(82.874479392903,-4.38660146132129,-0.633550254867047));
#14275=CARTESIAN_POINT('Ctrl Pts',(82.8692639398317,-4.40486251261772,-0.509315470570285));
#14276=CARTESIAN_POINT('Ctrl Pts',(82.8641471892087,-4.41780787734669,-0.384390475029427));
#14277=CARTESIAN_POINT('Ctrl Pts',(82.8590372507684,-4.4254380234901,-0.25927381989085));
#14278=CARTESIAN_POINT('Ctrl Pts',(82.8554668444273,-4.43076934450161,-0.171852551688031));
#14279=CARTESIAN_POINT('Ctrl Pts',(82.8518993357656,-4.43350664674304,-0.0843371748317401));
#14280=CARTESIAN_POINT('Ctrl Pts',(82.8483099710866,-4.43364346784954,0.00310368774768347));
#14281=CARTESIAN_POINT('Ctrl Pts',(90.1028989154209,-1.84736391785682,1.20202435615052));
#14282=CARTESIAN_POINT('Ctrl Pts',(90.140690073821,-2.22792678283258,0.617153363646938));
#14283=CARTESIAN_POINT('Ctrl Pts',(90.2162692554159,-2.38778162526882,-0.933200414266254));
#14284=CARTESIAN_POINT('Ctrl Pts',(90.3296364602056,-0.62872205324772,-2.48534112021196));
#14285=CARTESIAN_POINT('Ctrl Pts',(90.4052125065953,0.88959187531312,-2.13379067845246));
#14286=CARTESIAN_POINT('Ctrl Pts',(90.4430005297901,1.42252785196827,-1.68345790276281));
#14287=CARTESIAN_POINT('Ctrl Pts',(90.1853507684723,-1.72766177787012,1.12413775981909));
#14288=CARTESIAN_POINT('Ctrl Pts',(90.2231419268724,-2.08356561984736,0.577164178184089));
#14289=CARTESIAN_POINT('Ctrl Pts',(90.2987211084673,-2.23306247783782,-0.872732584650031));
#14290=CARTESIAN_POINT('Ctrl Pts',(90.4120883132569,-0.587983260796952,
-2.32430048939166));
#14291=CARTESIAN_POINT('Ctrl Pts',(90.4876643596466,0.831949712791466,-1.99552917619753));
#14292=CARTESIAN_POINT('Ctrl Pts',(90.5254523828415,1.33035346963605,-1.5743762477676));
#14293=CARTESIAN_POINT('Ctrl Pts',(90.2678026215237,-1.60795963788343,1.04625116348766));
#14294=CARTESIAN_POINT('Ctrl Pts',(90.3055937799238,-1.93920445686214,0.537174992721241));
#14295=CARTESIAN_POINT('Ctrl Pts',(90.3811729615186,-2.07834333040681,-0.812264755033806));
#14296=CARTESIAN_POINT('Ctrl Pts',(90.4945401663084,-0.547244468346182,
-2.16325985857137));
#14297=CARTESIAN_POINT('Ctrl Pts',(90.5701162126981,0.774307550269809,-1.85726767394259));
#14298=CARTESIAN_POINT('Ctrl Pts',(90.6079042358929,1.23817908730384,-1.4652945927724));
#14299=CARTESIAN_POINT('Ctrl Pts',(90.3502544745751,-1.48825749789673,0.968364567156219));
#14300=CARTESIAN_POINT('Ctrl Pts',(90.3880456329751,-1.79484329387692,0.497185807258393));
#14301=CARTESIAN_POINT('Ctrl Pts',(90.4636248145701,-1.92362418297579,-0.751796925417581));
#14302=CARTESIAN_POINT('Ctrl Pts',(90.5769920193598,-0.506505675895414,
-2.00221922775108));
#14303=CARTESIAN_POINT('Ctrl Pts',(90.6525680657495,0.716665387748153,-1.71900617168766));
#14304=CARTESIAN_POINT('Ctrl Pts',(90.6903560889443,1.14600470497162,-1.35621293777719));
#14305=CARTESIAN_POINT('',(90.4430005297901,1.42252785196811,-1.68345790276294));
#14306=CARTESIAN_POINT('',(90.4431198242969,-1.73942095919881,-0.360857735792951));
#14307=CARTESIAN_POINT('Ctrl Pts',(90.4430005297901,1.4225278519681,-1.68345790276293));
#14308=CARTESIAN_POINT('Ctrl Pts',(90.4430005297901,1.35849356753145,-1.72802743598216));
#14309=CARTESIAN_POINT('Ctrl Pts',(90.4430005297901,1.29211327677423,-1.76879332847206));
#14310=CARTESIAN_POINT('Ctrl Pts',(90.4430005297901,1.2237535666043,-1.80575874571065));
#14311=CARTESIAN_POINT('Ctrl Pts',(90.4430005297901,1.15444662534627,-1.8432363768294));
#14312=CARTESIAN_POINT('Ctrl Pts',(90.4430005297901,1.08310399459898,-1.87680762783793));
#14313=CARTESIAN_POINT('Ctrl Pts',(90.4430005297901,1.01008882139701,-1.90642508440335));
#14314=CARTESIAN_POINT('Ctrl Pts',(90.4430005297901,0.937375387724121,-1.93592014507482));
#14315=CARTESIAN_POINT('Ctrl Pts',(90.4430005297901,0.863002156179472,-1.96149402884287));
#14316=CARTESIAN_POINT('Ctrl Pts',(90.4430005297901,0.787324930454048,-1.98304902265781));
#14317=CARTESIAN_POINT('Ctrl Pts',(90.4430005297901,0.744830143839778,-1.99515272828203));
#14318=CARTESIAN_POINT('Ctrl Pts',(90.4430005297901,0.701924229092549,-2.00598831162974));
#14319=CARTESIAN_POINT('Ctrl Pts',(90.4430005297901,0.658671653783688,-2.0155313726465));
#14320=CARTESIAN_POINT('Ctrl Pts',(90.4430005297901,0.646172907588059,-2.01828904191188));
#14321=CARTESIAN_POINT('Ctrl Pts',(90.4430005297901,0.633654218360874,-2.02093674442495));
#14322=CARTESIAN_POINT('Ctrl Pts',(90.4430005297901,0.6211203149044,-2.02347372260162));
#14323=CARTESIAN_POINT('Ctrl Pts',(90.4430005297901,0.54560059660241,-2.03875961321869));
#14324=CARTESIAN_POINT('Ctrl Pts',(90.4430005297901,0.469491648693074,-2.05003826325601));
#14325=CARTESIAN_POINT('Ctrl Pts',(90.4430005297901,0.393135312105228,-2.05726598238489));
#14326=CARTESIAN_POINT('Ctrl Pts',(90.4430005297901,0.317994445888144,-2.06437864782154));
#14327=CARTESIAN_POINT('Ctrl Pts',(90.4430005297901,0.242613051580121,-2.06756819235657));
#14328=CARTESIAN_POINT('Ctrl Pts',(90.4430005297901,0.167322657815908,-2.06674371029539));
#14329=CARTESIAN_POINT('Ctrl Pts',(90.4430005297901,0.11103882258771,-2.06612736324021));
#14330=CARTESIAN_POINT('Ctrl Pts',(90.4430005297901,0.0548058830603974,
-2.06326681098423));
#14331=CARTESIAN_POINT('Ctrl Pts',(90.4430005297901,-0.0012308310801181,
-2.05810621712317));
#14332=CARTESIAN_POINT('Ctrl Pts',(90.4430005297901,-0.0254665698698789,
-2.0558742731783));
#14333=CARTESIAN_POINT('Ctrl Pts',(90.4430005297901,-0.0496655066289054,
-2.05321190325344));
#14334=CARTESIAN_POINT('Ctrl Pts',(90.4430005297901,-0.0738153724767166,
-2.05011370335278));
#14335=CARTESIAN_POINT('Ctrl Pts',(90.4430005297901,-0.0915898373131206,
-2.04783340724109));
#14336=CARTESIAN_POINT('Ctrl Pts',(90.4430005297901,-0.109337713577792,
-2.04531700834963));
#14337=CARTESIAN_POINT('Ctrl Pts',(90.4430005297901,-0.127053980826188,
-2.04256216657338));
#14338=CARTESIAN_POINT('Ctrl Pts',(90.4430005297901,-0.141731501026049,
-2.04027984348288));
#14339=CARTESIAN_POINT('Ctrl Pts',(90.4430005297901,-0.15638983983332,-2.03783328837979));
#14340=CARTESIAN_POINT('Ctrl Pts',(90.4430005297901,-0.171003090990926,
-2.03522554868848));
#14341=CARTESIAN_POINT('Ctrl Pts',(90.4430005297901,-0.24257684235259,-2.02245318815976));
#14342=CARTESIAN_POINT('Ctrl Pts',(90.4430005297901,-0.313187615395152,
-2.00580133374315));
#14343=CARTESIAN_POINT('Ctrl Pts',(90.4430005297901,-0.382533842296712,
-1.9851947537543));
#14344=CARTESIAN_POINT('Ctrl Pts',(90.4430005297901,-0.420076293430716,
-1.97403882564059));
#14345=CARTESIAN_POINT('Ctrl Pts',(90.4430005297901,-0.457247853160685,
-1.96172298204888));
#14346=CARTESIAN_POINT('Ctrl Pts',(90.4430005297901,-0.493997977180851,
-1.94822944989876));
#14347=CARTESIAN_POINT('Ctrl Pts',(90.4430005297901,-0.563441751326172,
-1.92273179991692));
#14348=CARTESIAN_POINT('Ctrl Pts',(90.4430005297901,-0.631383008819566,
-1.8930310143353));
#14349=CARTESIAN_POINT('Ctrl Pts',(90.4430005297901,-0.697549630883036,
-1.85938942474586));
#14350=CARTESIAN_POINT('Ctrl Pts',(90.4430005297901,-0.728482655927117,
-1.84366191590772));
#14351=CARTESIAN_POINT('Ctrl Pts',(90.4430005297901,-0.759027301901942,
-1.82707257186965));
#14352=CARTESIAN_POINT('Ctrl Pts',(90.4430005297901,-0.78915271119639,-1.80964576389469));
#14353=CARTESIAN_POINT('Ctrl Pts',(90.4430005297901,-0.805665241648411,
-1.80009367135529));
#14354=CARTESIAN_POINT('Ctrl Pts',(90.4430005297901,-0.822051778690114,
-1.79028994553458));
#14355=CARTESIAN_POINT('Ctrl Pts',(90.4430005297901,-0.838306956091599,
-1.78023844910885));
#14356=CARTESIAN_POINT('Ctrl Pts',(90.4430005297901,-0.848486765356274,
-1.77394369674095));
#14357=CARTESIAN_POINT('Ctrl Pts',(90.4430005297901,-0.858617377556742,
-1.76755026518769));
#14358=CARTESIAN_POINT('Ctrl Pts',(90.4430005297901,-0.8686896401472,-1.76106412386972));
#14359=CARTESIAN_POINT('Ctrl Pts',(90.4430005297901,-0.929536413808207,
-1.72188119261045));
#14360=CARTESIAN_POINT('Ctrl Pts',(90.4430005297901,-0.988126176715454,
-1.67940471375811));
#14361=CARTESIAN_POINT('Ctrl Pts',(90.4430005297901,-1.04423185300513,-1.63391216703375));
#14362=CARTESIAN_POINT('Ctrl Pts',(90.4430005297901,-1.10035200605041,-1.58840788202328));
#14363=CARTESIAN_POINT('Ctrl Pts',(90.4430005297901,-1.15398744655177,-1.53988505913721));
#14364=CARTESIAN_POINT('Ctrl Pts',(90.4430005297901,-1.20487106311036,-1.4885881496131));
#14365=CARTESIAN_POINT('Ctrl Pts',(90.4430005297901,-1.25462208740418,-1.43843303162944));
#14366=CARTESIAN_POINT('Ctrl Pts',(90.4430005297901,-1.30174284252823,-1.38562506083014));
#14367=CARTESIAN_POINT('Ctrl Pts',(90.4430005297901,-1.34593792591377,-1.33037435808501));
#14368=CARTESIAN_POINT('Ctrl Pts',(90.4430005297901,-1.36324169050299,-1.30874197094025));
#14369=CARTESIAN_POINT('Ctrl Pts',(90.4430005297901,-1.38009642305358,-1.28673498876761));
#14370=CARTESIAN_POINT('Ctrl Pts',(90.4430005297901,-1.39648221326538,-1.26436566883624));
#14371=CARTESIAN_POINT('Ctrl Pts',(90.4430005297901,-1.40413618854343,-1.25391672377295));
#14372=CARTESIAN_POINT('Ctrl Pts',(90.4430005297901,-1.41168748957158,-1.24338902200559));
#14373=CARTESIAN_POINT('Ctrl Pts',(90.4430005297901,-1.41912637484514,-1.23279517460321));
#14374=CARTESIAN_POINT('Ctrl Pts',(90.4430005297901,-1.45875449510071,-1.17636007130585));
#14375=CARTESIAN_POINT('Ctrl Pts',(90.4430005297901,-1.49525634166903,-1.11796797580369));
#14376=CARTESIAN_POINT('Ctrl Pts',(90.4430005297901,-1.52837656473234,-1.05783238657755));
#14377=CARTESIAN_POINT('Ctrl Pts',(90.4430005297901,-1.56117405481083,-0.998282775838562));
#14378=CARTESIAN_POINT('Ctrl Pts',(90.4430005297902,-1.59065591048659,-0.937022733178418));
#14379=CARTESIAN_POINT('Ctrl Pts',(90.4430005297902,-1.61652448547098,-0.874251203149225));
#14380=CARTESIAN_POINT('Ctrl Pts',(90.4430005297902,-1.62298306524412,-0.85857910159664));
#14381=CARTESIAN_POINT('Ctrl Pts',(90.4430005297902,-1.62921615191981,-0.842812771601475));
#14382=CARTESIAN_POINT('Ctrl Pts',(90.4430005297902,-1.63521857834343,-0.826955310014817));
#14383=CARTESIAN_POINT('Ctrl Pts',(90.4430005297902,-1.64047153672403,-0.813077824501798));
#14384=CARTESIAN_POINT('Ctrl Pts',(90.4430005297902,-1.64554478527697,-0.799138477894344));
#14385=CARTESIAN_POINT('Ctrl Pts',(90.4430005297902,-1.65043379611912,-0.785144399166612));
#14386=CARTESIAN_POINT('Ctrl Pts',(90.4430005297902,-1.66472446959869,-0.744239435728744));
#14387=CARTESIAN_POINT('Ctrl Pts',(90.4430005297902,-1.67744682205688,-0.702853420185191));
#14388=CARTESIAN_POINT('Ctrl Pts',(90.4430005297902,-1.68852852013358,-0.66104002889664));
#14389=CARTESIAN_POINT('Ctrl Pts',(90.4430005297902,-1.70605020045957,-0.594927338365569));
#14390=CARTESIAN_POINT('Ctrl Pts',(90.4430005297902,-1.71947262347401,-0.527745396084227));
#14391=CARTESIAN_POINT('Ctrl Pts',(90.4430005297902,-1.72885247363525,-0.459849352265223));
#14392=CARTESIAN_POINT('Ctrl Pts',(90.4430005297902,-1.73338742826583,-0.427023083932308));
#14393=CARTESIAN_POINT('Ctrl Pts',(90.4430005297902,-1.73697664884795,-0.394030018123096));
#14394=CARTESIAN_POINT('Ctrl Pts',(90.4430005297902,-1.73962237473191,-0.360911589357311));
#14395=CARTESIAN_POINT('',(90.3498698986824,-0.176530238082941,-2.19735656904503));
#14396=CARTESIAN_POINT('Ctrl Pts',(90.4430005297901,1.42252785196811,-1.68345790276294));
#14397=CARTESIAN_POINT('Ctrl Pts',(90.4119569860875,0.984711319553738,-2.05341441334118));
#14398=CARTESIAN_POINT('Ctrl Pts',(90.380913442385,0.394220067868452,-2.23807424546201));
#14399=CARTESIAN_POINT('Ctrl Pts',(90.3498698986824,-0.175612058744845,
-2.19751079506226));
#14400=CARTESIAN_POINT('',(90.3498698986825,-1.48890580190326,0.968619417293912));
#14401=CARTESIAN_POINT('Ctrl Pts',(90.3498698986825,-0.181591443149775,
-2.19650644155093));
#14402=CARTESIAN_POINT('Ctrl Pts',(90.3498698986824,-0.257547497917167,
-2.18363784310908));
#14403=CARTESIAN_POINT('Ctrl Pts',(90.3498698986824,-0.332599118530173,
-2.16671926797208));
#14404=CARTESIAN_POINT('Ctrl Pts',(90.3498698986824,-0.406428811432403,
-2.1456565302238));
#14405=CARTESIAN_POINT('Ctrl Pts',(90.3498698986824,-0.449282745765014,
-2.1334308098551));
#14406=CARTESIAN_POINT('Ctrl Pts',(90.3498698986825,-0.491724687026784,
-2.1198079884639));
#14407=CARTESIAN_POINT('Ctrl Pts',(90.3498698986825,-0.533688867832701,
-2.10476240272968));
#14408=CARTESIAN_POINT('Ctrl Pts',(90.3498698986825,-0.572294897306717,
-2.09092082843575));
#14409=CARTESIAN_POINT('Ctrl Pts',(90.3498698986825,-0.610496552067535,
-2.07587494667672));
#14410=CARTESIAN_POINT('Ctrl Pts',(90.3498698986825,-0.648253856041698,
-2.05966215463175));
#14411=CARTESIAN_POINT('Ctrl Pts',(90.3498698986825,-0.670857500514945,
-2.04995626600279));
#14412=CARTESIAN_POINT('Ctrl Pts',(90.3498698986824,-0.693301845759945,
-2.03983211447536));
#14413=CARTESIAN_POINT('Ctrl Pts',(90.3498698986824,-0.715577834954405,
-2.0292972875901));
#14414=CARTESIAN_POINT('Ctrl Pts',(90.3498698986824,-0.727802722918567,
-2.02351585731242));
#14415=CARTESIAN_POINT('Ctrl Pts',(90.3498698986825,-0.739974677490572,
-2.0176117265465));
#14416=CARTESIAN_POINT('Ctrl Pts',(90.3498698986825,-0.752084605070805,
-2.0115902131628));
#14417=CARTESIAN_POINT('Ctrl Pts',(90.3498698986825,-0.821813208973862,
-1.97691851765953));
#14418=CARTESIAN_POINT('Ctrl Pts',(90.3498698986824,-0.889562996776269,
-1.93832331974276));
#14419=CARTESIAN_POINT('Ctrl Pts',(90.3498698986824,-0.955077779488232,
-1.8960902045986));
#14420=CARTESIAN_POINT('Ctrl Pts',(90.3498698986824,-1.00782120600229,-1.86208995132968));
#14421=CARTESIAN_POINT('Ctrl Pts',(90.3498698986824,-1.05911566374211,-1.82573079164599));
#14422=CARTESIAN_POINT('Ctrl Pts',(90.3498698986824,-1.10880929161885,-1.78714529169388));
#14423=CARTESIAN_POINT('Ctrl Pts',(90.3498698986824,-1.13549274836521,-1.76642644778974));
#14424=CARTESIAN_POINT('Ctrl Pts',(90.3498698986825,-1.16171434281069,-1.74506547534867));
#14425=CARTESIAN_POINT('Ctrl Pts',(90.3498698986825,-1.18744825102446,-1.7230816457625));
#14426=CARTESIAN_POINT('Ctrl Pts',(90.3498698986825,-1.19640383196496,-1.71543111854349));
#14427=CARTESIAN_POINT('Ctrl Pts',(90.3498698986825,-1.20529911666184,-1.70770612424301));
#14428=CARTESIAN_POINT('Ctrl Pts',(90.3498698986825,-1.21412602362739,-1.69991389128877));
#14429=CARTESIAN_POINT('Ctrl Pts',(90.3498698986825,-1.27138360828138,-1.6493679367701));
#14430=CARTESIAN_POINT('Ctrl Pts',(90.3498698986825,-1.32585220395615,-1.59592345890963));
#14431=CARTESIAN_POINT('Ctrl Pts',(90.3498698986825,-1.37729079289597,-1.5398445336051));
#14432=CARTESIAN_POINT('Ctrl Pts',(90.3498698986825,-1.42791166625755,-1.4846570909749));
#14433=CARTESIAN_POINT('Ctrl Pts',(90.3498698986825,-1.47559858119474,-1.4269174071782));
#14434=CARTESIAN_POINT('Ctrl Pts',(90.3498698986825,-1.52007933169395,-1.36685182768371));
#14435=CARTESIAN_POINT('Ctrl Pts',(90.3498698986825,-1.55818476634747,-1.31539529899061));
#14436=CARTESIAN_POINT('Ctrl Pts',(90.3498698986825,-1.59393674881564,-1.26223114492883));
#14437=CARTESIAN_POINT('Ctrl Pts',(90.3498698986825,-1.62713471283201,-1.20749362086063));
#14438=CARTESIAN_POINT('Ctrl Pts',(90.3498698986825,-1.64205050302995,-1.18290014203906));
#14439=CARTESIAN_POINT('Ctrl Pts',(90.3498698986825,-1.65645032490888,-1.15798898503546));
#14440=CARTESIAN_POINT('Ctrl Pts',(90.3498698986825,-1.67031397481906,-1.13277214815257));
#14441=CARTESIAN_POINT('Ctrl Pts',(90.3498698986825,-1.6764049122983,-1.12169323474428));
#14442=CARTESIAN_POINT('Ctrl Pts',(90.3498698986825,-1.68239233832551,-1.11055531714204));
#14443=CARTESIAN_POINT('Ctrl Pts',(90.3498698986825,-1.68827445817782,-1.09935941317281));
#14444=CARTESIAN_POINT('Ctrl Pts',(90.3498698986825,-1.69384736498092,-1.08875205885776));
#14445=CARTESIAN_POINT('Ctrl Pts',(90.3498698986825,-1.69932144666418,-1.07810081173515));
#14446=CARTESIAN_POINT('Ctrl Pts',(90.3498698986825,-1.70469477757152,-1.06740844245853));
#14447=CARTESIAN_POINT('Ctrl Pts',(90.3498698986825,-1.73697093001942,-1.00318225822526));
#14448=CARTESIAN_POINT('Ctrl Pts',(90.3498698986825,-1.76562679488746,-0.937452617252542));
#14449=CARTESIAN_POINT('Ctrl Pts',(90.3498698986825,-1.79041933774232,-0.870427041046266));
#14450=CARTESIAN_POINT('Ctrl Pts',(90.3498698986825,-1.80872633921019,-0.82093484780188));
#14451=CARTESIAN_POINT('Ctrl Pts',(90.3498698986825,-1.82492598563845,-0.770735606083873));
#14452=CARTESIAN_POINT('Ctrl Pts',(90.3498698986825,-1.838902364658,-0.71990970704802));
#14453=CARTESIAN_POINT('Ctrl Pts',(90.3498698986825,-1.8582790431049,-0.649445311297513));
#14454=CARTESIAN_POINT('Ctrl Pts',(90.3498698986825,-1.87338410187543,-0.577775460654213));
#14455=CARTESIAN_POINT('Ctrl Pts',(90.3498698986825,-1.88426075715438,-0.505262831342515));
#14456=CARTESIAN_POINT('Ctrl Pts',(90.3498698986825,-1.8895594387421,-0.469937510832042));
#14457=CARTESIAN_POINT('Ctrl Pts',(90.3498698986825,-1.89385383550029,-0.434412328255347));
#14458=CARTESIAN_POINT('Ctrl Pts',(90.3498698986825,-1.8971447051508,-0.398730679953565));
#14459=CARTESIAN_POINT('Ctrl Pts',(90.3498698986825,-1.89872539720832,-0.381591837015542));
#14460=CARTESIAN_POINT('Ctrl Pts',(90.3498698986825,-1.90007477485771,-0.364410850502331));
#14461=CARTESIAN_POINT('Ctrl Pts',(90.3498698986825,-1.90119093547224,-0.347226454365849));
#14462=CARTESIAN_POINT('Ctrl Pts',(90.3498698986825,-1.90581143780897,-0.276089252899803));
#14463=CARTESIAN_POINT('Ctrl Pts',(90.3498698986825,-1.90645067533891,-0.204804122651826));
#14464=CARTESIAN_POINT('Ctrl Pts',(90.3498698986825,-1.9031984808422,-0.133704998421274));
#14465=CARTESIAN_POINT('Ctrl Pts',(90.3498698986825,-1.89994229664681,-0.0625186518298186));
#14466=CARTESIAN_POINT('Ctrl Pts',(90.3498698986825,-1.8927847725229,0.00848227913307016));
#14467=CARTESIAN_POINT('Ctrl Pts',(90.3498698986825,-1.88176579781181,0.0789493591992786));
#14468=CARTESIAN_POINT('Ctrl Pts',(90.3498698986825,-1.87096201859867,0.148040249667054));
#14469=CARTESIAN_POINT('Ctrl Pts',(90.3498698986825,-1.8564456742516,0.216618795460744));
#14470=CARTESIAN_POINT('Ctrl Pts',(90.3498698986825,-1.83821237884615,0.284329866854858));
#14471=CARTESIAN_POINT('Ctrl Pts',(90.3498698986825,-1.83384319970924,0.30055522787132));
#14472=CARTESIAN_POINT('Ctrl Pts',(90.3498698986825,-1.82926041502798,0.316730622856352));
#14473=CARTESIAN_POINT('Ctrl Pts',(90.3498698986825,-1.82446364132743,0.332850848989154));
#14474=CARTESIAN_POINT('Ctrl Pts',(90.3498698986825,-1.82014892639808,0.34735104947842));
#14475=CARTESIAN_POINT('Ctrl Pts',(90.3498698986825,-1.81565974396159,0.361810316796933));
#14476=CARTESIAN_POINT('Ctrl Pts',(90.3498698986825,-1.81100440526727,0.376199140206947));
#14477=CARTESIAN_POINT('Ctrl Pts',(90.3498698986825,-1.78981976209559,0.441677102094775));
#14478=CARTESIAN_POINT('Ctrl Pts',(90.3498698986825,-1.76516982840305,0.505799597646084));
#14479=CARTESIAN_POINT('Ctrl Pts',(90.3498698986825,-1.73709975902306,0.568253064609059));
#14480=CARTESIAN_POINT('Ctrl Pts',(90.3498698986825,-1.70983211150237,0.628921212611786));
#14481=CARTESIAN_POINT('Ctrl Pts',(90.3498698986825,-1.67933655602438,0.688015070073776));
#14482=CARTESIAN_POINT('Ctrl Pts',(90.3498698986825,-1.64561668449442,0.745217717416419));
#14483=CARTESIAN_POINT('Ctrl Pts',(90.3498698986825,-1.61228551809801,0.801760962404725));
#14484=CARTESIAN_POINT('Ctrl Pts',(90.3498698986825,-1.57580358704956,0.856457003828013));
#14485=CARTESIAN_POINT('Ctrl Pts',(90.3498698986825,-1.5361431033198,0.908960632930662));
#14486=CARTESIAN_POINT('Ctrl Pts',(90.3498698986825,-1.52086991362194,0.929179697644422));
#14487=CARTESIAN_POINT('Ctrl Pts',(90.3498698986825,-1.50512503817007,0.949073159039));
#14488=CARTESIAN_POINT('Ctrl Pts',(90.3498698986825,-1.48890580190333,0.968619417293832));
#14489=CARTESIAN_POINT('',(90.4430005297901,-1.73988535811011,-0.357579366202886));
#14490=CARTESIAN_POINT('Ctrl Pts',(90.3498698986825,-1.48890580190333,0.96861941729381));
#14491=CARTESIAN_POINT('Ctrl Pts',(90.3654557264859,-1.61537991701543,0.774210715156588));
#14492=CARTESIAN_POINT('Ctrl Pts',(90.379221234229,-1.70257359128787,0.556897371306134));
#14493=CARTESIAN_POINT('Ctrl Pts',(90.4021533800625,-1.76705540299077,0.214682455565629));
#14494=CARTESIAN_POINT('Ctrl Pts',(90.4100841123922,-1.77731049373243,0.0986496254663364));
#14495=CARTESIAN_POINT('Ctrl Pts',(90.4263924918293,-1.77503537078494,-0.131797860813206));
#14496=CARTESIAN_POINT('Ctrl Pts',(90.4347211409246,-1.76288391808981,-0.245674537377828));
#14497=CARTESIAN_POINT('Ctrl Pts',(90.4430005297901,-1.73988535811011,-0.357579366202886));
#14498=CARTESIAN_POINT('Ctrl Pts',(90.4431198242969,-1.73921714336317,-0.36081545245689));
#14499=CARTESIAN_POINT('Ctrl Pts',(90.4430800594613,-1.73944088489587,-0.359736964529839));
#14500=CARTESIAN_POINT('Ctrl Pts',(90.4430402946257,-1.73966362327333,-0.358658268489662));
#14501=CARTESIAN_POINT('Ctrl Pts',(90.4430005297901,-1.73988535811011,-0.357579366202887));
#14502=CARTESIAN_POINT('Origin',(88.3562164250559,0.,0.));
#14503=CARTESIAN_POINT('',(90.3498698986825,0.429156946220653,1.72362651929313));
#14504=CARTESIAN_POINT('Origin',(90.3498698986825,0.,0.));
#14505=CARTESIAN_POINT('',(90.4430005297901,-0.906280710947669,1.52765157528285));
#14506=CARTESIAN_POINT('Ctrl Pts',(90.3498698986825,0.429156946220653,1.72362651929313));
#14507=CARTESIAN_POINT('Ctrl Pts',(90.3581493387364,0.318297078944027,1.75122895031072));
#14508=CARTESIAN_POINT('Ctrl Pts',(90.3664780352276,0.205018872177277,1.7680748527967));
#14509=CARTESIAN_POINT('Ctrl Pts',(90.3827864379183,-0.0251386642564886,
1.7798686437189));
#14510=CARTESIAN_POINT('Ctrl Pts',(90.3907171496873,-0.141496109361598,
1.77441601847775));
#14511=CARTESIAN_POINT('Ctrl Pts',(90.4136492336215,-0.486082830458068,
1.72412731573226));
#14512=CARTESIAN_POINT('Ctrl Pts',(90.4274147017556,-0.706812911108985,
1.64598603215369));
#14513=CARTESIAN_POINT('Ctrl Pts',(90.4430005297901,-0.906280710947671,
1.52765157528285));
#14514=CARTESIAN_POINT('Origin',(90.4430005297901,0.,0.));
#14515=CARTESIAN_POINT('Ctrl Pts',(90.1025143645163,1.30770975493414,-1.2010560632029));
#14516=CARTESIAN_POINT('Ctrl Pts',(90.1403023877111,1.68793071858886,-0.787071505416501));
#14517=CARTESIAN_POINT('Ctrl Pts',(90.2158784341009,2.0214346950512,0.423355288987036));
#14518=CARTESIAN_POINT('Ctrl Pts',(90.3292456386917,0.830626863199002,1.8909219215733));
#14519=CARTESIAN_POINT('Ctrl Pts',(90.4048248200878,-0.422610284094226,
1.81385139676035));
#14520=CARTESIAN_POINT('Ctrl Pts',(90.442615978289,-0.906052876477412,1.52699333780199));
#14521=CARTESIAN_POINT('Ctrl Pts',(90.1849662092383,1.41289023394354,-1.29765827295793));
#14522=CARTESIAN_POINT('Ctrl Pts',(90.2227542324332,1.82369277193898,-0.850376499236438));
#14523=CARTESIAN_POINT('Ctrl Pts',(90.2983302788229,2.18402082604052,0.457406202745833));
#14524=CARTESIAN_POINT('Ctrl Pts',(90.4116974834138,0.897435060522396,2.04301077212292));
#14525=CARTESIAN_POINT('Ctrl Pts',(90.4872766648098,-0.45660127632136,1.95974138346671));
#14526=CARTESIAN_POINT('Ctrl Pts',(90.525067823011,-0.978927667841591,1.64981102736054));
#14527=CARTESIAN_POINT('Ctrl Pts',(90.2674180539604,1.51807071295294,-1.39426048271296));
#14528=CARTESIAN_POINT('Ctrl Pts',(90.3052060771553,1.95945482528912,-0.913681493056375));
#14529=CARTESIAN_POINT('Ctrl Pts',(90.3807821235449,2.34660695702982,0.491457116504633));
#14530=CARTESIAN_POINT('Ctrl Pts',(90.4941493281359,0.964243257845793,2.19509962267253));
#14531=CARTESIAN_POINT('Ctrl Pts',(90.5697285095319,-0.490592268548493,
2.10563137017308));
#14532=CARTESIAN_POINT('Ctrl Pts',(90.607519667733,-1.05180245920577,1.77262871691909));
#14533=CARTESIAN_POINT('Ctrl Pts',(90.3498698986825,1.62325119196233,-1.49086269246798));
#14534=CARTESIAN_POINT('Ctrl Pts',(90.3876579218773,2.09521687863925,-0.976986486876311));
#14535=CARTESIAN_POINT('Ctrl Pts',(90.463233968267,2.50919308801913,0.52550803026343));
#14536=CARTESIAN_POINT('Ctrl Pts',(90.5766011728579,1.03105145516918,2.34718847322216));
#14537=CARTESIAN_POINT('Ctrl Pts',(90.6521803542539,-0.524583260775627,
2.25152135687945));
#14538=CARTESIAN_POINT('Ctrl Pts',(90.6899715124551,-1.12467725056995,1.89544640647765));
#14539=CARTESIAN_POINT('',(90.4430005297901,2.20288941995875,0.0846757462792571));
#14540=CARTESIAN_POINT('Ctrl Pts',(90.4430005297901,-0.906280710947677,
1.52765157528285));
#14541=CARTESIAN_POINT('Ctrl Pts',(90.4430005297901,-0.854277760616062,
1.56729260000298));
#14542=CARTESIAN_POINT('Ctrl Pts',(90.4430005297901,-0.800108744344487,
1.60369925011022));
#14543=CARTESIAN_POINT('Ctrl Pts',(90.4430005297901,-0.744125790040279,
1.63692383774151));
#14544=CARTESIAN_POINT('Ctrl Pts',(90.4430005297901,-0.686154010767151,
1.6713287469597));
#14545=CARTESIAN_POINT('Ctrl Pts',(90.4430005297901,-0.626236599116127,
1.70232196503617));
#14546=CARTESIAN_POINT('Ctrl Pts',(90.4430005297901,-0.564718925219456,
1.72992757472046));
#14547=CARTESIAN_POINT('Ctrl Pts',(90.4430005297901,-0.512092172801297,
1.75354344791891));
#14548=CARTESIAN_POINT('Ctrl Pts',(90.4430005297901,-0.458293231174634,
1.77467969048475));
#14549=CARTESIAN_POINT('Ctrl Pts',(90.4430005297901,-0.403518249784151,
1.79332882529259));
#14550=CARTESIAN_POINT('Ctrl Pts',(90.4430005297901,-0.378653325916343,
1.80179453911715));
#14551=CARTESIAN_POINT('Ctrl Pts',(90.4430005297901,-0.353587059186378,
1.80974744290714));
#14552=CARTESIAN_POINT('Ctrl Pts',(90.4430005297901,-0.328336895404217,
1.81718529672686));
#14553=CARTESIAN_POINT('Ctrl Pts',(90.4430005297901,-0.315371182046073,
1.82100456227533));
#14554=CARTESIAN_POINT('Ctrl Pts',(90.4430005297901,-0.302356972411375,
1.82468800737921));
#14555=CARTESIAN_POINT('Ctrl Pts',(90.4430005297901,-0.289296585325211,
1.82823522504611));
#14556=CARTESIAN_POINT('Ctrl Pts',(90.4430005297901,-0.277975229628828,
1.83131011958596));
#14557=CARTESIAN_POINT('Ctrl Pts',(90.4430005297901,-0.266619082046204,
1.83428258023668));
#14558=CARTESIAN_POINT('Ctrl Pts',(90.4430005297901,-0.255244023393878,
1.83714894810172));
#14559=CARTESIAN_POINT('Ctrl Pts',(90.4430005297901,-0.186918851849708,
1.85436600887245));
#14560=CARTESIAN_POINT('Ctrl Pts',(90.4430005297901,-0.117787865443795,
1.8677937815248));
#14561=CARTESIAN_POINT('Ctrl Pts',(90.4430005297901,-0.0482176105662551,
1.87746078885698));
#14562=CARTESIAN_POINT('Ctrl Pts',(90.4430005297901,0.0225458393465897,
1.88729359441967));
#14563=CARTESIAN_POINT('Ctrl Pts',(90.4430005297901,0.0937646734743491,
1.89323595416038));
#14564=CARTESIAN_POINT('Ctrl Pts',(90.4430005297901,0.165083212114906,1.89527294746021));
#14565=CARTESIAN_POINT('Ctrl Pts',(90.4430005297901,0.235975923373851,1.89729777831897));
#14566=CARTESIAN_POINT('Ctrl Pts',(90.4430005297901,0.306968202656807,1.89546400374334));
#14567=CARTESIAN_POINT('Ctrl Pts',(90.4430005297901,0.377725173679162,1.88970801775622));
#14568=CARTESIAN_POINT('Ctrl Pts',(90.4430005297901,0.38708606610097,1.88894652154138));
#14569=CARTESIAN_POINT('Ctrl Pts',(90.4430005297901,0.396442847540757,1.88811630351685));
#14570=CARTESIAN_POINT('Ctrl Pts',(90.4430005297901,0.405794746349182,1.88721714781831));
#14571=CARTESIAN_POINT('Ctrl Pts',(90.4430005297901,0.41906845278398,1.88594092263387));
#14572=CARTESIAN_POINT('Ctrl Pts',(90.4430005297901,0.432332323108797,1.88452581977721));
#14573=CARTESIAN_POINT('Ctrl Pts',(90.4430005297901,0.4455841469567,1.88297116443225));
#14574=CARTESIAN_POINT('Ctrl Pts',(90.4430005297901,0.458728559964043,1.88142911013294));
#14575=CARTESIAN_POINT('Ctrl Pts',(90.4430005297901,0.471853391141752,1.87975060439521));
#14576=CARTESIAN_POINT('Ctrl Pts',(90.4430005297901,0.484948310227801,1.8779367216178));
#14577=CARTESIAN_POINT('Ctrl Pts',(90.4430005297901,0.557788263474281,1.86784707266058));
#14578=CARTESIAN_POINT('Ctrl Pts',(90.4430005297901,0.629779464650553,1.85356363281223));
#14579=CARTESIAN_POINT('Ctrl Pts',(90.4430005297901,0.700551912386958,1.83508091077558));
#14580=CARTESIAN_POINT('Ctrl Pts',(90.4430005297901,0.732380673074804,1.82676860626471));
#14581=CARTESIAN_POINT('Ctrl Pts',(90.4430005297901,0.763963163282864,1.81760628974152));
#14582=CARTESIAN_POINT('Ctrl Pts',(90.4430005297901,0.795266463078768,1.80759010215849));
#14583=CARTESIAN_POINT('Ctrl Pts',(90.4430005297901,0.863383166190852,1.78579464671587));
#14584=CARTESIAN_POINT('Ctrl Pts',(90.4430005297901,0.930178515592966,1.75995975736864));
#14585=CARTESIAN_POINT('Ctrl Pts',(90.4430005297901,0.995462794522614,1.73037590133247));
#14586=CARTESIAN_POINT('Ctrl Pts',(90.4430005297901,1.05348264614204,1.70408395224931));
#14587=CARTESIAN_POINT('Ctrl Pts',(90.4430005297901,1.11030929879789,1.67482990061158));
#14588=CARTESIAN_POINT('Ctrl Pts',(90.4430005297901,1.16580106122498,1.64278422184805));
#14589=CARTESIAN_POINT('Ctrl Pts',(90.4430005297901,1.1762422869831,1.63675456714062));
#14590=CARTESIAN_POINT('Ctrl Pts',(90.4430005297901,1.18662850495694,1.63063043366675));
#14591=CARTESIAN_POINT('Ctrl Pts',(90.4430005297901,1.19695660054926,1.62441474165913));
#14592=CARTESIAN_POINT('Ctrl Pts',(90.4430005297901,1.25999165646837,1.58647875532222));
#14593=CARTESIAN_POINT('Ctrl Pts',(90.4430005297901,1.32088999310675,1.54512054405464));
#14594=CARTESIAN_POINT('Ctrl Pts',(90.4430005297901,1.37946364276531,1.50067032140515));
#14595=CARTESIAN_POINT('Ctrl Pts',(90.4430005297901,1.43980234042177,1.45488064360901));
#14596=CARTESIAN_POINT('Ctrl Pts',(90.4430005297901,1.4976749624294,1.40580945467811));
#14597=CARTESIAN_POINT('Ctrl Pts',(90.4430005297901,1.55286316603457,1.35376300243271));
#14598=CARTESIAN_POINT('Ctrl Pts',(90.4430005297901,1.60805136963973,1.30171655018731));
#14599=CARTESIAN_POINT('Ctrl Pts',(90.4430005297901,1.66055597517919,1.2466941849305));
#14600=CARTESIAN_POINT('Ctrl Pts',(90.4430005297901,1.71013357145278,1.18895618401778));
#14601=CARTESIAN_POINT('Ctrl Pts',(90.4430005297901,1.72296507476095,1.17401263278891));
#14602=CARTESIAN_POINT('Ctrl Pts',(90.4430005297901,1.73560034241773,1.15888696127208));
#14603=CARTESIAN_POINT('Ctrl Pts',(90.4430005297901,1.74803477487696,1.14358326375263));
#14604=CARTESIAN_POINT('Ctrl Pts',(90.4430005297901,1.76083174777711,1.12783336900912));
#14605=CARTESIAN_POINT('Ctrl Pts',(90.4430005297901,1.77341879728594,1.11189092493475));
#14606=CARTESIAN_POINT('Ctrl Pts',(90.4430005297901,1.78576841317893,1.09579034652113));
#14607=CARTESIAN_POINT('Ctrl Pts',(90.4430005297901,1.83344349969788,1.03363485314175));
#14608=CARTESIAN_POINT('Ctrl Pts',(90.4430005297901,1.87765235974256,0.96904318706518));
#14609=CARTESIAN_POINT('Ctrl Pts',(90.4430005297901,1.91815905620923,0.902327591860497));
#14610=CARTESIAN_POINT('Ctrl Pts',(90.4430005297901,1.95747515213314,0.837572947086005));
#14611=CARTESIAN_POINT('Ctrl Pts',(90.4430005297901,1.99330413338327,0.770816566121482));
#14612=CARTESIAN_POINT('Ctrl Pts',(90.4430005297901,2.02539955299598,0.702308430193654));
#14613=CARTESIAN_POINT('Ctrl Pts',(90.4430005297901,2.03357309269832,0.684861891849646));
#14614=CARTESIAN_POINT('Ctrl Pts',(90.4430005297901,2.04150431230281,0.667301596050367));
#14615=CARTESIAN_POINT('Ctrl Pts',(90.4430005297901,2.04918873720806,0.649631385046051));
#14616=CARTESIAN_POINT('Ctrl Pts',(90.4430005297901,2.05671130248248,0.632333367649584));
#14617=CARTESIAN_POINT('Ctrl Pts',(90.4430005297901,2.06399514527129,0.614934728437702));
#14618=CARTESIAN_POINT('Ctrl Pts',(90.4430005297901,2.07103059613546,0.597454518134323));
#14619=CARTESIAN_POINT('Ctrl Pts',(90.4430005297901,2.09104535379643,0.547726052988361));
#14620=CARTESIAN_POINT('Ctrl Pts',(90.4430005297901,2.10906573010327,0.497303151678278));
#14621=CARTESIAN_POINT('Ctrl Pts',(90.4430005297901,2.12501355371715,0.446278571766078));
#14622=CARTESIAN_POINT('Ctrl Pts',(90.4430005297901,2.14793295022753,0.372948654963803));
#14623=CARTESIAN_POINT('Ctrl Pts',(90.4430005297901,2.16657429828593,0.298376904723251));
#14624=CARTESIAN_POINT('Ctrl Pts',(90.4430005297901,2.18107268216625,0.222889057559564));
#14625=CARTESIAN_POINT('Ctrl Pts',(90.4430005297901,2.18985901387143,0.177141802529971));
#14626=CARTESIAN_POINT('Ctrl Pts',(90.4430005297901,2.19712286143422,0.131057562795162));
#14627=CARTESIAN_POINT('Ctrl Pts',(90.4430005297901,2.2028857444688,0.0847053108012291));
#14628=CARTESIAN_POINT('',(90.3497506833166,0.432411172325593,1.72302747110366));
#14629=CARTESIAN_POINT('Ctrl Pts',(90.3498698986825,0.429156946220652,1.72362651929313));
#14630=CARTESIAN_POINT('Ctrl Pts',(90.3498301602272,0.430225058085747,1.72336057558601));
#14631=CARTESIAN_POINT('Ctrl Pts',(90.3497904217719,0.431292922747308,1.72309363903332));
#14632=CARTESIAN_POINT('Ctrl Pts',(90.3497506833166,0.432360538359997,1.72282571009637));
#14633=CARTESIAN_POINT('',(90.3498698986825,1.62325119196235,-1.49086269246796));
#14634=CARTESIAN_POINT('Ctrl Pts',(90.3498698986825,0.432473260079399,1.72322635770742));
#14635=CARTESIAN_POINT('Ctrl Pts',(90.3498698986825,0.500689037073848,1.71492876273114));
#14636=CARTESIAN_POINT('Ctrl Pts',(90.3498698986825,0.568201159921544,1.7026236132268));
#14637=CARTESIAN_POINT('Ctrl Pts',(90.3498698986825,0.63464679981471,1.68629351059737));
#14638=CARTESIAN_POINT('Ctrl Pts',(90.3498698986825,0.66677182170839,1.67839826110711));
#14639=CARTESIAN_POINT('Ctrl Pts',(90.3498698986825,0.698647807968663,1.66956143909895));
#14640=CARTESIAN_POINT('Ctrl Pts',(90.3498698986825,0.730234584403305,1.65977677709578));
#14641=CARTESIAN_POINT('Ctrl Pts',(90.3498698986825,0.781946426308745,1.64375795682607));
#14642=CARTESIAN_POINT('Ctrl Pts',(90.3498698986825,0.832883402990908,1.62519998965726));
#14643=CARTESIAN_POINT('Ctrl Pts',(90.3498698986825,0.88294589212397,1.60424660726948));
#14644=CARTESIAN_POINT('Ctrl Pts',(90.3498698986825,0.894457590187191,1.5994284486915));
#14645=CARTESIAN_POINT('Ctrl Pts',(90.3498698986825,0.905920948354246,1.59448434130905));
#14646=CARTESIAN_POINT('Ctrl Pts',(90.3498698986825,0.917326683635254,1.58941980305414));
#14647=CARTESIAN_POINT('Ctrl Pts',(90.3498698986825,0.979664976023323,1.56173945989633));
#14648=CARTESIAN_POINT('Ctrl Pts',(90.3498698986825,1.0403517211105,1.53043727360066));
#14649=CARTESIAN_POINT('Ctrl Pts',(90.3498698986825,1.09919843952219,1.49582959807598));
#14650=CARTESIAN_POINT('Ctrl Pts',(90.3498698986825,1.15010544628058,1.46589125623842));
#14651=CARTESIAN_POINT('Ctrl Pts',(90.3498698986825,1.19963574840112,1.43347809869087));
#14652=CARTESIAN_POINT('Ctrl Pts',(90.3498698986825,1.24766201189904,1.39876400501927));
#14653=CARTESIAN_POINT('Ctrl Pts',(90.3498698986825,1.26296034952528,1.38770614028658));
#14654=CARTESIAN_POINT('Ctrl Pts',(90.3498698986825,1.27810601388692,1.37641460218754));
#14655=CARTESIAN_POINT('Ctrl Pts',(90.3498698986825,1.29309468960961,1.36489446808101));
#14656=CARTESIAN_POINT('Ctrl Pts',(90.3498698986825,1.30640467453454,1.35466455757203));
#14657=CARTESIAN_POINT('Ctrl Pts',(90.3498698986825,1.31959368966207,1.34425192002828));
#14658=CARTESIAN_POINT('Ctrl Pts',(90.3498698986825,1.33263794396078,1.33367724437743));
#14659=CARTESIAN_POINT('Ctrl Pts',(90.3498698986825,1.38778035157091,1.28897456826191));
#14660=CARTESIAN_POINT('Ctrl Pts',(90.3498698986825,1.44040951217242,1.24132658210685));
#14661=CARTESIAN_POINT('Ctrl Pts',(90.3498698986825,1.49033018861726,1.19105566689337));
#14662=CARTESIAN_POINT('Ctrl Pts',(90.3498698986825,1.54132495686097,1.13970312415401));
#14663=CARTESIAN_POINT('Ctrl Pts',(90.3498698986825,1.58949432651507,1.08561309730986));
#14664=CARTESIAN_POINT('Ctrl Pts',(90.3498698986825,1.63461237105893,1.02907775276922));
#14665=CARTESIAN_POINT('Ctrl Pts',(90.3498698986825,1.67109719589425,0.983360298402049));
#14666=CARTESIAN_POINT('Ctrl Pts',(90.3498698986825,1.70558655725381,0.936042670410925));
#14667=CARTESIAN_POINT('Ctrl Pts',(90.3498698986825,1.73794656373637,0.887259053299169));
#14668=CARTESIAN_POINT('Ctrl Pts',(90.3498698986825,1.75291021222756,0.864700933634309));
#14669=CARTESIAN_POINT('Ctrl Pts',(90.3498698986825,1.76741833878176,0.841829120502184));
#14670=CARTESIAN_POINT('Ctrl Pts',(90.3498698986825,1.78145646826647,0.818655805601394));
#14671=CARTESIAN_POINT('Ctrl Pts',(90.3498698986825,1.7878902939984,0.808035226138498));
#14672=CARTESIAN_POINT('Ctrl Pts',(90.3498698986825,1.79422637477591,0.797349598647965));
#14673=CARTESIAN_POINT('Ctrl Pts',(90.3498698986825,1.8004601115605,0.786605484523137));
#14674=CARTESIAN_POINT('Ctrl Pts',(90.3498698986825,1.83793113462181,0.722022560659537));
#14675=CARTESIAN_POINT('Ctrl Pts',(90.3498698986825,1.87157440109755,0.655560357407762));
#14676=CARTESIAN_POINT('Ctrl Pts',(90.3498698986825,1.9011666568507,0.587535602339381));
#14677=CARTESIAN_POINT('Ctrl Pts',(90.3498698986825,1.92600732300679,0.530433492750316));
#14678=CARTESIAN_POINT('Ctrl Pts',(90.3498698986825,1.94799336759623,0.47222923559375));
#14679=CARTESIAN_POINT('Ctrl Pts',(90.3498698986825,1.96697450572884,0.41308845846253));
#14680=CARTESIAN_POINT('Ctrl Pts',(90.3498698986825,1.98906817163189,0.344249774393362));
#14681=CARTESIAN_POINT('Ctrl Pts',(90.3498698986825,2.007092396991,0.274142320643778));
#14682=CARTESIAN_POINT('Ctrl Pts',(90.3498698986825,2.02116104200529,0.20307430952008));
#14683=CARTESIAN_POINT('Ctrl Pts',(90.3498698986825,2.02849211048846,0.166041286369528));
#14684=CARTESIAN_POINT('Ctrl Pts',(90.3498698986825,2.03474828995461,0.128747041232483));
#14685=CARTESIAN_POINT('Ctrl Pts',(90.3498698986825,2.03994046639292,0.0912332730845031));
#14686=CARTESIAN_POINT('Ctrl Pts',(90.3498698986825,2.04159548143424,0.0792756958951641));
#14687=CARTESIAN_POINT('Ctrl Pts',(90.3498698986825,2.04314268181887,0.0672931065835388));
#14688=CARTESIAN_POINT('Ctrl Pts',(90.3498698986825,2.04458127608794,0.0552958865448525));
#14689=CARTESIAN_POINT('Ctrl Pts',(90.3498698986825,2.05337295176474,-0.0180226785786454));
#14690=CARTESIAN_POINT('Ctrl Pts',(90.3498698986825,2.05809534086541,-0.0917277015695579));
#14691=CARTESIAN_POINT('Ctrl Pts',(90.3498698986825,2.05891131036709,-0.165484762976481));
#14692=CARTESIAN_POINT('Ctrl Pts',(90.3498698986825,2.05975504538853,-0.241751603415596));
#14693=CARTESIAN_POINT('Ctrl Pts',(90.3498698986825,2.05642222258581,-0.31807488200744));
#14694=CARTESIAN_POINT('Ctrl Pts',(90.3498698986825,2.04904110315226,-0.394108580280238));
#14695=CARTESIAN_POINT('Ctrl Pts',(90.3498698986825,2.04165998371871,-0.47014227855304));
#14696=CARTESIAN_POINT('Ctrl Pts',(90.3498698986825,2.03023052285033,-0.545887393002507));
#14697=CARTESIAN_POINT('Ctrl Pts',(90.3498698986825,2.01482901135003,-0.621007387284477));
#14698=CARTESIAN_POINT('Ctrl Pts',(90.3498698986825,2.0082558082846,-0.653067810489036));
#14699=CARTESIAN_POINT('Ctrl Pts',(90.3498698986825,2.00095845789534,-0.685014398435953));
#14700=CARTESIAN_POINT('Ctrl Pts',(90.3498698986825,1.99294003791299,-0.716820819516162));
#14701=CARTESIAN_POINT('Ctrl Pts',(90.3498698986825,1.98892248395689,-0.732757127806477));
#14702=CARTESIAN_POINT('Ctrl Pts',(90.3498698986825,1.98472264433957,-0.748662300766758));
#14703=CARTESIAN_POINT('Ctrl Pts',(90.3498698986825,1.98034860459119,-0.764505835419566));
#14704=CARTESIAN_POINT('Ctrl Pts',(90.3498698986825,1.95934426572443,-0.840587213239224));
#14705=CARTESIAN_POINT('Ctrl Pts',(90.3498698986825,1.93430052129815,-0.91536072687171));
#14706=CARTESIAN_POINT('Ctrl Pts',(90.3498698986825,1.90535385031768,-0.988470818953257));
#14707=CARTESIAN_POINT('Ctrl Pts',(90.3498698986825,1.87638204882009,-1.06164438273494));
#14708=CARTESIAN_POINT('Ctrl Pts',(90.3498698986825,1.8435004604687,-1.13315267365607));
#14709=CARTESIAN_POINT('Ctrl Pts',(90.3498698986825,1.80679432959692,-1.20264141611964));
#14710=CARTESIAN_POINT('Ctrl Pts',(90.3498698986825,1.7704793662928,-1.27138963535931));
#14711=CARTESIAN_POINT('Ctrl Pts',(90.3498698986825,1.73042077500635,-1.33816212418963));
#14712=CARTESIAN_POINT('Ctrl Pts',(90.3498698986825,1.68665261190661,-1.4026027958059));
#14713=CARTESIAN_POINT('Ctrl Pts',(90.3498698986825,1.66632005262628,-1.43253879683743));
#14714=CARTESIAN_POINT('Ctrl Pts',(90.3498698986825,1.64518626524376,-1.46197129625266));
#14715=CARTESIAN_POINT('Ctrl Pts',(90.3498698986825,1.62325119196239,-1.49086269246791));
#14716=CARTESIAN_POINT('Ctrl Pts',(90.3498698986825,1.62325119196235,-1.49086269246796));
#14717=CARTESIAN_POINT('Ctrl Pts',(90.380913442385,2.01097952971941,-1.06870410630073));
#14718=CARTESIAN_POINT('Ctrl Pts',(90.4119569860876,2.21987663538069,-0.486345711720857));
#14719=CARTESIAN_POINT('Ctrl Pts',(90.4430005297901,2.20288941995875,0.0846757462792571));
#14720=CARTESIAN_POINT('Origin',(90.3498698986825,-2.40291074888303E-16,
0.));
#14721=CARTESIAN_POINT('',(90.3498698986825,-2.69912154532077E-16,2.204));
#14722=CARTESIAN_POINT('Origin',(90.3498698986825,0.,0.));
#14723=CARTESIAN_POINT('Origin',(90.3498698986825,0.,0.));
#14724=CARTESIAN_POINT('Origin',(66.9212607628943,0.,0.));
#14725=CARTESIAN_POINT('',(81.4430005297901,-2.69912154532077E-16,2.204));
#14726=CARTESIAN_POINT('Origin',(81.4430005297901,0.,0.));
#14727=CARTESIAN_POINT('',(66.9212607628943,-2.69912154532077E-16,2.204));
#14728=CARTESIAN_POINT('Origin',(90.4430005297901,0.,0.));
#14729=CARTESIAN_POINT('Ctrl Pts',(82.0295201802136,-1.65306427348725,3.32899555241991));
#14730=CARTESIAN_POINT('Ctrl Pts',(82.0621173237355,-2.19852390520666,3.05813912872495));
#14731=CARTESIAN_POINT('Ctrl Pts',(82.1273116107797,-3.14747075323877,2.24346380767911));
#14732=CARTESIAN_POINT('Ctrl Pts',(82.257700184868,-4.08359169347408,-0.09571649437622));
#14733=CARTESIAN_POINT('Ctrl Pts',(82.4206859024783,-2.86883663152734,-3.29923455674864));
#14734=CARTESIAN_POINT('Ctrl Pts',(82.6162687636106,1.16238339903618,-4.2168753806827));
#14735=CARTESIAN_POINT('Ctrl Pts',(82.811851624743,4.15031934985653,-1.37057296918483));
#14736=CARTESIAN_POINT('Ctrl Pts',(83.0074344858754,3.44345504116371,2.69406016453184));
#14737=CARTESIAN_POINT('Ctrl Pts',(83.2030173470079,-0.333719683741995,
4.35943641705783));
#14738=CARTESIAN_POINT('Ctrl Pts',(83.39860020814,-3.81263960805445,2.13930714802621));
#14739=CARTESIAN_POINT('Ctrl Pts',(83.5941830692725,-3.8944646466128,-1.98684861864105));
#14740=CARTESIAN_POINT('Ctrl Pts',(83.7897659304049,-0.50564373165627,-4.3426562533637));
#14741=CARTESIAN_POINT('Ctrl Pts',(83.9853487915373,3.3336643879048,-2.8285491238196));
#14742=CARTESIAN_POINT('Ctrl Pts',(84.1809316526696,4.20232603899528,1.20609443396036));
#14743=CARTESIAN_POINT('Ctrl Pts',(84.3765145138021,1.32618441591987,4.16598292634243));
#14744=CARTESIAN_POINT('Ctrl Pts',(84.5720973749343,-2.73173526363988,3.41346879580696));
#14745=CARTESIAN_POINT('Ctrl Pts',(84.7676802360668,-4.35535562891122,-0.380852351780076));
#14746=CARTESIAN_POINT('Ctrl Pts',(84.963263097199,-2.09782657360965,-3.83579056771449));
#14747=CARTESIAN_POINT('Ctrl Pts',(85.1588459583315,2.02911726294498,-3.87257613345951));
#14748=CARTESIAN_POINT('Ctrl Pts',(85.3544288194639,4.34787387083917,-0.458430425156126));
#14749=CARTESIAN_POINT('Ctrl Pts',(85.5500116805963,2.7921507497253,3.36423229852469));
#14750=CARTESIAN_POINT('Ctrl Pts',(85.7455945417287,-1.25171488096045,4.18895863102669));
#14751=CARTESIAN_POINT('Ctrl Pts',(85.9411774028608,-4.18015184799219,1.28081826434192));
#14752=CARTESIAN_POINT('Ctrl Pts',(86.1367602639934,-3.38356990681389,-2.76868550442667));
#14753=CARTESIAN_POINT('Ctrl Pts',(86.3323431251257,0.428180394291547,-4.35095693918743));
#14754=CARTESIAN_POINT('Ctrl Pts',(86.5279259862581,3.85837041772825,-2.05600160947017));
#14755=CARTESIAN_POINT('Ctrl Pts',(86.7235088473905,3.85028754068497,2.07109884112684));
#14756=CARTESIAN_POINT('Ctrl Pts',(86.9190917085228,0.4111347439794,4.3526007156551));
#14757=CARTESIAN_POINT('Ctrl Pts',(87.1146745696552,-3.39438885318226,2.7554110337347));
#14758=CARTESIAN_POINT('Ctrl Pts',(87.3102574307876,-4.17510263508425,-1.29718185414927));
#14759=CARTESIAN_POINT('Ctrl Pts',(87.50584029192,-1.23529790690718,-4.19382935913003));
#14760=CARTESIAN_POINT('Ctrl Pts',(87.7014231530522,2.80530789506251,-3.35326986418407));
#14761=CARTESIAN_POINT('Ctrl Pts',(87.8970060141848,4.34604268780248,0.475457386481673));
#14762=CARTESIAN_POINT('Ctrl Pts',(88.092588875317,2.01393751246173,3.88049411074219));
#14763=CARTESIAN_POINT('Ctrl Pts',(88.2881717364494,-2.11284414771308,3.82754458225146));
#14764=CARTESIAN_POINT('Ctrl Pts',(88.4837545975819,-4.35679539852597,0.36378874697873));
#14765=CARTESIAN_POINT('Ctrl Pts',(88.6793374587141,-2.71838192148609,-3.42414057059281));
#14766=CARTESIAN_POINT('Ctrl Pts',(88.8749203198466,1.34256965287038,-4.16076063290167));
#14767=CARTESIAN_POINT('Ctrl Pts',(89.0705031809788,4.20685975871864,-1.18961625113958));
#14768=CARTESIAN_POINT('Ctrl Pts',(89.2660860421113,3.322882630607,2.84156747674539));
#14769=CARTESIAN_POINT('Ctrl Pts',(89.4616689032436,-0.523309385250935,
4.34067852736659));
#14770=CARTESIAN_POINT('Ctrl Pts',(89.6572517643761,-3.9008702141681,1.97150514629555));
#14771=CARTESIAN_POINT('Ctrl Pts',(89.8528346255084,-3.80698675149828,-2.15407172965046));
#14772=CARTESIAN_POINT('Ctrl Pts',(90.0484174866407,-0.310961962579554,
-4.3610176492037));
#14773=CARTESIAN_POINT('Ctrl Pts',(90.211403204251,2.81536141761182,-2.95949706107794));
#14774=CARTESIAN_POINT('Ctrl Pts',(90.3418371019651,3.81133709361766,-0.644214494217));
#14775=CARTESIAN_POINT('Ctrl Pts',(90.4070767126353,3.71781142410833,0.603927146986502));
#14776=CARTESIAN_POINT('Ctrl Pts',(90.4397191797832,3.52383717212292,1.18211855844504));
#14777=CARTESIAN_POINT('Ctrl Pts',(82.1685848090598,-1.76019011105466,3.54472911011085));
#14778=CARTESIAN_POINT('Ctrl Pts',(82.2011819525819,-2.34099792665557,3.25631999852939));
#14779=CARTESIAN_POINT('Ctrl Pts',(82.2663762396261,-3.35144070532561,2.38885013252105));
#14780=CARTESIAN_POINT('Ctrl Pts',(82.3967648137143,-4.34822640094612,-0.101919344315883));
#14781=CARTESIAN_POINT('Ctrl Pts',(82.5597505313248,-3.05474986667829,-3.51303947098677));
#14782=CARTESIAN_POINT('Ctrl Pts',(82.7553333924568,1.23771095719187,-4.49014745746654));
#14783=CARTESIAN_POINT('Ctrl Pts',(82.9509162535894,4.41927830303003,-1.45939212741482));
#14784=CARTESIAN_POINT('Ctrl Pts',(83.1464991147216,3.66660607728902,2.86864711569356));
#14785=CARTESIAN_POINT('Ctrl Pts',(83.3420819758541,-0.355346187446032,
4.64194707619514));
#14786=CARTESIAN_POINT('Ctrl Pts',(83.5376648369865,-4.05971542833935,2.2779436630861));
#14787=CARTESIAN_POINT('Ctrl Pts',(83.7332476981189,-4.146843089385,-2.11560515025648));
#14788=CARTESIAN_POINT('Ctrl Pts',(83.9288305592512,-0.538411670043889,
-4.6240794840694));
#14789=CARTESIAN_POINT('Ctrl Pts',(84.1244134203835,3.54970050667567,-3.01185155122646));
#14790=CARTESIAN_POINT('Ctrl Pts',(84.319996281516,4.47465525442806,1.28425465948555));
#14791=CARTESIAN_POINT('Ctrl Pts',(84.5155791426482,1.41212700061114,4.435956948184));
#14792=CARTESIAN_POINT('Ctrl Pts',(84.7111620037808,-2.90876372697514,3.63467659130886));
#14793=CARTESIAN_POINT('Ctrl Pts',(84.9067448649131,-4.63760183502324,-0.405533259732842));
#14794=CARTESIAN_POINT('Ctrl Pts',(85.1023277260453,-2.23377496495383,-4.08436667203786));
#14795=CARTESIAN_POINT('Ctrl Pts',(85.2979105871779,2.16061298867192,-4.12353610428102));
#14796=CARTESIAN_POINT('Ctrl Pts',(85.4934934483101,4.62963522611218,-0.488138733567902));
#14797=CARTESIAN_POINT('Ctrl Pts',(85.6890763094425,2.97309440235643,3.58224935238705));
#14798=CARTESIAN_POINT('Ctrl Pts',(85.884659170575,-1.33283151215811,4.46042157961329));
#14799=CARTESIAN_POINT('Ctrl Pts',(86.0802420317073,-4.45104407829276,1.36382092282285));
#14800=CARTESIAN_POINT('Ctrl Pts',(86.2758248928396,-3.60284012276907,-2.94810850592725));
#14801=CARTESIAN_POINT('Ctrl Pts',(86.471407753972,0.455928367618472,-4.63291809085333));
#14802=CARTESIAN_POINT('Ctrl Pts',(86.6669906151044,4.10840979567241,-2.18923955912946));
#14803=CARTESIAN_POINT('Ctrl Pts',(86.8625734762367,4.09980311263617,2.20531515781764));
#14804=CARTESIAN_POINT('Ctrl Pts',(87.0581563373692,0.437778084173888,4.63466839126788));
#14805=CARTESIAN_POINT('Ctrl Pts',(87.2537391985015,-3.61436018445999,2.93397379113351));
#14806=CARTESIAN_POINT('Ctrl Pts',(87.4493220596338,-4.44566765417441,-1.38124494524121));
#14807=CARTESIAN_POINT('Ctrl Pts',(87.6449049207663,-1.31535064595982,-4.46560795232644));
#14808=CARTESIAN_POINT('Ctrl Pts',(87.8404877818986,2.98710418859627,-3.57057650407201));
#14809=CARTESIAN_POINT('Ctrl Pts',(88.036070643031,4.62768537435842,0.506269116897338));
#14810=CARTESIAN_POINT('Ctrl Pts',(88.2316535041634,2.14444952357415,4.13196720132669));
#14811=CARTESIAN_POINT('Ctrl Pts',(88.4272363652956,-2.24976574392887,4.07558631043868));
#14812=CARTESIAN_POINT('Ctrl Pts',(88.6228192264281,-4.63913490804326,0.387363858269165));
#14813=CARTESIAN_POINT('Ctrl Pts',(88.8184020875603,-2.89454502950186,-3.64603994405123));
#14814=CARTESIAN_POINT('Ctrl Pts',(89.013984948693,1.42957407300277,-4.43039622715286));
#14815=CARTESIAN_POINT('Ctrl Pts',(89.2095678098251,4.47948277913555,-1.26670861792234));
#14816=CARTESIAN_POINT('Ctrl Pts',(89.4051506709576,3.5382200440707,3.02571355069598));
#14817=CARTESIAN_POINT('Ctrl Pts',(89.60073353209,-0.557222135711404,4.62197359272669));
#14818=CARTESIAN_POINT('Ctrl Pts',(89.7963163932224,-4.15366376589914,2.09926735339947));
#14819=CARTESIAN_POINT('Ctrl Pts',(89.9918992543546,-4.05369624180864,-2.29366505455626));
#14820=CARTESIAN_POINT('Ctrl Pts',(90.1874821154872,-0.331113665829834,
-4.64363077914069));
#14821=CARTESIAN_POINT('Ctrl Pts',(90.3504678330974,2.99780922363717,-3.15128549092374));
#14822=CARTESIAN_POINT('Ctrl Pts',(90.4809017308115,4.05832850523665,-0.685962427659713));
#14823=CARTESIAN_POINT('Ctrl Pts',(90.5461413414815,3.95874196087756,0.643064283084749));
#14824=CARTESIAN_POINT('Ctrl Pts',(90.5787838086296,3.75219732397504,1.25872504175513));
#14825=CARTESIAN_POINT('Ctrl Pts',(82.3076494379063,-1.86731594862207,3.76046266780178));
#14826=CARTESIAN_POINT('Ctrl Pts',(82.3402465814283,-2.48347194810449,3.45450086833384));
#14827=CARTESIAN_POINT('Ctrl Pts',(82.4054408684725,-3.55541065741244,2.53423645736299));
#14828=CARTESIAN_POINT('Ctrl Pts',(82.5358294425606,-4.61286110841813,-0.108122194255548));
#14829=CARTESIAN_POINT('Ctrl Pts',(82.698815160171,-3.24066310182923,-3.7268443852249));
#14830=CARTESIAN_POINT('Ctrl Pts',(82.8943980213033,1.31303851534757,-4.76341953425041));
#14831=CARTESIAN_POINT('Ctrl Pts',(83.0899808824357,4.68823725620352,-1.5482112856448));
#14832=CARTESIAN_POINT('Ctrl Pts',(83.2855637435681,3.88975711341433,3.04323406685525));
#14833=CARTESIAN_POINT('Ctrl Pts',(83.4811466047003,-0.376972691150075,
4.92445773533245));
#14834=CARTESIAN_POINT('Ctrl Pts',(83.6767294658329,-4.30679124862426,2.41658017814598));
#14835=CARTESIAN_POINT('Ctrl Pts',(83.8723123269652,-4.39922153215723,-2.2443616818719));
#14836=CARTESIAN_POINT('Ctrl Pts',(84.0678951880976,-0.571179608431502,
-4.90550271477511));
#14837=CARTESIAN_POINT('Ctrl Pts',(84.26347804923,3.76573662544653,-3.19515397863332));
#14838=CARTESIAN_POINT('Ctrl Pts',(84.4590609103622,4.74698446986084,1.36241488501073));
#14839=CARTESIAN_POINT('Ctrl Pts',(84.6546437714947,1.4980695853024,4.70593097002559));
#14840=CARTESIAN_POINT('Ctrl Pts',(84.850226632627,-3.08579219031039,3.85588438681077));
#14841=CARTESIAN_POINT('Ctrl Pts',(85.0458094937594,-4.91984804113526,-0.430214167685617));
#14842=CARTESIAN_POINT('Ctrl Pts',(85.2413923548919,-2.369723356298,-4.33294277636122));
#14843=CARTESIAN_POINT('Ctrl Pts',(85.4369752160242,2.29210871439886,-4.37449607510255));
#14844=CARTESIAN_POINT('Ctrl Pts',(85.6325580771566,4.91139658138516,-0.517847041979676));
#14845=CARTESIAN_POINT('Ctrl Pts',(85.8281409382889,3.15403805498757,3.80026640624941));
#14846=CARTESIAN_POINT('Ctrl Pts',(86.0237237994213,-1.41394814335575,4.73188452819988));
#14847=CARTESIAN_POINT('Ctrl Pts',(86.2193066605536,-4.72193630859334,1.44682358130377));
#14848=CARTESIAN_POINT('Ctrl Pts',(86.414889521686,-3.82211033872426,-3.12753150742783));
#14849=CARTESIAN_POINT('Ctrl Pts',(86.6104723828184,0.483676340945399,-4.91487924251923));
#14850=CARTESIAN_POINT('Ctrl Pts',(86.8060552439507,4.35844917361658,-2.32247750878875));
#14851=CARTESIAN_POINT('Ctrl Pts',(87.0016381050832,4.34931868458738,2.33953147450845));
#14852=CARTESIAN_POINT('Ctrl Pts',(87.1972209662155,0.464421424368368,4.91673606688068));
#14853=CARTESIAN_POINT('Ctrl Pts',(87.3928038273479,-3.83433151573773,3.11253654853231));
#14854=CARTESIAN_POINT('Ctrl Pts',(87.5883866884802,-4.71623267326457,-1.46530803633315));
#14855=CARTESIAN_POINT('Ctrl Pts',(87.7839695496127,-1.39540338501245,-4.73738654552288));
#14856=CARTESIAN_POINT('Ctrl Pts',(87.9795524107449,3.16890048213002,-3.78788314395994));
#14857=CARTESIAN_POINT('Ctrl Pts',(88.1751352718774,4.90932806091437,0.537080847313));
#14858=CARTESIAN_POINT('Ctrl Pts',(88.3707181330097,2.27496153468657,4.38344029191121));
#14859=CARTESIAN_POINT('Ctrl Pts',(88.5663009941421,-2.38668734014466,4.3236280386259));
#14860=CARTESIAN_POINT('Ctrl Pts',(88.7618838552744,-4.92147441756056,0.410938969559601));
#14861=CARTESIAN_POINT('Ctrl Pts',(88.9574667164069,-3.07070813751762,-3.86793931750963));
#14862=CARTESIAN_POINT('Ctrl Pts',(89.1530495775392,1.51657849313516,-4.70003182140403));
#14863=CARTESIAN_POINT('Ctrl Pts',(89.3486324386716,4.75210579955249,-1.34380098470509));
#14864=CARTESIAN_POINT('Ctrl Pts',(89.5442152998039,3.75355745753441,3.20985962464658));
#14865=CARTESIAN_POINT('Ctrl Pts',(89.7397981609363,-0.59113488617187,4.9032686580868));
#14866=CARTESIAN_POINT('Ctrl Pts',(89.9353810220687,-4.40645731763019,2.22702956050341));
#14867=CARTESIAN_POINT('Ctrl Pts',(90.1309638832011,-4.30040573211902,-2.43325837946207));
#14868=CARTESIAN_POINT('Ctrl Pts',(90.3265467443335,-0.351265369080108,
-4.92624390907766));
#14869=CARTESIAN_POINT('Ctrl Pts',(90.4895324619438,3.18025702966254,-3.34307392076952));
#14870=CARTESIAN_POINT('Ctrl Pts',(90.6199663596579,4.30531991685567,-0.727710361102428));
#14871=CARTESIAN_POINT('Ctrl Pts',(90.6852059703279,4.19967249764679,0.682201419182997));
#14872=CARTESIAN_POINT('Ctrl Pts',(90.7178484374759,3.98055747582716,1.33533152506521));
#14873=CARTESIAN_POINT('Ctrl Pts',(82.4467140667525,-1.97444178618949,3.97619622549273));
#14874=CARTESIAN_POINT('Ctrl Pts',(82.4793112102746,-2.6259459695534,3.65268173813828));
#14875=CARTESIAN_POINT('Ctrl Pts',(82.5445054973187,-3.75938060949927,2.67962278220492));
#14876=CARTESIAN_POINT('Ctrl Pts',(82.6748940714069,-4.87749581589017,-0.114325044195209));
#14877=CARTESIAN_POINT('Ctrl Pts',(82.8378797890173,-3.42657633698018,-3.94064929946303));
#14878=CARTESIAN_POINT('Ctrl Pts',(83.0334626501496,1.38836607350325,-5.03669161103426));
#14879=CARTESIAN_POINT('Ctrl Pts',(83.2290455112822,4.95719620937701,-1.63703044387478));
#14880=CARTESIAN_POINT('Ctrl Pts',(83.4246283724142,4.11290814953964,3.21782101801696));
#14881=CARTESIAN_POINT('Ctrl Pts',(83.6202112335468,-0.39859919485411,5.20696839446976));
#14882=CARTESIAN_POINT('Ctrl Pts',(83.815794094679,-4.55386706890918,2.55521669320588));
#14883=CARTESIAN_POINT('Ctrl Pts',(84.0113769558115,-4.65159997492945,-2.37311821348732));
#14884=CARTESIAN_POINT('Ctrl Pts',(84.2069598169438,-0.603947546819121,
-5.18692594548081));
#14885=CARTESIAN_POINT('Ctrl Pts',(84.4025426780763,3.9817727442174,-3.37845640604018));
#14886=CARTESIAN_POINT('Ctrl Pts',(84.5981255392086,5.01931368529363,1.44057511053593));
#14887=CARTESIAN_POINT('Ctrl Pts',(84.7937084003409,1.58401216999367,4.97590499186716));
#14888=CARTESIAN_POINT('Ctrl Pts',(84.9892912614734,-3.26282065364566,4.07709218231267));
#14889=CARTESIAN_POINT('Ctrl Pts',(85.1848741226057,-5.20209424724726,-0.454895075638387));
#14890=CARTESIAN_POINT('Ctrl Pts',(85.3804569837381,-2.5056717476422,-4.58151888068461));
#14891=CARTESIAN_POINT('Ctrl Pts',(85.5760398448705,2.4236044401258,-4.62545604592406));
#14892=CARTESIAN_POINT('Ctrl Pts',(85.7716227060028,5.19315793665816,-0.547555350391454));
#14893=CARTESIAN_POINT('Ctrl Pts',(85.9672055671352,3.33498170761871,4.01828346011176));
#14894=CARTESIAN_POINT('Ctrl Pts',(86.1627884282675,-1.49506477455341,5.00334747678646));
#14895=CARTESIAN_POINT('Ctrl Pts',(86.3583712893999,-4.99282853889391,1.52982623978471));
#14896=CARTESIAN_POINT('Ctrl Pts',(86.5539541505323,-4.04138055467945,-3.30695450892843));
#14897=CARTESIAN_POINT('Ctrl Pts',(86.7495370116647,0.511424314272321,-5.19684039418513));
#14898=CARTESIAN_POINT('Ctrl Pts',(86.9451198727969,4.60848855156075,-2.45571545844803));
#14899=CARTESIAN_POINT('Ctrl Pts',(87.1407027339295,4.59883425653857,2.47374779119925));
#14900=CARTESIAN_POINT('Ctrl Pts',(87.3362855950617,0.491064764562854,5.19880374249346));
#14901=CARTESIAN_POINT('Ctrl Pts',(87.5318684561942,-4.05430284701545,3.29109930593112));
#14902=CARTESIAN_POINT('Ctrl Pts',(87.7274513173265,-4.98679769235471,-1.54937112742509));
#14903=CARTESIAN_POINT('Ctrl Pts',(87.9230341784589,-1.4754561240651,-5.00916513871929));
#14904=CARTESIAN_POINT('Ctrl Pts',(88.1186170395912,3.35069677566378,-4.00518978384787));
#14905=CARTESIAN_POINT('Ctrl Pts',(88.3141999007237,5.1909707474703,0.567892577728663));
#14906=CARTESIAN_POINT('Ctrl Pts',(88.509782761856,2.405473545799,4.63491338249572));
#14907=CARTESIAN_POINT('Ctrl Pts',(88.7053656229884,-2.52360893636046,4.57166976681311));
#14908=CARTESIAN_POINT('Ctrl Pts',(88.9009484841208,-5.20381392707786,0.434514080850038));
#14909=CARTESIAN_POINT('Ctrl Pts',(89.0965313452531,-3.24687124553338,-4.08983869096806));
#14910=CARTESIAN_POINT('Ctrl Pts',(89.2921142063854,1.60358291326754,-4.96966741565522));
#14911=CARTESIAN_POINT('Ctrl Pts',(89.4876970675179,5.0247288199694,-1.42089335148785));
#14912=CARTESIAN_POINT('Ctrl Pts',(89.6832799286502,3.96889487099811,3.39400569859719));
#14913=CARTESIAN_POINT('Ctrl Pts',(89.8788627897826,-0.625047636632337,
5.1845637234469));
#14914=CARTESIAN_POINT('Ctrl Pts',(90.0744456509149,-4.65925086936123,2.35479176760734));
#14915=CARTESIAN_POINT('Ctrl Pts',(90.2700285120473,-4.54711522242937,-2.57285170436789));
#14916=CARTESIAN_POINT('Ctrl Pts',(90.4656113731797,-0.37141707233039,-5.20885703901466));
#14917=CARTESIAN_POINT('Ctrl Pts',(90.62859709079,3.3627048356879,-3.53486235061532));
#14918=CARTESIAN_POINT('Ctrl Pts',(90.7590309885042,4.55231132847466,-0.769458294545144));
#14919=CARTESIAN_POINT('Ctrl Pts',(90.8242705991742,4.44060303441602,0.721338555281245));
#14920=CARTESIAN_POINT('Ctrl Pts',(90.8569130663221,4.20891762767928,1.41193800837531));
#14921=CARTESIAN_POINT('Ctrl Pts',(90.4430005297901,-0.73514273060804,-4.37679816075785));
#14922=CARTESIAN_POINT('Ctrl Pts',(90.4430005297901,-0.604496150119999,
-4.38932450298291));
#14923=CARTESIAN_POINT('Ctrl Pts',(90.4430005297901,-0.473689093681419,
-4.39569210928025));
#14924=CARTESIAN_POINT('Ctrl Pts',(90.4430005297901,-0.343055129970561,
-4.39568396726792));
#14925=CARTESIAN_POINT('Ctrl Pts',(90.4430005297901,-0.334607555765647,
-4.39568344075665));
#14926=CARTESIAN_POINT('Ctrl Pts',(90.4430005297901,-0.32616070523362,-4.39565623476939));
#14927=CARTESIAN_POINT('Ctrl Pts',(90.4430005297901,-0.317714668695276,
-4.39560228305825));
#14928=CARTESIAN_POINT('Ctrl Pts',(90.4430005297901,-0.185997485433182,
-4.39476089818012));
#14929=CARTESIAN_POINT('Ctrl Pts',(90.4430005297901,-0.0544775308798676,
-4.38741913239443));
#14930=CARTESIAN_POINT('Ctrl Pts',(90.4430005297901,0.0764804063629183,
-4.37382331815532));
#14931=CARTESIAN_POINT('Ctrl Pts',(90.4430005297901,0.212139516587092,-4.35973943671001));
#14932=CARTESIAN_POINT('Ctrl Pts',(90.4430005297901,0.347196453096418,-4.33894421155538));
#14933=CARTESIAN_POINT('Ctrl Pts',(90.4430005297901,0.481228112672906,-4.31165627564208));
#14934=CARTESIAN_POINT('Ctrl Pts',(90.4430005297901,0.615259772249436,-4.28436833972878));
#14935=CARTESIAN_POINT('Ctrl Pts',(90.4430005297901,0.748267008612133,-4.2505871487114));
#14936=CARTESIAN_POINT('Ctrl Pts',(90.4430005297901,0.879796089098197,-4.21048338220168));
#14937=CARTESIAN_POINT('Ctrl Pts',(90.4430005297901,0.89695340314272,-4.20525204542176));
#14938=CARTESIAN_POINT('Ctrl Pts',(90.4430005297901,0.914085511767477,-4.19991306416613));
#14939=CARTESIAN_POINT('Ctrl Pts',(90.4430005297901,0.931191357547311,-4.19446676463671));
#14940=CARTESIAN_POINT('Ctrl Pts',(90.4430005297901,0.947772132258861,-4.1891876415421));
#14941=CARTESIAN_POINT('Ctrl Pts',(90.4430005297901,0.964318662466657,-4.18381073214007));
#14942=CARTESIAN_POINT('Ctrl Pts',(90.4430005297901,0.980829620677607,-4.17833682356822));
#14943=CARTESIAN_POINT('Ctrl Pts',(90.4430005297901,1.10554259859385,-4.13699049889617));
#14944=CARTESIAN_POINT('Ctrl Pts',(90.4430005297901,1.22823748709516,-4.09011104027423));
#14945=CARTESIAN_POINT('Ctrl Pts',(90.4430005297901,1.34855752204243,-4.0379369945229));
#14946=CARTESIAN_POINT('Ctrl Pts',(90.4430005297901,1.46900346094926,-3.98570835338396));
#14947=CARTESIAN_POINT('Ctrl Pts',(90.4430005297901,1.58707030868872,-3.9281735359251));
#14948=CARTESIAN_POINT('Ctrl Pts',(90.4430005297901,1.70237501415389,-3.86552606404323));
#14949=CARTESIAN_POINT('Ctrl Pts',(90.4430005297901,1.81579371184005,-3.80390329985934));
#14950=CARTESIAN_POINT('Ctrl Pts',(90.4430005297902,1.9265404734797,-3.73733320231565));
#14951=CARTESIAN_POINT('Ctrl Pts',(90.4430005297902,2.03421675045152,-3.66596377333103));
#14952=CARTESIAN_POINT('Ctrl Pts',(90.4430005297902,2.12284103116633,-3.60722228925794));
#14953=CARTESIAN_POINT('Ctrl Pts',(90.4430005297902,2.2093848220462,-3.5452288234101));
#14954=CARTESIAN_POINT('Ctrl Pts',(90.4430005297902,2.29360397058158,-3.48005089866153));
#14955=CARTESIAN_POINT('Ctrl Pts',(90.4430005297902,2.31916577926078,-3.46026839466446));
#14956=CARTESIAN_POINT('Ctrl Pts',(90.4430005297901,2.34451328416944,-3.44019244944631));
#14957=CARTESIAN_POINT('Ctrl Pts',(90.4430005297901,2.36963923936788,-3.41982474290587));
#14958=CARTESIAN_POINT('Ctrl Pts',(90.4430005297901,2.38341896005211,-3.4086545682841));
#14959=CARTESIAN_POINT('Ctrl Pts',(90.4430005297901,2.39712536031611,-3.3974020346394));
#14960=CARTESIAN_POINT('Ctrl Pts',(90.4430005297901,2.41075460651509,-3.38607005694197));
#14961=CARTESIAN_POINT('Ctrl Pts',(90.4430005297901,2.50863448983006,-3.30468825206748));
#14962=CARTESIAN_POINT('Ctrl Pts',(90.4430005297901,2.60258657057775,-3.21917278388622));
#14963=CARTESIAN_POINT('Ctrl Pts',(90.4430005297901,2.69225999789868,-3.1297002006669));
#14964=CARTESIAN_POINT('Ctrl Pts',(90.4430005297901,2.78082905928829,-3.04132950989942));
#14965=CARTESIAN_POINT('Ctrl Pts',(90.4430005297901,2.86522469916423,-2.94909808560927));
#14966=CARTESIAN_POINT('Ctrl Pts',(90.4430005297901,2.94506902490659,-2.85314508885547));
#14967=CARTESIAN_POINT('Ctrl Pts',(90.4430005297901,3.02294128071918,-2.75956202907352));
#14968=CARTESIAN_POINT('Ctrl Pts',(90.4430005297901,3.09648463049278,-2.66243847701636));
#14969=CARTESIAN_POINT('Ctrl Pts',(90.4430005297901,3.1653041061699,-2.56188124623051));
#14970=CARTESIAN_POINT('Ctrl Pts',(90.4430005297901,3.18089572893538,-2.53909917192192));
#14971=CARTESIAN_POINT('Ctrl Pts',(90.4430005297901,3.19624468510206,-2.51614077549817));
#14972=CARTESIAN_POINT('Ctrl Pts',(90.4430005297901,3.21134602536756,-2.49300717327593));
#14973=CARTESIAN_POINT('Ctrl Pts',(90.4430005297901,3.25596252339905,-2.42465957631677));
#14974=CARTESIAN_POINT('Ctrl Pts',(90.4430005297901,3.29841825709037,-2.35478264430401));
#14975=CARTESIAN_POINT('Ctrl Pts',(90.4430005297901,3.33867108373866,-2.28349579149761));
#14976=CARTESIAN_POINT('Ctrl Pts',(90.4430005297901,3.35066966420011,-2.26224657472299));
#14977=CARTESIAN_POINT('Ctrl Pts',(90.4430005297901,3.3624724508268,-2.24087208124526));
#14978=CARTESIAN_POINT('Ctrl Pts',(90.4430005297901,3.37407817045463,-2.21937547389453));
#14979=CARTESIAN_POINT('Ctrl Pts',(90.4430005297901,3.38411062455509,-2.20079293584626));
#14980=CARTESIAN_POINT('Ctrl Pts',(90.4430005297901,3.39399467672431,-2.18212103945774));
#14981=CARTESIAN_POINT('Ctrl Pts',(90.4430005297901,3.40372092738814,-2.16337919409448));
#14982=CARTESIAN_POINT('Ctrl Pts',(90.4430005297901,3.46057573179043,-2.05382372517903));
#14983=CARTESIAN_POINT('Ctrl Pts',(90.4430005297901,3.5121286929711,-1.94172159775054));
#14984=CARTESIAN_POINT('Ctrl Pts',(90.4430005297901,3.55833134911402,-1.8275194805919));
#14985=CARTESIAN_POINT('Ctrl Pts',(90.4430005297901,3.60477976717121,-1.71270989768844));
#14986=CARTESIAN_POINT('Ctrl Pts',(90.4430005297901,3.64582094812531,-1.59577700537774));
#14987=CARTESIAN_POINT('Ctrl Pts',(90.4430005297901,3.6813548895811,-1.47716007623973));
#14988=CARTESIAN_POINT('Ctrl Pts',(90.4430005297901,3.71649769738405,-1.35984880222698));
#14989=CARTESIAN_POINT('Ctrl Pts',(90.4430005297901,3.74625384223616,-1.24088947957952));
#14990=CARTESIAN_POINT('Ctrl Pts',(90.4430005297901,3.7704762210856,-1.1207062915184));
#14991=CARTESIAN_POINT('Ctrl Pts',(90.4430005297901,3.78454126019077,-1.05092036131019));
#14992=CARTESIAN_POINT('Ctrl Pts',(90.4430005297901,3.79673954198557,-0.980721835780695));
#14993=CARTESIAN_POINT('Ctrl Pts',(90.4430005297901,3.80703431601148,-0.910195398393013));
#14994=CARTESIAN_POINT('Ctrl Pts',(90.4430005297901,3.81275326778125,-0.871016559411345));
#14995=CARTESIAN_POINT('Ctrl Pts',(90.4430005297901,3.81788468776157,-0.831736555533269));
#14996=CARTESIAN_POINT('Ctrl Pts',(90.4430005297901,3.82242148213659,-0.792370186591988));
#14997=CARTESIAN_POINT('Ctrl Pts',(90.4430005297901,3.82477895958205,-0.771914040860601));
#14998=CARTESIAN_POINT('Ctrl Pts',(90.4430005297901,3.82697612959026,-0.751431871386736));
#14999=CARTESIAN_POINT('Ctrl Pts',(90.4430005297901,3.82901104070976,-0.730934968196642));
#15000=CARTESIAN_POINT('Ctrl Pts',(90.4430005297901,3.83052437597814,-0.715691704649243));
#15001=CARTESIAN_POINT('Ctrl Pts',(90.4430005297901,3.83194777392775,-0.700442447857438));
#15002=CARTESIAN_POINT('Ctrl Pts',(90.4430005297901,3.83328081539606,-0.685190377817832));
#15003=CARTESIAN_POINT('Ctrl Pts',(90.4430005297901,3.83425091868927,-0.674090885622473));
#15004=CARTESIAN_POINT('Ctrl Pts',(90.4430005297901,3.83517321726714,-0.662989405527434));
#15005=CARTESIAN_POINT('Ctrl Pts',(90.4430005297901,3.83604763234583,-0.651886262828403));
#15006=CARTESIAN_POINT('Ctrl Pts',(90.4430005297901,3.84560195175947,-0.530567481362801));
#15007=CARTESIAN_POINT('Ctrl Pts',(90.4430005297901,3.84944379016812,-0.409049619730809));
#15008=CARTESIAN_POINT('Ctrl Pts',(90.4430005297901,3.84760828243506,-0.287700070934821));
#15009=CARTESIAN_POINT('Ctrl Pts',(90.4430005297901,3.84578233256279,-0.166982413835497));
#15010=CARTESIAN_POINT('Ctrl Pts',(90.4430005297901,3.83833779215534,-0.0464305624906118));
#15011=CARTESIAN_POINT('Ctrl Pts',(90.4430005297901,3.82525995547212,0.0735799566286457));
#15012=CARTESIAN_POINT('Ctrl Pts',(90.4430005297901,3.82045107309815,0.117709309522672));
#15013=CARTESIAN_POINT('Ctrl Pts',(90.4430005297901,3.81488003307241,0.161765275517719));
#15014=CARTESIAN_POINT('Ctrl Pts',(90.4430005297901,3.80854450228283,0.205728399455354));
#15015=CARTESIAN_POINT('Ctrl Pts',(90.4430005297901,3.80423315264889,0.235645450542401));
#15016=CARTESIAN_POINT('Ctrl Pts',(90.4430005297901,3.79956659035793,0.26552569568798));
#15017=CARTESIAN_POINT('Ctrl Pts',(90.4430005297901,3.79455002103167,0.295328529435823));
#15018=CARTESIAN_POINT('Ctrl Pts',(90.4430005297901,3.77482815796987,0.412493740918343));
#15019=CARTESIAN_POINT('Ctrl Pts',(90.4430005297901,3.74969110989646,0.528545803924548));
#15020=CARTESIAN_POINT('Ctrl Pts',(90.4430005297901,3.7191465886351,0.643128876190501));
#15021=CARTESIAN_POINT('Ctrl Pts',(90.4430005297901,3.68911896816514,0.75577287466225));
#15022=CARTESIAN_POINT('Ctrl Pts',(90.4430005297901,3.65386504693388,0.86699780520124));
#15023=CARTESIAN_POINT('Ctrl Pts',(90.4430005297901,3.61334804281027,0.976442362197689));
#15024=CARTESIAN_POINT('Ctrl Pts',(90.4430005297901,3.58775745474183,1.04556767476729));
#15025=CARTESIAN_POINT('Ctrl Pts',(90.4430005297901,3.56006645269277,1.11398226512644));
#15026=CARTESIAN_POINT('Ctrl Pts',(90.4430005297901,3.5302572329849,1.18158852036477));
#15027=CARTESIAN_POINT('',(82.4415333234128,-2.16533833838417,-3.03088926843041));
#15028=CARTESIAN_POINT('Ctrl Pts',(82.4430005297901,-2.16672251220859,-3.03255290461515));
#15029=CARTESIAN_POINT('Ctrl Pts',(82.4430005297901,-2.2696406448299,-2.97356260115279));
#15030=CARTESIAN_POINT('Ctrl Pts',(82.4430005297901,-2.36930641006408,-2.9095828574348));
#15031=CARTESIAN_POINT('Ctrl Pts',(82.4430005297901,-2.46528951680289,-2.84070661811295));
#15032=CARTESIAN_POINT('Ctrl Pts',(82.4430005297902,-2.55861706129925,-2.77373597600251));
#15033=CARTESIAN_POINT('Ctrl Pts',(82.4430005297901,-2.64846403506778,-2.70213611715619));
#15034=CARTESIAN_POINT('Ctrl Pts',(82.4430005297901,-2.73474523689391,-2.6262943269763));
#15035=CARTESIAN_POINT('Ctrl Pts',(82.4430005297901,-2.7766889505776,-2.58942550427522));
#15036=CARTESIAN_POINT('Ctrl Pts',(82.4430005297901,-2.81778965642945,-2.55155350981108));
#15037=CARTESIAN_POINT('Ctrl Pts',(82.4430005297901,-2.85803541810069,-2.51271907899779));
#15038=CARTESIAN_POINT('Ctrl Pts',(82.4430005297901,-2.8806302377794,-2.49091661023797));
#15039=CARTESIAN_POINT('Ctrl Pts',(82.4430005297901,-2.90295682592989,-2.46880946058695));
#15040=CARTESIAN_POINT('Ctrl Pts',(82.4430005297901,-2.92500922126342,-2.44640821512361));
#15041=CARTESIAN_POINT('Ctrl Pts',(82.4430005297901,-2.94264658870197,-2.4284918395398));
#15042=CARTESIAN_POINT('Ctrl Pts',(82.4430005297901,-2.96010315890421,-2.41039277122427));
#15043=CARTESIAN_POINT('Ctrl Pts',(82.4430005297901,-2.97737164425535,-2.3921219690667));
#15044=CARTESIAN_POINT('Ctrl Pts',(82.4430005297901,-3.05889223068647,-2.30586967327093));
#15045=CARTESIAN_POINT('Ctrl Pts',(82.4430005297901,-3.13626978859535,-2.2157468104726));
#15046=CARTESIAN_POINT('Ctrl Pts',(82.4430005297901,-3.20941666153041,-2.12217282556583));
#15047=CARTESIAN_POINT('Ctrl Pts',(82.4430005297901,-3.28383577531618,-2.02697131180667));
#15048=CARTESIAN_POINT('Ctrl Pts',(82.4430005297901,-3.3538762580029,-1.92819703496745));
#15049=CARTESIAN_POINT('Ctrl Pts',(82.4430005297901,-3.41941495616528,-1.8262468129962));
#15050=CARTESIAN_POINT('Ctrl Pts',(82.4430005297901,-3.44787585716834,-1.78197380702992));
#15051=CARTESIAN_POINT('Ctrl Pts',(82.4430005297901,-3.47548736563765,-1.73710135664425));
#15052=CARTESIAN_POINT('Ctrl Pts',(82.4430005297901,-3.50223725630824,-1.69165980496045));
#15053=CARTESIAN_POINT('Ctrl Pts',(82.4430005297901,-3.51811119609673,-1.66469384595122));
#15054=CARTESIAN_POINT('Ctrl Pts',(82.4430005297901,-3.53368487909068,-1.63752135795755));
#15055=CARTESIAN_POINT('Ctrl Pts',(82.4430005297901,-3.54893402419485,-1.61018817838778));
#15056=CARTESIAN_POINT('Ctrl Pts',(82.4430005297901,-3.6091502173992,-1.50225425746175));
#15057=CARTESIAN_POINT('Ctrl Pts',(82.4430005297901,-3.66437396957584,-1.39171139125269));
#15058=CARTESIAN_POINT('Ctrl Pts',(82.4430005297901,-3.71451260875185,-1.2789963503931));
#15059=CARTESIAN_POINT('Ctrl Pts',(82.4430005297901,-3.76520285462665,-1.16504126048922));
#15060=CARTESIAN_POINT('Ctrl Pts',(82.4430005297901,-3.81069597912495,-1.04886525967351));
#15061=CARTESIAN_POINT('Ctrl Pts',(82.4430005297901,-3.85086009590959,-0.930879705196395));
#15062=CARTESIAN_POINT('Ctrl Pts',(82.4430005297901,-3.89098099755938,-0.81302109890226));
#15063=CARTESIAN_POINT('Ctrl Pts',(82.4430005297901,-3.92578479490074,-0.69335605824151));
#15064=CARTESIAN_POINT('Ctrl Pts',(82.4430005297901,-3.95509723183628,-0.57226596872187));
#15065=CARTESIAN_POINT('Ctrl Pts',(82.4430005297901,-3.97614380137511,-0.485322293750682));
#15066=CARTESIAN_POINT('Ctrl Pts',(82.4430005297901,-3.99435851010471,-0.397643325062507));
#15067=CARTESIAN_POINT('Ctrl Pts',(82.4430005297901,-4.00966125689264,-0.309364507448106));
#15068=CARTESIAN_POINT('Ctrl Pts',(82.4430005297901,-4.01435795168095,-0.282270112673519));
#15069=CARTESIAN_POINT('Ctrl Pts',(82.4430005297901,-4.01878024374387,-0.255119189321616));
#15070=CARTESIAN_POINT('Ctrl Pts',(82.4430005297901,-4.02292554754272,-0.227915601567328));
#15071=CARTESIAN_POINT('Ctrl Pts',(82.4430005297901,-4.02569591908626,-0.20973501721123));
#15072=CARTESIAN_POINT('Ctrl Pts',(82.4430005297901,-4.02834281759651,-0.191528743140453));
#15073=CARTESIAN_POINT('Ctrl Pts',(82.4430005297901,-4.03086308406066,-0.173316124913738));
#15074=CARTESIAN_POINT('Ctrl Pts',(82.4430005297901,-4.04843750869815,-0.046315154568297));
#15075=CARTESIAN_POINT('Ctrl Pts',(82.4430005297901,-4.05988667808791,0.0811706755148063));
#15076=CARTESIAN_POINT('Ctrl Pts',(82.4430005297901,-4.06508069808371,0.208716684251388));
#15077=CARTESIAN_POINT('Ctrl Pts',(82.4430005297901,-4.06928311936486,0.311912679236813));
#15078=CARTESIAN_POINT('Ctrl Pts',(82.4430005297901,-4.06939010282019,0.41514889890651));
#15079=CARTESIAN_POINT('Ctrl Pts',(82.4430005297901,-4.06531043519685,0.518211439887893));
#15080=CARTESIAN_POINT('Ctrl Pts',(82.4430005297901,-4.06037373247765,0.642924816879994));
#15081=CARTESIAN_POINT('Ctrl Pts',(82.4430005297901,-4.04930850365813,0.767384162347736));
#15082=CARTESIAN_POINT('Ctrl Pts',(82.4430005297901,-4.03236186892167,0.891221661938466));
#15083=CARTESIAN_POINT('Ctrl Pts',(82.4430005297901,-4.01541523418522,1.01505916152921));
#15084=CARTESIAN_POINT('Ctrl Pts',(82.4430005297901,-3.99258695128159,1.13827557220802));
#15085=CARTESIAN_POINT('Ctrl Pts',(82.4430005297901,-3.96407180720896,1.26050316969768));
#15086=CARTESIAN_POINT('Ctrl Pts',(82.4430005297901,-3.95547258916303,1.29736294355562));
#15087=CARTESIAN_POINT('Ctrl Pts',(82.4430005297901,-3.9463558470242,1.33413274985256));
#15088=CARTESIAN_POINT('Ctrl Pts',(82.4430005297901,-3.93672603994556,1.37080234332704));
#15089=CARTESIAN_POINT('Ctrl Pts',(82.4430005297901,-3.93229805917785,1.38766376675315));
#15090=CARTESIAN_POINT('Ctrl Pts',(82.4430005297901,-3.92776385858572,1.40449532876003));
#15091=CARTESIAN_POINT('Ctrl Pts',(82.4430005297901,-3.92312493683006,1.42129347051884));
#15092=CARTESIAN_POINT('Ctrl Pts',(82.4430005297901,-3.88922045173421,1.54406604071895));
#15093=CARTESIAN_POINT('Ctrl Pts',(82.4430005297901,-3.84971460164585,1.66509780755738));
#15094=CARTESIAN_POINT('Ctrl Pts',(82.4430005297901,-3.80489648218867,1.78401656475369));
#15095=CARTESIAN_POINT('Ctrl Pts',(82.4430005297901,-3.75909623688204,1.90554125871933));
#15096=CARTESIAN_POINT('Ctrl Pts',(82.4430005297901,-3.70774825330481,2.02486010771724));
#15097=CARTESIAN_POINT('Ctrl Pts',(82.4430005297901,-3.65110614360382,2.14157776456584));
#15098=CARTESIAN_POINT('Ctrl Pts',(82.4430005297901,-3.59646760587821,2.25416682826126));
#15099=CARTESIAN_POINT('Ctrl Pts',(82.4430005297901,-3.53690231336455,2.36433614457288));
#15100=CARTESIAN_POINT('Ctrl Pts',(82.4430005297901,-3.47259286055702,2.47172179522677));
#15101=CARTESIAN_POINT('Ctrl Pts',(82.4430005297901,-3.40566020000046,2.58348774859871));
#15102=CARTESIAN_POINT('Ctrl Pts',(82.4430005297901,-3.33358842352915,2.69223917331592));
#15103=CARTESIAN_POINT('Ctrl Pts',(82.4430005297901,-3.25661397611832,2.79770775568241));
#15104=CARTESIAN_POINT('Ctrl Pts',(82.4430005297901,-3.24591769429999,2.81236355014301));
#15105=CARTESIAN_POINT('Ctrl Pts',(82.4430005297901,-3.23512667474305,2.82695590898394));
#15106=CARTESIAN_POINT('Ctrl Pts',(82.4430005297901,-3.22424148623506,2.8414840661082));
#15107=CARTESIAN_POINT('Ctrl Pts',(82.4430005297901,-3.19678203985352,2.87813342236721));
#15108=CARTESIAN_POINT('Ctrl Pts',(82.4430005297901,-3.16876263224132,2.91432166979658));
#15109=CARTESIAN_POINT('Ctrl Pts',(82.4430005297901,-3.14020380828486,2.95003182240799));
#15110=CARTESIAN_POINT('Ctrl Pts',(82.4430005297901,-3.05724825873483,3.05376002000154));
#15111=CARTESIAN_POINT('Ctrl Pts',(82.4430005297901,-2.96972905213257,3.15347708428787));
#15112=CARTESIAN_POINT('Ctrl Pts',(82.4430005297901,-2.87797244189919,3.24894641929633));
#15113=CARTESIAN_POINT('Ctrl Pts',(82.4430005297901,-2.78576185253439,3.34488810268026));
#15114=CARTESIAN_POINT('Ctrl Pts',(82.4430005297901,-2.68927141017721,3.43654055759438));
#15115=CARTESIAN_POINT('Ctrl Pts',(82.4430005297901,-2.58878423218922,3.52364130332058));
#15116=CARTESIAN_POINT('Ctrl Pts',(82.4430005297901,-2.48907040233302,3.61007172273917));
#15117=CARTESIAN_POINT('Ctrl Pts',(82.4430005297901,-2.38542062149339,3.69202080476271));
#15118=CARTESIAN_POINT('Ctrl Pts',(82.4430005297901,-2.27807132967477,3.7692010985491));
#15119=CARTESIAN_POINT('Ctrl Pts',(82.4430005297901,-2.18508355965287,3.83605597283143));
#15120=CARTESIAN_POINT('Ctrl Pts',(82.4430005297901,-2.08931913384727,3.89933243962664));
#15121=CARTESIAN_POINT('Ctrl Pts',(82.4430005297901,-1.99091130097234,3.9588194824242));
#15122=CARTESIAN_POINT('Ctrl Pts',(82.4430005297901,-1.98447919887495,3.96270765597266));
#15123=CARTESIAN_POINT('Ctrl Pts',(82.4430005297901,-1.97803579776514,3.96657963149843));
#15124=CARTESIAN_POINT('Ctrl Pts',(82.4430005297901,-1.97158113240047,3.97043534620103));
#15125=CARTESIAN_POINT('Ctrl Pts',(82.4415333234128,-2.16408072405065,-3.02912894778225));
#15126=CARTESIAN_POINT('Ctrl Pts',(82.4420336965111,-2.15504512285644,-3.03558419307279));
#15127=CARTESIAN_POINT('Ctrl Pts',(82.4425340696094,-2.14598063840387,-3.04199900959491));
#15128=CARTESIAN_POINT('Ctrl Pts',(82.4430344427077,-2.13688763362806,-3.04837314050421));
#15129=CARTESIAN_POINT('Ctrl Pts',(82.0310032950812,2.5732449024852,-3.61351950356445));
#15130=CARTESIAN_POINT('Ctrl Pts',(82.0636457680076,3.16616325925722,-3.19130979057643));
#15131=CARTESIAN_POINT('Ctrl Pts',(82.1288853844562,4.13207912470726,-2.05174262577274));
#15132=CARTESIAN_POINT('Ctrl Pts',(82.2593192879487,4.79464520668388,0.882555540610264));
#15133=CARTESIAN_POINT('Ctrl Pts',(82.4223050055592,2.75914274104666,4.42905501007769));
#15134=CARTESIAN_POINT('Ctrl Pts',(82.6178878666914,-2.16479008544544,4.75065483431134));
#15135=CARTESIAN_POINT('Ctrl Pts',(82.8134707278238,-5.14967299145611,0.832949191282387));
#15136=CARTESIAN_POINT('Ctrl Pts',(83.0090535889562,-3.55042897662582,-3.82414592282758));
#15137=CARTESIAN_POINT('Ctrl Pts',(83.2046364500884,1.21504830394734,-5.0748705164238));
#15138=CARTESIAN_POINT('Ctrl Pts',(83.400219311221,4.89660859864141,-1.80258629906098));
#15139=CARTESIAN_POINT('Ctrl Pts',(83.5958021723532,4.21527029670854,3.07568249282053));
#15140=CARTESIAN_POINT('Ctrl Pts',(83.7913850334858,-0.222660655853561,
5.21331275103613));
#15141=CARTESIAN_POINT('Ctrl Pts',(83.9869678946179,-4.46203744762071,2.7051724468734));
#15142=CARTESIAN_POINT('Ctrl Pts',(84.1825507557504,-4.72526831706301,-2.21356276749624));
#15143=CARTESIAN_POINT('Ctrl Pts',(84.3781336168827,-0.777683074796472,
-5.15976630774078));
#15144=CARTESIAN_POINT('Ctrl Pts',(84.5737164780151,3.86289539882142,-3.50798698251897));
#15145=CARTESIAN_POINT('Ctrl Pts',(84.7692993391475,5.06117659898468,1.26982667827935));
#15146=CARTESIAN_POINT('Ctrl Pts',(84.96488220028,1.74933589258655,4.91607408021796));
#15147=CARTESIAN_POINT('Ctrl Pts',(85.1604650614123,-3.12137193940479,4.18150613925552));
#15148=CARTESIAN_POINT('Ctrl Pts',(85.3560479225446,-5.21056228074381,-0.279286952965116));
#15149=CARTESIAN_POINT('Ctrl Pts',(85.5516307836769,-2.65651348040282,-4.49120199383985));
#15150=CARTESIAN_POINT('Ctrl Pts',(85.7472136448093,2.26480862632819,-4.70091489012678));
#15151=CARTESIAN_POINT('Ctrl Pts',(85.9427965059417,5.16791352719978,-0.721546383514633));
#15152=CARTESIAN_POINT('Ctrl Pts',(86.1383793670741,3.46578485734584,3.90080690363208));
#15153=CARTESIAN_POINT('Ctrl Pts',(86.3339622282066,-1.32477558834876,5.04707131090363));
#15154=CARTESIAN_POINT('Ctrl Pts',(86.5295450893389,-4.93480143762726,1.69578718575462));
#15155=CARTESIAN_POINT('Ctrl Pts',(86.7251279504711,-4.14732466254241,-3.16664760615603));
#15156=CARTESIAN_POINT('Ctrl Pts',(86.9207108116036,0.335917868796414,-5.20721791424714));
#15157=CARTESIAN_POINT('Ctrl Pts',(87.1162936727359,4.51981737154225,-2.60752975275673));
#15158=CARTESIAN_POINT('Ctrl Pts',(87.3118765338683,4.67601458569188,2.3157815033228));
#15159=CARTESIAN_POINT('Ctrl Pts',(87.5074593950007,0.665320577523391,5.17545253638813));
#15160=CARTESIAN_POINT('Ctrl Pts',(87.7030422561331,-3.93825640509612,3.42317175243948));
#15161=CARTESIAN_POINT('Ctrl Pts',(87.8986251172654,-5.03236803225271,-1.37956714940564));
#15162=CARTESIAN_POINT('Ctrl Pts',(88.0942079783978,-1.64204264387256,-4.95294612034352));
#15163=CARTESIAN_POINT('Ctrl Pts',(88.2897908395301,3.21155918647893,-4.11265223251709));
#15164=CARTESIAN_POINT('Ctrl Pts',(88.4853737006626,5.20323685809616,0.39250777042273));
#15165=CARTESIAN_POINT('Ctrl Pts',(88.6809565617948,2.55828132447017,4.54790108430783));
#15166=CARTESIAN_POINT('Ctrl Pts',(88.8765394229273,-2.36656955065493,4.65055642185629));
#15167=CARTESIAN_POINT('Ctrl Pts',(89.0721222840597,-5.1821983422279,0.609026662521216));
#15168=CARTESIAN_POINT('Ctrl Pts',(89.2677051451921,-3.38052451202556,-3.97526189866621));
#15169=CARTESIAN_POINT('Ctrl Pts',(89.4632880063243,1.43495189680254,-5.01702611225074));
#15170=CARTESIAN_POINT('Ctrl Pts',(89.6588708674568,4.96896142408185,-1.58819351471315));
#15171=CARTESIAN_POINT('Ctrl Pts',(89.8544537285891,4.08065273654629,3.25627251816026));
#15172=CARTESIAN_POINT('Ctrl Pts',(90.0500365897215,-0.455561874102168,
5.19825550801701));
#15173=CARTESIAN_POINT('Ctrl Pts',(90.2130223073318,-3.87588474101625,2.95720212609757));
#15174=CARTESIAN_POINT('Ctrl Pts',(90.3434108814201,-4.6129921626674,0.0418147320781305));
#15175=CARTESIAN_POINT('Ctrl Pts',(90.4086051684642,-4.26823548650425,-1.41053445637093));
#15176=CARTESIAN_POINT('Ctrl Pts',(90.4412023119862,-3.93156634387324,-2.05472598388759));
#15177=CARTESIAN_POINT('Ctrl Pts',(82.1694296294366,2.43416713531397,-3.41821736823327));
#15178=CARTESIAN_POINT('Ctrl Pts',(82.202072102363,2.99503966500787,-3.01882708611391));
#15179=CARTESIAN_POINT('Ctrl Pts',(82.2673117188115,3.9087500751154,-1.94085081639738));
#15180=CARTESIAN_POINT('Ctrl Pts',(82.3977456223042,4.53550603610597,0.834855512574021));
#15181=CARTESIAN_POINT('Ctrl Pts',(82.5607313399144,2.61001763781187,4.18967512016311));
#15182=CARTESIAN_POINT('Ctrl Pts',(82.7563142010469,-2.04778832972938,4.49389323874026));
#15183=CARTESIAN_POINT('Ctrl Pts',(82.9518970621792,-4.8713454134545,0.787930268451231));
#15184=CARTESIAN_POINT('Ctrl Pts',(83.1474799233117,-3.3585367342309,-3.61745993045656));
#15185=CARTESIAN_POINT('Ctrl Pts',(83.3430627844438,1.14937783280214,-4.80058583429903));
#15186=CARTESIAN_POINT('Ctrl Pts',(83.5386456455763,4.63195854922217,-1.70516079658948));
#15187=CARTESIAN_POINT('Ctrl Pts',(83.7342285067087,3.98744496211903,2.90944916881162));
#15188=CARTESIAN_POINT('Ctrl Pts',(83.9298113678411,-0.210626376946379,
4.93154559538018));
#15189=CARTESIAN_POINT('Ctrl Pts',(84.1253942289734,-4.22087493539727,2.55896430968406));
#15190=CARTESIAN_POINT('Ctrl Pts',(84.3209770901058,-4.46987880237384,-2.09392496430875));
#15191=CARTESIAN_POINT('Ctrl Pts',(84.5165599512381,-0.735651154124987,
-4.88089320999837));
#15192=CARTESIAN_POINT('Ctrl Pts',(84.7121428123705,3.6541150894287,-3.31838862896805));
#15193=CARTESIAN_POINT('Ctrl Pts',(84.9077256735029,4.78763204053,1.20119556627793));
#15194=CARTESIAN_POINT('Ctrl Pts',(85.1033085346353,1.65478844794245,4.65037196781321));
#15195=CARTESIAN_POINT('Ctrl Pts',(85.2988913957676,-2.95266920946872,3.95550567707689));
#15196=CARTESIAN_POINT('Ctrl Pts',(85.4944742569001,-4.92894378146587,-0.264192157370293));
#15197=CARTESIAN_POINT('Ctrl Pts',(85.6900571180323,-2.51293524462826,-4.24846320725372));
#15198=CARTESIAN_POINT('Ctrl Pts',(85.8856399791648,2.14240110634607,-4.44684162024508));
#15199=CARTESIAN_POINT('Ctrl Pts',(86.0812228402971,4.88860009162169,-0.682548517500101));
#15200=CARTESIAN_POINT('Ctrl Pts',(86.2768057014295,3.27846742829351,3.6899775675672));
#15201=CARTESIAN_POINT('Ctrl Pts',(86.4723885625619,-1.25317461844009,4.7742891097239));
#15202=CARTESIAN_POINT('Ctrl Pts',(86.6679714236942,-4.6680871560928,1.60413392136281));
#15203=CARTESIAN_POINT('Ctrl Pts',(86.8635542848266,-3.92317162788817,-2.9954978341087));
#15204=CARTESIAN_POINT('Ctrl Pts',(87.0591371459591,0.31776230688313,-4.92578017002461));
#15205=CARTESIAN_POINT('Ctrl Pts',(87.2547200070913,4.27553199184569,-2.46659897096611));
#15206=CARTESIAN_POINT('Ctrl Pts',(87.4503028682238,4.42328711804585,2.19061902056514));
#15207=CARTESIAN_POINT('Ctrl Pts',(87.645885729356,0.62936158260391,4.89573163529303));
#15208=CARTESIAN_POINT('Ctrl Pts',(87.8414685904886,-3.72540301254123,3.23815746036292));
#15209=CARTESIAN_POINT('Ctrl Pts',(88.0370514516208,-4.76038050831605,-1.30500482592964));
#15210=CARTESIAN_POINT('Ctrl Pts',(88.2326343127533,-1.55329414415176,-4.68525116186073));
#15211=CARTESIAN_POINT('Ctrl Pts',(88.4282171738855,3.03798205032592,-3.89037316024618));
#15212=CARTESIAN_POINT('Ctrl Pts',(88.623800035018,4.92201428049067,0.371293658911228));
#15213=CARTESIAN_POINT('Ctrl Pts',(88.8193828961503,2.42001230310359,4.30209784672624));
#15214=CARTESIAN_POINT('Ctrl Pts',(89.0149657572827,-2.23866209472541,4.39920490741982));
#15215=CARTESIAN_POINT('Ctrl Pts',(89.2105486184151,-4.90211284637034,0.576110219826852));
#15216=CARTESIAN_POINT('Ctrl Pts',(89.4061314795474,-3.19781520186777,-3.760408447192));
#15217=CARTESIAN_POINT('Ctrl Pts',(89.6017143406798,1.35739615944824,-4.74586778260333));
#15218=CARTESIAN_POINT('Ctrl Pts',(89.7972972018122,4.70040087652035,-1.50235543235697));
#15219=CARTESIAN_POINT('Ctrl Pts',(89.9928800629445,3.86010316092995,3.08027873276914));
#15220=CARTESIAN_POINT('Ctrl Pts',(90.188462924077,-0.430939838244923,4.91730216053644));
#15221=CARTESIAN_POINT('Ctrl Pts',(90.3514486416872,-3.66640238856974,2.79737238413463));
#15222=CARTESIAN_POINT('Ctrl Pts',(90.4818372157755,-4.36367090710306,0.0395547452550024));
#15223=CARTESIAN_POINT('Ctrl Pts',(90.5470315028196,-4.03754750937051,-1.33429842360129));
#15224=CARTESIAN_POINT('Ctrl Pts',(90.5796286463417,-3.71907453321684,-1.94367293110128));
#15225=CARTESIAN_POINT('Ctrl Pts',(82.307855963792,2.29508936814274,-3.22291523290208));
#15226=CARTESIAN_POINT('Ctrl Pts',(82.3404984367184,2.82391607075853,-2.84634438165137));
#15227=CARTESIAN_POINT('Ctrl Pts',(82.4057380531669,3.68542102552352,-1.82995900702202));
#15228=CARTESIAN_POINT('Ctrl Pts',(82.5361719566594,4.27636686552807,0.787155484537778));
#15229=CARTESIAN_POINT('Ctrl Pts',(82.6991576742698,2.46089253457709,3.95029523024854));
#15230=CARTESIAN_POINT('Ctrl Pts',(82.8947405354022,-1.93078657401334,4.23713164316919));
#15231=CARTESIAN_POINT('Ctrl Pts',(83.0903233965346,-4.59301783545288,0.742911345620072));
#15232=CARTESIAN_POINT('Ctrl Pts',(83.2859062576669,-3.16664449183598,-3.41077393808554));
#15233=CARTESIAN_POINT('Ctrl Pts',(83.4814891187993,1.08370736165695,-4.52630115217425));
#15234=CARTESIAN_POINT('Ctrl Pts',(83.6770719799316,4.36730849980295,-1.60773529411797));
#15235=CARTESIAN_POINT('Ctrl Pts',(83.8726548410641,3.75961962752953,2.7432158448027));
#15236=CARTESIAN_POINT('Ctrl Pts',(84.0682377021964,-0.198592098039204,
4.64977843972425));
#15237=CARTESIAN_POINT('Ctrl Pts',(84.2638205633287,-3.97971242317383,2.41275617249475));
#15238=CARTESIAN_POINT('Ctrl Pts',(84.4594034244612,-4.21448928768466,-1.97428716112127));
#15239=CARTESIAN_POINT('Ctrl Pts',(84.6549862855934,-0.693619233453502,
-4.60202011225595));
#15240=CARTESIAN_POINT('Ctrl Pts',(84.8505691467259,3.44533478003599,-3.12879027541714));
#15241=CARTESIAN_POINT('Ctrl Pts',(85.0461520078582,4.51408748207532,1.13256445427651));
#15242=CARTESIAN_POINT('Ctrl Pts',(85.2417348689906,1.56024100329834,4.38466985540846));
#15243=CARTESIAN_POINT('Ctrl Pts',(85.437317730123,-2.78396647953264,3.72950521489826));
#15244=CARTESIAN_POINT('Ctrl Pts',(85.6329005912553,-4.64732528218793,-0.249097361775471));
#15245=CARTESIAN_POINT('Ctrl Pts',(85.8284834523878,-2.36935700885369,-4.00572442066759));
#15246=CARTESIAN_POINT('Ctrl Pts',(86.02406631352,2.01999358636394,-4.19276835036339));
#15247=CARTESIAN_POINT('Ctrl Pts',(86.2196491746525,4.60928665604361,-0.643550651485564));
#15248=CARTESIAN_POINT('Ctrl Pts',(86.4152320357848,3.09114999924119,3.47914823150234));
#15249=CARTESIAN_POINT('Ctrl Pts',(86.6108148969172,-1.18157364853143,4.50150690854415));
#15250=CARTESIAN_POINT('Ctrl Pts',(86.8063977580496,-4.40137287455832,1.512480656971));
#15251=CARTESIAN_POINT('Ctrl Pts',(87.0019806191819,-3.69901859323395,-2.82434806206138));
#15252=CARTESIAN_POINT('Ctrl Pts',(87.1975634803144,0.299606744969849,-4.6443424258021));
#15253=CARTESIAN_POINT('Ctrl Pts',(87.3931463414466,4.03124661214913,-2.3256681891755));
#15254=CARTESIAN_POINT('Ctrl Pts',(87.5887292025792,4.17055965039982,2.06545653780747));
#15255=CARTESIAN_POINT('Ctrl Pts',(87.7843120637113,0.593402587684435,4.61601073419793));
#15256=CARTESIAN_POINT('Ctrl Pts',(87.9798949248439,-3.51254961998634,3.05314316828636));
#15257=CARTESIAN_POINT('Ctrl Pts',(88.1754777859761,-4.48839298437938,-1.23044250245362));
#15258=CARTESIAN_POINT('Ctrl Pts',(88.3710606471085,-1.46454564443096,-4.41755620337796));
#15259=CARTESIAN_POINT('Ctrl Pts',(88.566643508241,2.8644049141729,-3.66809408797527));
#15260=CARTESIAN_POINT('Ctrl Pts',(88.7622263693732,4.64079170288519,0.350079547399718));
#15261=CARTESIAN_POINT('Ctrl Pts',(88.9578092305058,2.28174328173701,4.05629460914468));
#15262=CARTESIAN_POINT('Ctrl Pts',(89.1533920916379,-2.11075463879587,4.14785339298334));
#15263=CARTESIAN_POINT('Ctrl Pts',(89.3489749527706,-4.62202735051278,0.543193777132494));
#15264=CARTESIAN_POINT('Ctrl Pts',(89.5445578139026,-3.01510589170997,-3.54555499571779));
#15265=CARTESIAN_POINT('Ctrl Pts',(89.7401406750352,1.27984042209396,-4.47470945295592));
#15266=CARTESIAN_POINT('Ctrl Pts',(89.9357235361675,4.43184032895884,-1.41651735000079));
#15267=CARTESIAN_POINT('Ctrl Pts',(90.1313063972999,3.6395535853136,2.90428494737804));
#15268=CARTESIAN_POINT('Ctrl Pts',(90.3268892584322,-0.406317802387683,
4.63634881305585));
#15269=CARTESIAN_POINT('Ctrl Pts',(90.4898749760426,-3.45692003612324,2.63754264217168));
#15270=CARTESIAN_POINT('Ctrl Pts',(90.6202635501308,-4.11434965153871,0.0372947584318718));
#15271=CARTESIAN_POINT('Ctrl Pts',(90.6854578371749,-3.80685953223677,-1.25806239083166));
#15272=CARTESIAN_POINT('Ctrl Pts',(90.718054980697,-3.50658272256043,-1.83261987831497));
#15273=CARTESIAN_POINT('Ctrl Pts',(82.4462822981473,2.15601160097152,-3.0276130975709));
#15274=CARTESIAN_POINT('Ctrl Pts',(82.4789247710738,2.65279247650918,-2.67386167718884));
#15275=CARTESIAN_POINT('Ctrl Pts',(82.5441643875223,3.46209197593166,-1.71906719764665));
#15276=CARTESIAN_POINT('Ctrl Pts',(82.6745982910148,4.01722769495016,0.739455456501537));
#15277=CARTESIAN_POINT('Ctrl Pts',(82.8375840086252,2.3117674313423,3.71091534033396));
#15278=CARTESIAN_POINT('Ctrl Pts',(83.0331668697575,-1.81378481829728,3.98037004759811));
#15279=CARTESIAN_POINT('Ctrl Pts',(83.2287497308899,-4.31469025745127,0.697892422788916));
#15280=CARTESIAN_POINT('Ctrl Pts',(83.4243325920222,-2.97475224944107,-3.20408794571452));
#15281=CARTESIAN_POINT('Ctrl Pts',(83.6199154531546,1.01803689051175,-4.25201647004949));
#15282=CARTESIAN_POINT('Ctrl Pts',(83.815498314287,4.10265845038372,-1.51030979164646));
#15283=CARTESIAN_POINT('Ctrl Pts',(84.0110811754194,3.53179429294001,2.57698252079379));
#15284=CARTESIAN_POINT('Ctrl Pts',(84.2066640365517,-0.186557819132022,
4.3680112840683));
#15285=CARTESIAN_POINT('Ctrl Pts',(84.4022468976841,-3.73854991095039,2.26654803530542));
#15286=CARTESIAN_POINT('Ctrl Pts',(84.5978297588165,-3.95909977299548,-1.85464935793378));
#15287=CARTESIAN_POINT('Ctrl Pts',(84.7934126199488,-0.651587312782014,
-4.32314701451353));
#15288=CARTESIAN_POINT('Ctrl Pts',(84.9889954810813,3.23655447064327,-2.93919192186622));
#15289=CARTESIAN_POINT('Ctrl Pts',(85.1845783422135,4.24054292362064,1.06393334227509));
#15290=CARTESIAN_POINT('Ctrl Pts',(85.380161203346,1.46569355865423,4.11896774300371));
#15291=CARTESIAN_POINT('Ctrl Pts',(85.5757440644783,-2.61526374959657,3.50350475271963));
#15292=CARTESIAN_POINT('Ctrl Pts',(85.7713269256107,-4.36570678291,-0.234002566180649));
#15293=CARTESIAN_POINT('Ctrl Pts',(85.966909786743,-2.22577877307914,-3.76298563408145));
#15294=CARTESIAN_POINT('Ctrl Pts',(86.1624926478755,1.89758606638183,-3.93869508048168));
#15295=CARTESIAN_POINT('Ctrl Pts',(86.3580755090077,4.32997322046552,-0.604552785471028));
#15296=CARTESIAN_POINT('Ctrl Pts',(86.5536583701403,2.90383257018886,3.26831889543747));
#15297=CARTESIAN_POINT('Ctrl Pts',(86.7492412312724,-1.10997267862275,4.22872470736441));
#15298=CARTESIAN_POINT('Ctrl Pts',(86.944824092405,-4.13465859302386,1.42082739257919));
#15299=CARTESIAN_POINT('Ctrl Pts',(87.1404069535373,-3.47486555857972,-2.65319829001405));
#15300=CARTESIAN_POINT('Ctrl Pts',(87.3359898146697,0.281451183056565,-4.36290468157959));
#15301=CARTESIAN_POINT('Ctrl Pts',(87.5315726758021,3.78696123245258,-2.18473740738487));
#15302=CARTESIAN_POINT('Ctrl Pts',(87.7271555369346,3.91783218275379,1.9402940550498));
#15303=CARTESIAN_POINT('Ctrl Pts',(87.9227383980667,0.557443592764954,4.33628983310282));
#15304=CARTESIAN_POINT('Ctrl Pts',(88.1183212591992,-3.29969622743145,2.8681288762098));
#15305=CARTESIAN_POINT('Ctrl Pts',(88.3139041203315,-4.21640546044272,-1.15588017897761));
#15306=CARTESIAN_POINT('Ctrl Pts',(88.5094869814639,-1.37579714471017,-4.14986124489519));
#15307=CARTESIAN_POINT('Ctrl Pts',(88.7050698425962,2.69082777801989,-3.44581501570436));
#15308=CARTESIAN_POINT('Ctrl Pts',(88.9006527037287,4.3595691252797,0.328865435888209));
#15309=CARTESIAN_POINT('Ctrl Pts',(89.096235564861,2.14347426037042,3.8104913715631));
#15310=CARTESIAN_POINT('Ctrl Pts',(89.2918184259934,-1.98284718286635,3.89650187854686));
#15311=CARTESIAN_POINT('Ctrl Pts',(89.4874012871258,-4.34194185465522,0.510277334438133));
#15312=CARTESIAN_POINT('Ctrl Pts',(89.6829841482581,-2.83239658155217,-3.33070154424358));
#15313=CARTESIAN_POINT('Ctrl Pts',(89.8785670093905,1.20228468473967,-4.20355112330852));
#15314=CARTESIAN_POINT('Ctrl Pts',(90.0741498705228,4.16327978139733,-1.3306792676446));
#15315=CARTESIAN_POINT('Ctrl Pts',(90.2697327316552,3.41900400969726,2.72829116198692));
#15316=CARTESIAN_POINT('Ctrl Pts',(90.4653155927876,-0.381695766530438,
4.35539546557527));
#15317=CARTESIAN_POINT('Ctrl Pts',(90.6283013103979,-3.24743768367674,2.47771290020874));
#15318=CARTESIAN_POINT('Ctrl Pts',(90.7586898844862,-3.86502839597435,0.035034771608743));
#15319=CARTESIAN_POINT('Ctrl Pts',(90.8238841715303,-3.57617155510303,-1.18182635806204));
#15320=CARTESIAN_POINT('Ctrl Pts',(90.8564813150523,-3.29409091190402,-1.72156682552866));
#15321=CARTESIAN_POINT('',(90.4444676558701,0.0297160312282678,3.7247948877017));
#15322=CARTESIAN_POINT('Ctrl Pts',(90.4430005297901,0.0295740726440573,
3.72695441077287));
#15323=CARTESIAN_POINT('Ctrl Pts',(90.4430005297901,-0.0884458352819756,
3.73973311544784));
#15324=CARTESIAN_POINT('Ctrl Pts',(90.4430005297901,-0.206685143677292,
3.7465459652833));
#15325=CARTESIAN_POINT('Ctrl Pts',(90.4430005297901,-0.324736322595995,
3.74724091818272));
#15326=CARTESIAN_POINT('Ctrl Pts',(90.4430005297901,-0.439290627898788,
3.74791528541344));
#15327=CARTESIAN_POINT('Ctrl Pts',(90.4430005297901,-0.55366870084768,3.74282988407892));
#15328=CARTESIAN_POINT('Ctrl Pts',(90.4430005297901,-0.66757511375052,3.73226995515168));
#15329=CARTESIAN_POINT('Ctrl Pts',(90.4430005297901,-0.784700158626253,
3.72141163630932));
#15330=CARTESIAN_POINT('Ctrl Pts',(90.4430005297901,-0.901327146820539,
3.70476502258063));
#15331=CARTESIAN_POINT('Ctrl Pts',(90.4430005297901,-1.01714336497883,3.68258477181881));
#15332=CARTESIAN_POINT('Ctrl Pts',(90.4430005297901,-1.13295958313712,3.660404521057));
#15333=CARTESIAN_POINT('Ctrl Pts',(90.4430005297901,-1.24796575142807,3.63269035768899));
#15334=CARTESIAN_POINT('Ctrl Pts',(90.4430005297901,-1.36184717318807,3.59964481501032));
#15335=CARTESIAN_POINT('Ctrl Pts',(90.4430005297901,-1.37934384898826,3.59456771693801));
#15336=CARTESIAN_POINT('Ctrl Pts',(90.4430005297901,-1.39681395895271,3.58936467583837));
#15337=CARTESIAN_POINT('Ctrl Pts',(90.4430005297901,-1.41425634058429,3.584036323652));
#15338=CARTESIAN_POINT('Ctrl Pts',(90.4430005297901,-1.43024624853253,3.57915167757696));
#15339=CARTESIAN_POINT('Ctrl Pts',(90.4430005297901,-1.44620373585888,3.57416449842206));
#15340=CARTESIAN_POINT('Ctrl Pts',(90.4430005297901,-1.46212623027145,3.56907619712215));
#15341=CARTESIAN_POINT('Ctrl Pts',(90.4430005297901,-1.57724288748944,3.53228873019729));
#15342=CARTESIAN_POINT('Ctrl Pts',(90.4430005297901,-1.69055927763167,3.49021107252789));
#15343=CARTESIAN_POINT('Ctrl Pts',(90.4430005297901,-1.80175485570888,3.44314758727645));
#15344=CARTESIAN_POINT('Ctrl Pts',(90.4430005297901,-1.91486434019661,3.3952740418798));
#15345=CARTESIAN_POINT('Ctrl Pts',(90.4430005297901,-2.02578012661322,3.34224138479951));
#15346=CARTESIAN_POINT('Ctrl Pts',(90.4430005297901,-2.13416539498154,3.28431509258683));
#15347=CARTESIAN_POINT('Ctrl Pts',(90.4430005297901,-2.2433349494361,3.22596964022727));
#15348=CARTESIAN_POINT('Ctrl Pts',(90.4430005297901,-2.34993804867473,3.16265919293307));
#15349=CARTESIAN_POINT('Ctrl Pts',(90.4430005297901,-2.45361918023358,3.09460343027293));
#15350=CARTESIAN_POINT('Ctrl Pts',(90.4430005297901,-2.50781789043285,3.05902767504775));
#15351=CARTESIAN_POINT('Ctrl Pts',(90.4430005297901,-2.56121787735912,3.02215438256582));
#15352=CARTESIAN_POINT('Ctrl Pts',(90.4430005297901,-2.61376597529677,2.98400978512265));
#15353=CARTESIAN_POINT('Ctrl Pts',(90.4430005297901,-2.64845254685223,2.95883084695753));
#15354=CARTESIAN_POINT('Ctrl Pts',(90.4430005297901,-2.68276789522009,2.93309790327227));
#15355=CARTESIAN_POINT('Ctrl Pts',(90.4430005297901,-2.7166962006516,2.90681771213872));
#15356=CARTESIAN_POINT('Ctrl Pts',(90.4430005297901,-2.74521796869836,2.88472531741983));
#15357=CARTESIAN_POINT('Ctrl Pts',(90.4430005297901,-2.77347318832931,2.86223997607677));
#15358=CARTESIAN_POINT('Ctrl Pts',(90.4430005297901,-2.8013972675781,2.83941177244806));
#15359=CARTESIAN_POINT('Ctrl Pts',(90.4430005297901,-2.89986803616091,2.75891097109109));
#15360=CARTESIAN_POINT('Ctrl Pts',(90.4430005297901,-2.99436179703228,2.67404616107294));
#15361=CARTESIAN_POINT('Ctrl Pts',(90.4430005297901,-3.08452940138303,2.58509397524089));
#15362=CARTESIAN_POINT('Ctrl Pts',(90.4430005297901,-3.17439015065303,2.49644450822192));
#15363=CARTESIAN_POINT('Ctrl Pts',(90.4430005297901,-3.25995494461917,2.40373502869822));
#15364=CARTESIAN_POINT('Ctrl Pts',(90.4430005297901,-3.34085919834289,2.30719182178546));
#15365=CARTESIAN_POINT('Ctrl Pts',(90.4430005297901,-3.41877281360875,2.21421734969377));
#15366=CARTESIAN_POINT('Ctrl Pts',(90.4430005297901,-3.49236462902197,2.11768677390185));
#15367=CARTESIAN_POINT('Ctrl Pts',(90.4430005297901,-3.56128171283005,2.01776553973379));
#15368=CARTESIAN_POINT('Ctrl Pts',(90.4430005297901,-3.57213897168619,2.0020238593747));
#15369=CARTESIAN_POINT('Ctrl Pts',(90.4430005297901,-3.58288014117297,1.98619795895379));
#15370=CARTESIAN_POINT('Ctrl Pts',(90.4430005297901,-3.59350376280769,1.97028841204379));
#15371=CARTESIAN_POINT('Ctrl Pts',(90.4430005297901,-3.65258853086704,1.88180522604296));
#15372=CARTESIAN_POINT('Ctrl Pts',(90.4430005297901,-3.70803921479689,1.79073595284716));
#15373=CARTESIAN_POINT('Ctrl Pts',(90.4430005297901,-3.75982007731666,1.6973347500856));
#15374=CARTESIAN_POINT('Ctrl Pts',(90.4430005297901,-3.76811332474679,1.68237556927864));
#15375=CARTESIAN_POINT('Ctrl Pts',(90.4430005297901,-3.77631159693478,1.66735785530936));
#15376=CARTESIAN_POINT('Ctrl Pts',(90.4430005297901,-3.78440902583728,1.65229362110776));
#15377=CARTESIAN_POINT('Ctrl Pts',(90.4430005297901,-3.84464515396214,1.54023198371691));
#15378=CARTESIAN_POINT('Ctrl Pts',(90.4430005297901,-3.89939440465314,1.42543769098813));
#15379=CARTESIAN_POINT('Ctrl Pts',(90.4430005297901,-3.9486855424696,1.30840674512748));
#15380=CARTESIAN_POINT('Ctrl Pts',(90.4430005297901,-3.99805880821873,1.19118080458689));
#15381=CARTESIAN_POINT('Ctrl Pts',(90.4430005297901,-4.04195599351763,1.07170998780389));
#15382=CARTESIAN_POINT('Ctrl Pts',(90.4430005297901,-4.08036631284025,0.950453612822061));
#15383=CARTESIAN_POINT('Ctrl Pts',(90.4430005297901,-4.11930037137882,0.82754386135488));
#15384=CARTESIAN_POINT('Ctrl Pts',(90.4430005297901,-4.15259726130455,0.70279877082149));
#15385=CARTESIAN_POINT('Ctrl Pts',(90.4430005297901,-4.18020045894591,0.576667891668107));
#15386=CARTESIAN_POINT('Ctrl Pts',(90.4430005297901,-4.20692512936151,0.454551381168132));
#15387=CARTESIAN_POINT('Ctrl Pts',(90.4430005297901,-4.22831276327775,0.331135046718066));
#15388=CARTESIAN_POINT('Ctrl Pts',(90.4430005297901,-4.24426791493629,0.206812112669407));
#15389=CARTESIAN_POINT('Ctrl Pts',(90.4430005297901,-4.24661469917407,0.188525912182953));
#15390=CARTESIAN_POINT('Ctrl Pts',(90.4430005297901,-4.24884387475333,0.170220083948822));
#15391=CARTESIAN_POINT('Ctrl Pts',(90.4430005297901,-4.25095505388501,0.151895867868624));
#15392=CARTESIAN_POINT('Ctrl Pts',(90.4430005297901,-4.25302188555424,0.133956570563175));
#15393=CARTESIAN_POINT('Ctrl Pts',(90.4430005297901,-4.25497512784511,0.116003677579542));
#15394=CARTESIAN_POINT('Ctrl Pts',(90.4430005297901,-4.25681383615621,0.0980463316274628));
#15395=CARTESIAN_POINT('Ctrl Pts',(90.4430005297901,-4.25874402274226,0.0791955829424464));
#15396=CARTESIAN_POINT('Ctrl Pts',(90.4430005297901,-4.2605482999999,0.0603373167362675));
#15397=CARTESIAN_POINT('Ctrl Pts',(90.4430005297901,-4.26222661848671,0.0414729768254311));
#15398=CARTESIAN_POINT('Ctrl Pts',(90.4430005297901,-4.27381294532833,-0.0887576138379506));
#15399=CARTESIAN_POINT('Ctrl Pts',(90.4430005297901,-4.27940028199616,-0.219276168214218));
#15400=CARTESIAN_POINT('Ctrl Pts',(90.4430005297901,-4.27910474674571,-0.349707946183935));
#15401=CARTESIAN_POINT('Ctrl Pts',(90.4430005297901,-4.27880600452057,-0.481555093074704));
#15402=CARTESIAN_POINT('Ctrl Pts',(90.4430005297901,-4.27249612571558,-0.613314293192436));
#15403=CARTESIAN_POINT('Ctrl Pts',(90.4430005297901,-4.26024353119921,-0.744611026846881));
#15404=CARTESIAN_POINT('Ctrl Pts',(90.4430005297901,-4.2544172843308,-0.807044104369089));
#15405=CARTESIAN_POINT('Ctrl Pts',(90.4430005297901,-4.24724656794793,-0.86937272698293));
#15406=CARTESIAN_POINT('Ctrl Pts',(90.4430005297901,-4.23873461501025,-0.931556866122166));
#15407=CARTESIAN_POINT('Ctrl Pts',(90.4430005297901,-4.2351230880836,-0.957940904492233));
#15408=CARTESIAN_POINT('Ctrl Pts',(90.4430005297901,-4.23126959330347,-0.984301416906842));
#15409=CARTESIAN_POINT('Ctrl Pts',(90.4430005297901,-4.22717812966965,-1.01061216318246));
#15410=CARTESIAN_POINT('Ctrl Pts',(90.4430005297901,-4.2065986047346,-1.14295176277282));
#15411=CARTESIAN_POINT('Ctrl Pts',(90.4430005297901,-4.17998717845608,-1.27415495149143));
#15412=CARTESIAN_POINT('Ctrl Pts',(90.4430005297901,-4.14743840998,-1.40383584303523));
#15413=CARTESIAN_POINT('Ctrl Pts',(90.4430005297901,-4.11495992051962,-1.53323672873422));
#15414=CARTESIAN_POINT('Ctrl Pts',(90.4430005297901,-4.07656968007687,-1.66112266026152));
#15415=CARTESIAN_POINT('Ctrl Pts',(90.4430005297901,-4.03231018308459,-1.78711174587462));
#15416=CARTESIAN_POINT('Ctrl Pts',(90.4430005297901,-4.00078732771841,-1.87684470701038));
#15417=CARTESIAN_POINT('Ctrl Pts',(90.4430005297901,-3.96628611272653,-1.96561551660628));
#15418=CARTESIAN_POINT('Ctrl Pts',(90.4430005297901,-3.92880598357856,-2.05328335682074));
#15419=CARTESIAN_POINT('Ctrl Pts',(90.4429666115571,0.0630101736086566,
3.72221671595325));
#15420=CARTESIAN_POINT('Ctrl Pts',(90.4434669596614,0.0519070659346713,
3.72240467081873));
#15421=CARTESIAN_POINT('Ctrl Pts',(90.4439673077658,0.0408031172722711,
3.72254294568215));
#15422=CARTESIAN_POINT('Ctrl Pts',(90.4444676558701,0.0296987722225578,
3.72263153500699));
#15423=CARTESIAN_POINT('Ctrl Pts',(82.4430005297902,1.9774016913413,3.97328893098977));
#15424=CARTESIAN_POINT('Ctrl Pts',(82.4430005297902,2.09010205945686,3.90686165204006));
#15425=CARTESIAN_POINT('Ctrl Pts',(82.4430005297901,2.19942886412691,3.83533535974096));
#15426=CARTESIAN_POINT('Ctrl Pts',(82.4430005297901,2.30496647500187,3.75870816478727));
#15427=CARTESIAN_POINT('Ctrl Pts',(82.4430005297901,2.31220701604366,3.75345105933093));
#15428=CARTESIAN_POINT('Ctrl Pts',(82.4430005297901,2.3194297087469,3.74816992928516));
#15429=CARTESIAN_POINT('Ctrl Pts',(82.4430005297901,2.32663441280681,3.74286476721896));
#15430=CARTESIAN_POINT('Ctrl Pts',(82.4430005297901,2.43426588168457,3.66361066030873));
#15431=CARTESIAN_POINT('Ctrl Pts',(82.4430005297901,2.53788621769259,3.57899596069104));
#15432=CARTESIAN_POINT('Ctrl Pts',(82.4430005297901,2.6373133241208,3.48943324204214));
#15433=CARTESIAN_POINT('Ctrl Pts',(82.4430005297901,2.71277582762782,3.4214575439359));
#15434=CARTESIAN_POINT('Ctrl Pts',(82.4430005297901,2.78582208230832,3.35063071617187));
#15435=CARTESIAN_POINT('Ctrl Pts',(82.4430005297901,2.85635530402485,3.27712288314481));
#15436=CARTESIAN_POINT('Ctrl Pts',(82.4430005297901,2.8718224849478,3.26100340178534));
#15437=CARTESIAN_POINT('Ctrl Pts',(82.4430005297901,2.88716274481628,3.2447612118818));
#15438=CARTESIAN_POINT('Ctrl Pts',(82.4430005297901,2.90237274291231,3.22840114134905));
#15439=CARTESIAN_POINT('Ctrl Pts',(82.4430005297901,2.99230521074578,3.13166861662084));
#15440=CARTESIAN_POINT('Ctrl Pts',(82.4430005297901,3.07771715585099,3.03078619899924));
#15441=CARTESIAN_POINT('Ctrl Pts',(82.4430005297901,3.158442407978,2.92616122334003));
#15442=CARTESIAN_POINT('Ctrl Pts',(82.4430005297901,3.23958388738415,2.82099679109442));
#15443=CARTESIAN_POINT('Ctrl Pts',(82.4430005297901,3.31599056878158,2.71205028395246));
#15444=CARTESIAN_POINT('Ctrl Pts',(82.4430005297901,3.38744699628565,2.59971212298357));
#15445=CARTESIAN_POINT('Ctrl Pts',(82.4430005297901,3.41263912973242,2.56010703718311));
#15446=CARTESIAN_POINT('Ctrl Pts',(82.4430005297901,3.43721553351162,2.52008024063316));
#15447=CARTESIAN_POINT('Ctrl Pts',(82.4430005297901,3.46116526677623,2.4796484520622));
#15448=CARTESIAN_POINT('Ctrl Pts',(82.4430005297901,3.47596320889566,2.45466665955338));
#15449=CARTESIAN_POINT('Ctrl Pts',(82.4430005297901,3.4905218915381,2.42953025043779));
#15450=CARTESIAN_POINT('Ctrl Pts',(82.4430005297901,3.50483857765273,2.4042431483245));
#15451=CARTESIAN_POINT('Ctrl Pts',(82.4430005297901,3.51750213823568,2.38187590865641));
#15452=CARTESIAN_POINT('Ctrl Pts',(82.4430005297901,3.52997604592585,2.35939102284286));
#15453=CARTESIAN_POINT('Ctrl Pts',(82.4430005297901,3.54224655904973,2.33681381979864));
#15454=CARTESIAN_POINT('Ctrl Pts',(82.4430005297901,3.60467283460315,2.22195222564727));
#15455=CARTESIAN_POINT('Ctrl Pts',(82.4430005297901,3.66192221873425,2.10455703827989));
#15456=CARTESIAN_POINT('Ctrl Pts',(82.4430005297901,3.71383452978784,1.98501482074639));
#15457=CARTESIAN_POINT('Ctrl Pts',(82.4430005297901,3.7654562526684,1.86614176152789));
#15458=CARTESIAN_POINT('Ctrl Pts',(82.4430005297901,3.81180071343808,1.74514481543744));
#15459=CARTESIAN_POINT('Ctrl Pts',(82.4430005297901,3.85266154558337,1.62238908638377));
#15460=CARTESIAN_POINT('Ctrl Pts',(82.4430005297901,3.8932624517446,1.50041423725836));
#15461=CARTESIAN_POINT('Ctrl Pts',(82.4430005297901,3.92844948626349,1.37670214001919));
#15462=CARTESIAN_POINT('Ctrl Pts',(82.4430005297901,3.95796854830322,1.25160798889632));
#15463=CARTESIAN_POINT('Ctrl Pts',(82.4430005297901,3.98748761034294,1.12651383777344));
#15464=CARTESIAN_POINT('Ctrl Pts',(82.4430005297901,4.0113389709295,1.00003688317767));
#15465=CARTESIAN_POINT('Ctrl Pts',(82.4430005297901,4.02921301288841,0.87254067379718));
#15466=CARTESIAN_POINT('Ctrl Pts',(82.4430005297901,4.03025722954012,0.865092237390291));
#15467=CARTESIAN_POINT('Ctrl Pts',(82.4430005297901,4.0312810292029,0.857640326545073));
#15468=CARTESIAN_POINT('Ctrl Pts',(82.4430005297901,4.03228434397425,0.850185015481216));
#15469=CARTESIAN_POINT('Ctrl Pts',(82.4430005297901,4.03459129039469,0.833042834718831));
#15470=CARTESIAN_POINT('Ctrl Pts',(82.4430005297901,4.03678865170643,0.815892170444972));
#15471=CARTESIAN_POINT('Ctrl Pts',(82.4430005297901,4.03887577431093,0.798735610694988));
#15472=CARTESIAN_POINT('Ctrl Pts',(82.4430005297901,4.05392301973012,0.675044283433661));
#15473=CARTESIAN_POINT('Ctrl Pts',(82.4430005297901,4.06324834973339,0.551017529415817));
#15474=CARTESIAN_POINT('Ctrl Pts',(82.4430005297901,4.06666460622852,0.426983323709972));
#15475=CARTESIAN_POINT('Ctrl Pts',(82.4430005297901,4.06939901272044,0.327705082224308));
#15476=CARTESIAN_POINT('Ctrl Pts',(82.4430005297901,4.06834683332202,0.228421806365612));
#15477=CARTESIAN_POINT('Ctrl Pts',(82.4430005297901,4.06338801735055,0.129303333680083));
#15478=CARTESIAN_POINT('Ctrl Pts',(82.4430005297901,4.05712876754241,0.00419135438749774));
#15479=CARTESIAN_POINT('Ctrl Pts',(82.4430005297901,4.04464633015305,-0.12065912809382));
#15480=CARTESIAN_POINT('Ctrl Pts',(82.4430005297901,4.02611519956499,-0.24482089419588));
#15481=CARTESIAN_POINT('Ctrl Pts',(82.4430005297901,4.00740439235759,-0.370186524588744));
#15482=CARTESIAN_POINT('Ctrl Pts',(82.4430005297901,3.98252663505701,-0.494850938703189));
#15483=CARTESIAN_POINT('Ctrl Pts',(82.4430005297901,3.9516152925171,-0.618346917085276));
#15484=CARTESIAN_POINT('Ctrl Pts',(82.4430005297901,3.94537341568365,-0.643284257981823));
#15485=CARTESIAN_POINT('Ctrl Pts',(82.4430005297901,3.93888539014275,-0.668173807600427));
#15486=CARTESIAN_POINT('Ctrl Pts',(82.4430005297901,3.93215207449842,-0.693011663701305));
#15487=CARTESIAN_POINT('Ctrl Pts',(82.4430005297901,3.92584560877593,-0.716274955724776));
#15488=CARTESIAN_POINT('Ctrl Pts',(82.4430005297901,3.91932525976329,-0.739487607266908));
#15489=CARTESIAN_POINT('Ctrl Pts',(82.4430005297901,3.91259863317221,-0.762624947309619));
#15490=CARTESIAN_POINT('Ctrl Pts',(82.4430005297901,3.87825099017711,-0.880769322485307));
#15491=CARTESIAN_POINT('Ctrl Pts',(82.4430005297901,3.83848575512177,-0.997112855082767));
#15492=CARTESIAN_POINT('Ctrl Pts',(82.4430005297901,3.79350625410374,-1.11126573136492));
#15493=CARTESIAN_POINT('Ctrl Pts',(82.4430005297901,3.74871960416427,-1.22492917346451));
#15494=CARTESIAN_POINT('Ctrl Pts',(82.4430005297901,3.6987628126906,-1.33642146078559));
#15495=CARTESIAN_POINT('Ctrl Pts',(82.4430005297901,3.64379183897507,-1.44533316841575));
#15496=CARTESIAN_POINT('Ctrl Pts',(82.4430005297901,3.59527253015452,-1.54146246028581));
#15497=CARTESIAN_POINT('Ctrl Pts',(82.4430005297901,3.54284611646389,-1.63558134564552));
#15498=CARTESIAN_POINT('Ctrl Pts',(82.4430005297901,3.48659512784046,-1.7273852613035));
#15499=CARTESIAN_POINT('Ctrl Pts',(82.4430005297901,3.4267302138798,-1.82508725102156));
#15500=CARTESIAN_POINT('Ctrl Pts',(82.4430005297901,3.36253323060098,-1.92016776201096));
#15501=CARTESIAN_POINT('Ctrl Pts',(82.4430005297901,3.2941636601901,-2.01234893030668));
#15502=CARTESIAN_POINT('Ctrl Pts',(82.4430005297901,3.28199925485566,-2.02874992695785));
#15503=CARTESIAN_POINT('Ctrl Pts',(82.4430005297901,3.26970271301345,-2.04505905011743));
#15504=CARTESIAN_POINT('Ctrl Pts',(82.4430005297901,3.25727487268007,-2.06127461217243));
#15505=CARTESIAN_POINT('Ctrl Pts',(82.4430005297901,3.2464949893423,-2.07533995760013));
#15506=CARTESIAN_POINT('Ctrl Pts',(82.4430005297901,3.23562112293147,-2.08932859706152));
#15507=CARTESIAN_POINT('Ctrl Pts',(82.4430005297901,3.22465780066579,-2.10323500148988));
#15508=CARTESIAN_POINT('Ctrl Pts',(82.4430005297901,3.15047393397067,-2.19733338036832));
#15509=CARTESIAN_POINT('Ctrl Pts',(82.4430005297901,3.07214423094984,-2.28773884704917));
#15510=CARTESIAN_POINT('Ctrl Pts',(82.4430005297901,2.98991394062545,-2.37420105585054));
#15511=CARTESIAN_POINT('Ctrl Pts',(82.4430005297901,2.90806315298578,-2.46026423115419));
#15512=CARTESIAN_POINT('Ctrl Pts',(82.4430005297901,2.82234707698341,-2.54242092978593));
#15513=CARTESIAN_POINT('Ctrl Pts',(82.4430005297901,2.73297569139553,-2.62038408613581));
#15514=CARTESIAN_POINT('Ctrl Pts',(82.4430005297901,2.64463815610224,-2.69744536285576));
#15515=CARTESIAN_POINT('Ctrl Pts',(82.4430005297901,2.55272879796832,-2.77040993931852));
#15516=CARTESIAN_POINT('Ctrl Pts',(82.4430005297901,2.45742821329426,-2.83895504478));
#15517=CARTESIAN_POINT('Ctrl Pts',(82.4430005297901,2.3621276286202,-2.90750015024147));
#15518=CARTESIAN_POINT('Ctrl Pts',(82.4430005297901,2.26343528681409,-2.97162624539));
#15519=CARTESIAN_POINT('Ctrl Pts',(82.4430005297901,2.16151778945158,-3.03095833168065));
#15520=CARTESIAN_POINT('Origin',(81.4430005297901,0.,0.));
#15521=CARTESIAN_POINT('',(82.4430005297901,-5.42440960677665,-6.64298586220318E-16));
#15522=CARTESIAN_POINT('Origin',(82.4430005297901,0.,0.));
#15523=CARTESIAN_POINT('',(81.4430005297901,-5.42440960677665,-6.64298586220318E-16));
#15524=CARTESIAN_POINT('',(81.4430005297901,-5.42440960677665,-6.64298586220318E-16));
#15525=CARTESIAN_POINT('Origin',(81.4430005297901,0.,0.));
#15526=CARTESIAN_POINT('Origin',(82.4430005297901,0.,0.));
#15527=CARTESIAN_POINT('Origin',(90.4430005297901,0.,0.));
#15528=CARTESIAN_POINT('Origin',(81.4430005297901,0.,0.));
#27690=UNCERTAINTY_MEASURE_WITH_UNIT(LENGTH_MEASURE(0.01),#27708,
'DISTANCE_ACCURACY_VALUE',
'Maximum model space distance between geometric entities at asserted c
onnectivities');
#27695=UNCERTAINTY_MEASURE_WITH_UNIT(LENGTH_MEASURE(0.01),#27708,
'DISTANCE_ACCURACY_VALUE',
'Maximum model space distance between geometric entities at asserted c
onnectivities');
#27702=(
GEOMETRIC_REPRESENTATION_CONTEXT(3)
GLOBAL_UNCERTAINTY_ASSIGNED_CONTEXT((#27690))
GLOBAL_UNIT_ASSIGNED_CONTEXT((#27708,#27710,#27711))
REPRESENTATION_CONTEXT('','3D')
);
#27707=(
GEOMETRIC_REPRESENTATION_CONTEXT(3)
GLOBAL_UNCERTAINTY_ASSIGNED_CONTEXT((#27695))
GLOBAL_UNIT_ASSIGNED_CONTEXT((#27708,#27710,#27711))
REPRESENTATION_CONTEXT('','3D')
);
#27708=(
LENGTH_UNIT()
NAMED_UNIT(*)
SI_UNIT(.MILLI.,.METRE.)
);
#27710=(
NAMED_UNIT(*)
PLANE_ANGLE_UNIT()
SI_UNIT($,.RADIAN.)
);
#27711=(
NAMED_UNIT(*)
SI_UNIT($,.STERADIAN.)
SOLID_ANGLE_UNIT()
);
#27718=SHAPE_DEFINITION_REPRESENTATION(#27729,#27750);
#27729=PRODUCT_DEFINITION_SHAPE('',$,#27762);
#27750=SHAPE_REPRESENTATION('',(#4064),#27702);
#27755=PRODUCT_DEFINITION_CONTEXT('part definition',#27790,'design');
#27762=PRODUCT_DEFINITION('Screw','Screw',#27773,#27755);
#27773=PRODUCT_DEFINITION_FORMATION('',$,#27798);
#27790=APPLICATION_CONTEXT(
'Core Data for Automotive Mechanical Design Process');
#27791=PRODUCT_CONTEXT('part definition',#27790,'mechanical');
#27798=PRODUCT('Screw','Screw',$,(#27791));
#27804=PRESENTATION_STYLE_ASSIGNMENT((#27806));
#27806=SURFACE_STYLE_USAGE(.BOTH.,#27808);
#27808=SURFACE_SIDE_STYLE('',(#27810));
#27810=SURFACE_STYLE_FILL_AREA(#27812);
#27812=FILL_AREA_STYLE('Opaque(160,160,160)',(#27814));
#27814=FILL_AREA_STYLE_COLOUR('Opaque(160,160,160)',#27816);
#27816=COLOUR_RGB('Opaque(160,160,160)', 0.09019608, 0.27058824, 0.51372549);
ENDSEC;
END-ISO-10303-21;
